ISO-10303-21;
HEADER;
FILE_DESCRIPTION (('STEP AP214'),
    '1' );
FILE_NAME ('Finger.step',
    '2026-10-24T18:16:00',
    ( '' ),
    ( '' ),
    'SwSTEP 2.0',
    'SolidWorks 2025',
    '' );
FILE_SCHEMA (( 'AUTOMOTIVE_DESIGN' ));
ENDSEC;

DATA;
#1=CARTESIAN_POINT ( 'NONE',  ( -1.293236445124221312, 0.1355266887446167634, -0.03937007874015747977 ) ) ;
#7=EDGE_LOOP ( 'NONE', ( #10556, #3231, #5022, #13216 ) ) ;
#11=LINE ( 'NONE', #8523, #4655 ) ;
#12=CARTESIAN_POINT ( 'NONE',  ( -1.955186753849255776, -2.907980768360570067, -0.09148540428083716536 ) ) ;
#13=DIRECTION ( 'NONE',  ( -1.000000000000000000, 0.000000000000000000, 0.000000000000000000 ) ) ;
#16=CARTESIAN_POINT ( 'NONE',  ( -1.584115185264708403, 0.1296286773226380251, 0.03937007874015747977 ) ) ;
#18=CARTESIAN_POINT ( 'NONE',  ( -1.944256225378947711, -2.934796208935224637, 0.02867658400294463561 ) ) ;
#21=CARTESIAN_POINT ( 'NONE',  ( -1.599581448071076606, 0.1086921510886041942, 0.04859056056449020944 ) ) ;
#24=ORIENTED_EDGE ( 'NONE', *, *, #10025, .F. ) ;
#35=CARTESIAN_POINT ( 'NONE',  ( -1.352291563234457650, 0.1355266887446167634, -0.05905511811023622659 ) ) ;
#37=FACE_OUTER_BOUND ( 'NONE', #11677, .T. ) ;
#43=CARTESIAN_POINT ( 'NONE',  ( -1.592395536721568750, 0.1185427911281754926, -0.04121422034918896526 ) ) ;
#48=CARTESIAN_POINT ( 'NONE',  ( -1.964126537190516331, -2.749515453455444014, -0.1756903148397123138 ) ) ;
#57=ADVANCED_FACE ( 'NONE', ( #7220 ), #9740, .F. ) ;
#60=ORIENTED_EDGE ( 'NONE', *, *, #3949, .F. ) ;
#70=CARTESIAN_POINT ( 'NONE',  ( -1.580259682937487753, 0.1018956540318996240, -0.04477369844321320291 ) ) ;
#78=CARTESIAN_POINT ( 'NONE',  ( -2.156935286759944503, -2.012462723082548699, 0.1097304796145711775 ) ) ;
#80=CARTESIAN_POINT ( 'NONE',  ( -2.755905511811024056, -1.630597114118274238, 0.1033464566929129663 ) ) ;
#85=CARTESIAN_POINT ( 'NONE',  ( -2.061746446265113608, -2.382934929162861870, 0.1354791600993499601 ) ) ;
#87=CARTESIAN_POINT ( 'NONE',  ( -1.964126537190516997, -2.752050336136266928, -0.1561691687464109024 ) ) ;
#89=CARTESIAN_POINT ( 'NONE',  ( -0.07002599089419501988, 0.1451652216336531964, -0.05905511811023623353 ) ) ;
#92=CIRCLE ( 'NONE', #4574, 0.01968503937007874335 ) ;
#94=ORIENTED_EDGE ( 'NONE', *, *, #12675, .F. ) ;
#98=CARTESIAN_POINT ( 'NONE',  ( -1.411977487489316063, -0.03773484711301355182, 0.05405189641583445226 ) ) ;
#101=CIRCLE ( 'NONE', #8849, 0.03937007874015747977 ) ;
#108=CARTESIAN_POINT ( 'NONE',  ( -1.185590517044430081, 0.3351394466080224732, -0.05695402829526142324 ) ) ;
#109=CARTESIAN_POINT ( 'NONE',  ( -0.07635964791965739462, -0.1878198040935885327, 0.05905511811023622659 ) ) ;
#122=B_SPLINE_CURVE_WITH_KNOTS ( 'NONE', 3,
 ( #1208, #10680, #10591, #8541, #2360, #2582, #3476, #7059, #15378, #1126 ),
 .UNSPECIFIED., .F., .F.,
 ( 4, 2, 2, 2, 4 ),
 ( 6.547728381081633163E-06, 0.0002695768667942076403, 0.0005326060052073337261, 0.0007956351436204597578, 0.001058664282033585681 ),
 .UNSPECIFIED. ) ;
#128=EDGE_CURVE ( 'NONE', #7239, #11495, #15042, .T. ) ;
#134=CIRCLE ( 'NONE', #2132, 0.03937007874015751446 ) ;
#139=CARTESIAN_POINT ( 'NONE',  ( -0.01899774626693613230, 0.1736125314593575386, 0.03244910060855325795 ) ) ;
#144=CIRCLE ( 'NONE', #6605, 3.169291338582677753 ) ;
#165=EDGE_CURVE ( 'NONE', #4902, #13738, #13884, .T. ) ;
#166=SPHERICAL_SURFACE ( 'NONE', #13897, 0.01968503937007873988 ) ;
#167=CARTESIAN_POINT ( 'NONE',  ( -1.576192857444134843, 0.1076040293811589832, 0.06348264010174455019 ) ) ;
#171=EDGE_CURVE ( 'NONE', #11793, #14788, #383, .T. ) ;
#175=CIRCLE ( 'NONE', #5908, 0.01968503937007872948 ) ;
#176=CARTESIAN_POINT ( 'NONE',  ( -1.892121628034221459, -2.891752770451749388, 0.1316657767305224880 ) ) ;
#178=CARTESIAN_POINT ( 'NONE',  ( -1.953781456863171062, -2.911486273847457618, 0.08694686177389875092 ) ) ;
#181=ORIENTED_EDGE ( 'NONE', *, *, #8447, .T. ) ;
#183=ORIENTED_EDGE ( 'NONE', *, *, #1290, .T. ) ;
#189=CIRCLE ( 'NONE', #9445, 0.2106299212598415904 ) ;
#191=CARTESIAN_POINT ( 'NONE',  ( -1.293236445124221312, 0.1355266887446167634, 0.03937007874015747977 ) ) ;
#192=FACE_OUTER_BOUND ( 'NONE', #8001, .T. ) ;
#199=CARTESIAN_POINT ( 'NONE',  ( -0.04290857128006120985, -0.1835146052580345633, 0.05099426193563244558 ) ) ;
#207=ORIENTED_EDGE ( 'NONE', *, *, #14794, .T. ) ;
#210=DIRECTION ( 'NONE',  ( 0.000000000000000000, -1.000000000000000000, 0.000000000000000000 ) ) ;
#214=DIRECTION ( 'NONE',  ( -0.000000000000000000, 0.000000000000000000, 1.000000000000000000 ) ) ;
#217=CIRCLE ( 'NONE', #10951, 0.01968503937007873988 ) ;
#218=CARTESIAN_POINT ( 'NONE',  ( -1.392036056571634317, -0.02280807183030207283, 0.03937007874015747283 ) ) ;
#221=EDGE_LOOP ( 'NONE', ( #1582, #15254, #8822, #2376 ) ) ;
#225=CIRCLE ( 'NONE', #12233, 0.2303149606299203511 ) ;
#236=ORIENTED_EDGE ( 'NONE', *, *, #15238, .T. ) ;
#244=CARTESIAN_POINT ( 'NONE',  ( -0.07022707542947252690, -0.1870727099175784891, -0.03937007874015747283 ) ) ;
#245=CARTESIAN_POINT ( 'NONE',  ( -2.119441840507266139, -2.390209328812086031, 0.1345547373476347619 ) ) ;
#247=CARTESIAN_POINT ( 'NONE',  ( -1.909668712890198128, -2.916752030038837873, 0.1028102154675972768 ) ) ;
#254=ORIENTED_EDGE ( 'NONE', *, *, #8368, .F. ) ;
#261=CARTESIAN_POINT ( 'NONE',  ( -2.755905511811024056, -1.630597114118275348, -8.792486876640390747 ) ) ;
#263=CARTESIAN_POINT ( 'NONE',  ( -0.07545607570875818848, 0.1645859079935991787, -0.03937007874015747977 ) ) ;
#264=ORIENTED_EDGE ( 'NONE', *, *, #12028, .T. ) ;
#265=CARTESIAN_POINT ( 'NONE',  ( -1.574484809660039453, 0.1100025355994339177, -0.06175692796179814426 ) ) ;
#268=B_SPLINE_CURVE_WITH_KNOTS ( 'NONE', 3,
 ( #14257, #2333, #15438, #8372 ),
 .UNSPECIFIED., .F., .F.,
 ( 4, 4 ),
 ( 0.000000000000000000, 0.0006039794861555876143 ),
 .UNSPECIFIED. ) ;
#269=PLANE ( 'NONE',  #3681 ) ;
#271=EDGE_CURVE ( 'NONE', #2172, #6534, #268, .T. ) ;
#283=CARTESIAN_POINT ( 'NONE',  ( -1.596293587998474317, 0.1133155780026106618, 0.1968503937007874127 ) ) ;
#289=CARTESIAN_POINT ( 'NONE',  ( -2.024460782843922058, -2.569698609574572856, -0.1523405278397521878 ) ) ;
#290=CARTESIAN_POINT ( 'NONE',  ( -1.943748422590784841, -2.936027745407755685, -0.02327475659521720600 ) ) ;
#291=DIRECTION ( 'NONE',  ( -0.000000000000000000, -0.000000000000000000, -1.000000000000000000 ) ) ;
#292=DIRECTION ( 'NONE',  ( 0.000000000000000000, 1.000000000000000000, 9.367506770274758310E-14 ) ) ;
#296=CARTESIAN_POINT ( 'NONE',  ( -1.908307771495521443, -2.849947446465292522, 0.1332780079517500438 ) ) ;
#310=DIRECTION ( 'NONE',  ( -0.000000000000000000, 0.000000000000000000, 1.000000000000000000 ) ) ;
#314=CARTESIAN_POINT ( 'NONE',  ( -1.878928142437690685, -2.924394872804905621, 0.09130279448639455619 ) ) ;
#316=DIRECTION ( 'NONE',  ( -0.000000000000000000, -0.000000000000000000, -1.000000000000000000 ) ) ;
#317=EDGE_CURVE ( 'NONE', #12712, #11793, #134, .T. ) ;
#318=CARTESIAN_POINT ( 'NONE',  ( -1.596030944582886857, 0.1136756404968294887, 0.04477369844403809168 ) ) ;
#330=ADVANCED_FACE ( 'NONE', ( #1096 ), #166, .T. ) ;
#333=AXIS2_PLACEMENT_3D ( 'NONE', #13224, #2486, #10943 ) ;
#338=EDGE_LOOP ( 'NONE', ( #3355, #15265, #8955, #2444 ) ) ;
#345=CARTESIAN_POINT ( 'NONE',  ( -2.058602741089746946, -2.286826958241420016, 0.1276646238208032913 ) ) ;
#349=DIRECTION ( 'NONE',  ( 1.000000000000000000, 0.000000000000000000, 0.000000000000000000 ) ) ;
#360=AXIS2_PLACEMENT_3D ( 'NONE', #5949, #6017, #3378 ) ;
#362=VECTOR ( 'NONE', #2138, 39.37007874015748143 ) ;
#365=CARTESIAN_POINT ( 'NONE',  ( -1.943201140612624389, -2.937347705060309622, 0.005521057543908070714 ) ) ;
#369=CIRCLE ( 'NONE', #11114, 0.01968503937007875723 ) ;
#374=CARTESIAN_POINT ( 'NONE',  ( -1.879680750885767360, -2.922298882358313588, 0.01177973773464270624 ) ) ;
#383=CIRCLE ( 'NONE', #9126, 0.01968503937007875723 ) ;
#385=ORIENTED_EDGE ( 'NONE', *, *, #15256, .T. ) ;
#387=B_SPLINE_CURVE_WITH_KNOTS ( 'NONE', 3,
 ( #15169, #13044, #14234, #2304, #4431, #9218 ),
 .UNSPECIFIED., .F., .F.,
 ( 4, 2, 4 ),
 ( 0.000000000000000000, 0.0002588876643434665946, 0.0005177753286869331891 ),
 .UNSPECIFIED. ) ;
#388=CARTESIAN_POINT ( 'NONE',  ( -1.399712685083875030, -0.02644324258679336959, -0.07678689349530590236 ) ) ;
#390=CARTESIAN_POINT ( 'NONE',  ( -1.580080891953811628, 0.1020406297922293454, 0.1968503937007874127 ) ) ;
#393=AXIS2_PLACEMENT_3D ( 'NONE', #707, #4367, #10316 ) ;
#396=CARTESIAN_POINT ( 'NONE',  ( -1.871202120571936245, -2.943029077962952211, 0.04801288353396620384 ) ) ;
#399=CARTESIAN_POINT ( 'NONE',  ( -2.188516668597769499, -1.823600774912196520, -0.1033333524236228068 ) ) ;
#404=EDGE_CURVE ( 'NONE', #9943, #2172, #9224, .T. ) ;
#405=AXIS2_PLACEMENT_3D ( 'NONE', #1476, #4981, #10945 ) ;
#417=DIRECTION ( 'NONE',  ( 1.000000000000000000, -6.938893903907222856E-15, 0.000000000000000000 ) ) ;
#421=( CONVERSION_BASED_UNIT ( 'INCH', #12482 ) LENGTH_UNIT ( ) NAMED_UNIT ( #1062 ) );
#422=EDGE_CURVE ( 'NONE', #6873, #14162, #4769, .T. ) ;
#432=CARTESIAN_POINT ( 'NONE',  ( -2.092239122479251368, -2.009552950301321861, 0.08993382972064449532 ) ) ;
#452=EDGE_LOOP ( 'NONE', ( #15074, #4990 ) ) ;
#457=CARTESIAN_POINT ( 'NONE',  ( -1.925024858772766745, -2.949472151676825860, -0.01333363273917731115 ) ) ;
#461=FACE_OUTER_BOUND ( 'NONE', #11373, .T. ) ;
#462=DIRECTION ( 'NONE',  ( 6.484947573745102394E-15, -1.000000000000000000, 2.431855340154413200E-16 ) ) ;
#465=CARTESIAN_POINT ( 'NONE',  ( -1.915481817270058729, -2.830827465095222983, -0.1437034448495827788 ) ) ;
#466=CARTESIAN_POINT ( 'NONE',  ( -2.054789683517501242, -2.568945684013816066, -0.1522427580697401084 ) ) ;
#467=CARTESIAN_POINT ( 'NONE',  ( -1.276200637803905691, -0.1988000726501942539, 0.08366141732283455257 ) ) ;
#472=ADVANCED_FACE ( 'NONE', ( #7735 ), #4183, .T. ) ;
#475=CARTESIAN_POINT ( 'NONE',  ( -1.409468994508474404, -0.007141353241660916562, -0.06138260383184675206 ) ) ;
#478=LINE ( 'NONE', #390, #6847 ) ;
#483=CARTESIAN_POINT ( 'NONE',  ( -1.883836775286372056, -2.912146259469937881, -0.05616283913476798756 ) ) ;
#485=CARTESIAN_POINT ( 'NONE',  ( -2.119441840505075447, -2.390209328808487133, -0.1345547373467393670 ) ) ;
#486=CARTESIAN_POINT ( 'NONE',  ( -1.234181327013985197, 0.1355266887446167634, -0.03937007874015747977 ) ) ;
#491=DIRECTION ( 'NONE',  ( 0.000000000000000000, -0.000000000000000000, 1.000000000000000000 ) ) ;
#492=CARTESIAN_POINT ( 'NONE',  ( -0.4722458785514955237, -0.6629481244416842722, 0.07874015748031495954 ) ) ;
#495=ORIENTED_EDGE ( 'NONE', *, *, #9928, .F. ) ;
#496=CARTESIAN_POINT ( 'NONE',  ( -1.568343923620152180, 0.1178486908565801600, -0.05905511811023622659 ) ) ;
#501=ORIENTED_EDGE ( 'NONE', *, *, #13678, .T. ) ;
#502=EDGE_LOOP ( 'NONE', ( #12142, #12674, #7426, #14352 ) ) ;
#505=EDGE_CURVE ( 'NONE', #6948, #6036, #613, .T. ) ;
#507=CYLINDRICAL_SURFACE ( 'NONE', #14125, 0.03937007874015751446 ) ;
#508=ADVANCED_FACE ( 'NONE', ( #11025 ), #2235, .T. ) ;
#519=PLANE ( 'NONE',  #5081 ) ;
#520=CARTESIAN_POINT ( 'NONE',  ( -1.945810312050074042, -2.931088922611430281, -0.07891651694308547682 ) ) ;
#524=CARTESIAN_POINT ( 'NONE',  ( -1.973160353001477185, -2.810434395070632529, -0.1731278957434206622 ) ) ;
#525=CARTESIAN_POINT ( 'NONE',  ( -1.880200301354544967, -2.921039053327021850, 0.02314659398703503707 ) ) ;
#532=VERTEX_POINT ( 'NONE', #9284 ) ;
#533=ORIENTED_EDGE ( 'NONE', *, *, #2731, .T. ) ;
#538=CARTESIAN_POINT ( 'NONE',  ( -1.511943070284283097, 0.2262540267724839904, -0.05905511811023622659 ) ) ;
#542=CARTESIAN_POINT ( 'NONE',  ( -1.908381546755280489, -2.920376482534968954, 0.09751899391724366817 ) ) ;
#544=CARTESIAN_POINT ( 'NONE',  ( -2.156938452688012653, -2.012428322113554824, -0.1097289591313703738 ) ) ;
#546=EDGE_CURVE ( 'NONE', #2999, #877, #1956, .T. ) ;
#552=CARTESIAN_POINT ( 'NONE',  ( -1.100415514366371639, -0.04998955061625894036, 0.1968503937007874127 ) ) ;
#555=CARTESIAN_POINT ( 'NONE',  ( -0.04290857128006120985, -0.1835146052580345633, -0.05099426193563244558 ) ) ;
#557=CARTESIAN_POINT ( 'NONE',  ( -2.041848724490688216, -2.380718792664717309, 0.1160226956207114496 ) ) ;
#561=PRODUCT_DEFINITION ( 'UNKNOWN', '', #4613, #13178 ) ;
#564=( BOUNDED_SURFACE ( )  B_SPLINE_SURFACE ( 3, 2, ( 
 ( #9561, #13304, #3604 ),
 ( #9494, #8383, #12152 ),
 ( #3458, #10571, #1102 ),
 ( #6014, #3760, #11926 ),
 ( #15444, #10661, #10801 ),
 ( #1193, #13168, #4844 ),
 ( #9649, #14426, #3688 ),
 ( #3529, #13010, #4707 ),
 ( #8466, #8300, #12065 ),
 ( #8529, #7275, #1327 ),
 ( #8236, #6086, #10885 ),
 ( #14188, #176, #2568 ),
 ( #7345, #15356, #3825 ),
 ( #247, #4057, #6241 ),
 ( #542, #2662, #1645 ),
 ( #8609, #314, #8768 ),
 ( #14802, #5293, #13394 ),
 ( #10095, #11196, #7434 ),
 ( #1555, #4143, #5064 ),
 ( #12370, #13537, #4998 ),
 ( #8840, #396, #14882 ),
 ( #2799, #7670, #12295 ),
 ( #6308, #5150, #9870 ),
 ( #14740, #5227, #13710 ),
 ( #7743, #12234, #1493 ),
 ( #11030, #8936, #2975 ),
 ( #7509, #7571, #3917 ),
 ( #14655, #8699, #11104 ),
 ( #2739, #9958, #13473 ),
 ( #6403, #3994, #483 ),
 ( #10021, #13618, #2889 ),
 ( #12460, #1726, #6485 ),
 ( #11270, #1418, #6173 ),
 ( #10965, #9794, #14564 ),
 ( #5615, #13781, #2097 ),
 ( #937, #15191, #6872 ),
 ( #10252, #6714, #11505 ),
 ( #1872, #12604, #11431 ),
 ( #4455, #11667, #11574 ),
 ( #12826, #15264, #9074 ),
 ( #9009, #4220, #4285 ),
 ( #9238, #3350, #14011 ),
 ( #8044, #7901, #2017 ),
 ( #4523, #5529, #5693 ),
 ( #13851, #623, #3273 ),
 ( #9159, #13937, #11341 ) ),
 .UNSPECIFIED., .F., .F., .T. ) 
 B_SPLINE_SURFACE_WITH_KNOTS ( ( 4, 2, 2, 2, 2, 2, 2, 2, 2, 2, 2, 2, 2, 2, 2, 2, 2, 2, 2, 2, 2, 2, 4 ),
 ( 3, 3 ),
 ( 1.561251128379126385E-17, 0.0008753252358572001296, 0.001312987853785792334, 0.001750650471714384647, 0.002625975707571569055, 0.003501300943428753681, 0.004376626179285938306, 0.004814288797214530402, 0.005251951415143122498, 0.005689614033071714594, 0.006127276651000306690, 0.007002601886857491749, 0.007440264504786084712, 0.007877927122714676808, 0.008315589740643268904, 0.008753252358571861000, 0.009628577594429045192, 0.01050390283028622938, 0.01137922806614341531, 0.01225455330200059950, 0.01269221591992919160, 0.01312987853785778369, 0.01400520377371496789 ),
 ( 0.000000000000000000, 1.000000000000000000 ),
 .UNSPECIFIED. ) 
 GEOMETRIC_REPRESENTATION_ITEM ( )  RATIONAL_B_SPLINE_SURFACE ( (
 ( 1.000000000000000000, 0.7214151048184059833, 1.000000000000000000),
 ( 1.000000000000000000, 0.7139268977831511043, 1.000000000000000000),
 ( 1.000000000000000000, 0.7060919310600005661, 1.000000000000000000),
 ( 1.000000000000000000, 0.6937785501687134815, 1.000000000000000000),
 ( 1.000000000000000000, 0.6895805778049280965, 1.000000000000000000),
 ( 1.000000000000000000, 0.6809903301727727731, 1.000000000000000000),
 ( 1.000000000000000000, 0.6765849663043156381, 1.000000000000000000),
 ( 1.000000000000000000, 0.6633648450980306199, 1.000000000000000000),
 ( 1.000000000000000000, 0.6544550762639834707, 1.000000000000000000),
 ( 1.000000000000000000, 0.6365533617521316190, 1.000000000000000000),
 ( 1.000000000000000000, 0.6275095611399463813, 1.000000000000000000),
 ( 1.000000000000000000, 0.6103974523277966302, 1.000000000000000000),
 ( 1.000000000000000000, 0.6022255868237532672, 1.000000000000000000),
 ( 1.000000000000000000, 0.5908555208068133613, 1.000000000000000000),
 ( 1.000000000000000000, 0.5872289930507547107, 1.000000000000000000),
 ( 1.000000000000000000, 0.5805233329111295637, 1.000000000000000000),
 ( 1.000000000000000000, 0.5774191828807228033, 1.000000000000000000),
 ( 1.000000000000000000, 0.5717609404363922510, 1.000000000000000000),
 ( 1.000000000000000000, 0.5692067459845615573, 1.000000000000000000),
 ( 1.000000000000000000, 0.5647184317875526549, 1.000000000000000000),
 ( 1.000000000000000000, 0.5627791062741893668, 1.000000000000000000),
 ( 1.000000000000000000, 0.5581324696273656238, 1.000000000000000000),
 ( 1.000000000000000000, 0.5565289020892307814, 1.000000000000000000),
 ( 1.000000000000000000, 0.5564933751953636820, 1.000000000000000000),
 ( 1.000000000000000000, 0.5568862388217724613, 1.000000000000000000),
 ( 1.000000000000000000, 0.5584481643512820837, 1.000000000000000000),
 ( 1.000000000000000000, 0.5596129212104073991, 1.000000000000000000),
 ( 1.000000000000000000, 0.5626655503097565125, 1.000000000000000000),
 ( 1.000000000000000000, 0.5645534494397981273, 1.000000000000000000),
 ( 1.000000000000000000, 0.5690213772211072385, 1.000000000000000000),
 ( 1.000000000000000000, 0.5716084335653097703, 1.000000000000000000),
 ( 1.000000000000000000, 0.5801336838986037581, 1.000000000000000000),
 ( 1.000000000000000000, 0.5868791499827269442, 1.000000000000000000),
 ( 1.000000000000000000, 0.6020378157228721827, 1.000000000000000000),
 ( 1.000000000000000000, 0.6103019064041214081, 1.000000000000000000),
 ( 1.000000000000000000, 0.6274511639639016591, 1.000000000000000000),
 ( 1.000000000000000000, 0.6364857471627143326, 1.000000000000000000),
 ( 1.000000000000000000, 0.6544235474393820251, 1.000000000000000000),
 ( 1.000000000000000000, 0.6633507613998016472, 1.000000000000000000),
 ( 1.000000000000000000, 0.6765956464743652088, 1.000000000000000000),
 ( 1.000000000000000000, 0.6810032293232968215, 1.000000000000000000),
 ( 1.000000000000000000, 0.6895857131701266240, 1.000000000000000000),
 ( 1.000000000000000000, 0.6937808971552223980, 1.000000000000000000),
 ( 1.000000000000000000, 0.7060887547132419506, 1.000000000000000000),
 ( 1.000000000000000000, 0.7139238139413449646, 1.000000000000000000),
 ( 1.000000000000000000, 0.7214151048184016535, 1.000000000000000000) ) ) 
 REPRESENTATION_ITEM ( '' )  SURFACE ( )  );
#567=CARTESIAN_POINT ( 'NONE',  ( -2.011752225599860111, -2.517072610070153260, 0.1485602497173309500 ) ) ;
#568=CARTESIAN_POINT ( 'NONE',  ( 0.7052242655755273093, -1.858423098537180129, 0.08366141732283417787 ) ) ;
#570=DIRECTION ( 'NONE',  ( 1.349229370204184172E-15, 1.000000000000000000, 0.000000000000000000 ) ) ;
#574=CIRCLE ( 'NONE', #3077, 0.05905511811023620578 ) ;
#579=VERTEX_POINT ( 'NONE', #4664 ) ;
#586=ORIENTED_EDGE ( 'NONE', *, *, #12186, .T. ) ;
#591=CARTESIAN_POINT ( 'NONE',  ( -1.989672796122207599, -2.818351438590611213, 0.1526128802498082915 ) ) ;
#594=FACE_BOUND ( 'NONE', #5065, .T. ) ;
#596=AXIS2_PLACEMENT_3D ( 'NONE', #15015, #4033, #9052 ) ;
#602=CARTESIAN_POINT ( 'NONE',  ( -2.110117761716791218, -1.869184722427368772, -0.1064922012049425715 ) ) ;
#613=LINE ( 'NONE', #2653, #3638 ) ;
#623=CARTESIAN_POINT ( 'NONE',  ( -1.942129868064559339, -2.755778082694033682, -0.1769297588256847076 ) ) ;
#631=VERTEX_POINT ( 'NONE', #2299 ) ;
#634=EDGE_CURVE ( 'NONE', #12118, #2668, #1496, .T. ) ;
#643=DIRECTION ( 'NONE',  ( 0.000000000000000000, -1.000000000000000000, 2.224004456380530778E-16 ) ) ;
#651=CARTESIAN_POINT ( 'NONE',  ( -1.182292270647294030, 0.3416831661896216898, 0.04963306832873103785 ) ) ;
#661=CARTESIAN_POINT ( 'NONE',  ( -0.04047196874988819026, 0.1700209211169182444, -0.02286660095797711165 ) ) ;
#664=CIRCLE ( 'NONE', #5395, 2.814960629921260171 ) ;
#670=ADVANCED_FACE ( 'NONE', ( #1450 ), #9682, .T. ) ;
#681=CARTESIAN_POINT ( 'NONE',  ( -1.509677571405407148, 0.2301488344313167012, -0.03937007874015747977 ) ) ;
#682=CARTESIAN_POINT ( 'NONE',  ( -1.991652262238867044, -2.812949666188107489, 0.1538927778953757264 ) ) ;
#688=CIRCLE ( 'NONE', #9938, 0.01968503937007873988 ) ;
#690=CARTESIAN_POINT ( 'NONE',  ( -2.163017314575554462, -1.630597114118274238, -0.1033464566929129386 ) ) ;
#707=CARTESIAN_POINT ( 'NONE',  ( -1.100415514366370084, -0.04998955061625977997, -0.03937007874015747977 ) ) ;
#720=EDGE_CURVE ( 'NONE', #6036, #11956, #9160, .T. ) ;
#723=CARTESIAN_POINT ( 'NONE',  ( -1.276200637803905691, -0.1988000726501942539, -0.1033464566929132716 ) ) ;
#732=ADVANCED_FACE ( 'NONE', ( #5026 ), #4962, .T. ) ;
#736=ORIENTED_EDGE ( 'NONE', *, *, #5648, .T. ) ;
#739=CARTESIAN_POINT ( 'NONE',  ( -0.004432333661848699216, 0.1530140478773363566, -0.007791225829895984979 ) ) ;
#744=DIRECTION ( 'NONE',  ( -0.6722799013647171584, 0.7402970580929294497, 0.000000000000000000 ) ) ;
#749=VERTEX_POINT ( 'NONE', #7305 ) ;
#754=CARTESIAN_POINT ( 'NONE',  ( -2.090051324975687130, -2.010834692585359296, -0.09065852675045296682 ) ) ;
#757=CARTESIAN_POINT ( 'NONE',  ( -0.07874015748031501505, 0.1442356988431298948, -0.05905511811023622659 ) ) ;
#763=EDGE_LOOP ( 'NONE', ( #10546, #5020, #7300, #14173 ) ) ;
#766=CARTESIAN_POINT ( 'NONE',  ( -2.163017314575554462, -1.630597114118274238, 0.1033464566929129663 ) ) ;
#768=FACE_OUTER_BOUND ( 'NONE', #1689, .T. ) ;
#770=DIRECTION ( 'NONE',  ( -0.000000000000000000, -0.000000000000000000, -1.000000000000000000 ) ) ;
#781=CARTESIAN_POINT ( 'NONE',  ( -1.509677571405407148, 0.2301488344313167012, 0.05905511811023622659 ) ) ;
#802=CARTESIAN_POINT ( 'NONE',  ( 0.7052242655755273093, -1.858423098537180129, 0.1968503937007874127 ) ) ;
#811=EDGE_LOOP ( 'NONE', ( #1997, #5279, #9049, #3550, #14729 ) ) ;
#817=CARTESIAN_POINT ( 'NONE',  ( -1.332606523864378945, 0.1355266887446167634, -0.03937007874015747977 ) ) ;
#838=CARTESIAN_POINT ( 'NONE',  ( -0.004867930653576267239, 0.1761271985363120074, 0.009096853601420660032 ) ) ;
#861=CARTESIAN_POINT ( 'NONE',  ( -1.925560620047871874, -2.948015126518888529, 0.02361865587082091072 ) ) ;
#871=DIRECTION ( 'NONE',  ( 1.000000000000000000, 0.000000000000000000, 0.000000000000000000 ) ) ;
#874=CARTESIAN_POINT ( 'NONE',  ( -1.419615703680148000, -0.01226548409420232313, -0.08366141732283458032 ) ) ;
#877=VERTEX_POINT ( 'NONE', #8967 ) ;
#880=VERTEX_POINT ( 'NONE', #8794 ) ;
#882=CARTESIAN_POINT ( 'NONE',  ( -0.2362204724409448231, -0.02638708502139245488, 0.05905511811023622659 ) ) ;
#884=CARTESIAN_POINT ( 'NONE',  ( -1.591501945092674841, 0.08600752902535288569, -0.08366141732283462196 ) ) ;
#888=DIRECTION ( 'NONE',  ( -0.9162674345903500939, 0.4005670834070347297, 0.000000000000000000 ) ) ;
#894=EDGE_CURVE ( 'NONE', #2999, #13968, #13406, .T. ) ;
#898=CIRCLE ( 'NONE', #10156, 0.01968503937007875723 ) ;
#904=EDGE_LOOP ( 'NONE', ( #14618, #3065, #11206, #13154, #5873, #3253, #1821, #183, #12999, #7983 ) ) ;
#909=CYLINDRICAL_SURFACE ( 'NONE', #12864, 0.03937007874015747977 ) ;
#911=B_SPLINE_CURVE_WITH_KNOTS ( 'NONE', 3,
 ( #9915, #1684, #1754, #1594 ),
 .UNSPECIFIED., .F., .F.,
 ( 4, 4 ),
 ( 0.01504928987911790389, 0.01565334703627738883 ),
 .UNSPECIFIED. ) ;
#915=CARTESIAN_POINT ( 'NONE',  ( -1.100415514366356762, -0.04998955061627542718, 0.03937007874015747977 ) ) ;
#919=CARTESIAN_POINT ( 'NONE',  ( -1.398495881576244493, -0.02731002314121872693, 0.08366141732283458032 ) ) ;
#924=VERTEX_POINT ( 'NONE', #5720 ) ;
#925=VERTEX_POINT ( 'NONE', #8076 ) ;
#928=VECTOR ( 'NONE', #570, 39.37007874015748143 ) ;
#930=FACE_OUTER_BOUND ( 'NONE', #13768, .T. ) ;
#937=CARTESIAN_POINT ( 'NONE',  ( -1.923247296301440645, -2.877714865856489723, -0.1429548596504897628 ) ) ;
#939=DIRECTION ( 'NONE',  ( 0.5984233124757303290, 0.8011800915434523773, -4.135314009930608449E-15 ) ) ;
#940=DIRECTION ( 'NONE',  ( 0.5750876580239419056, 0.8180917953313906477, 0.000000000000000000 ) ) ;
#941=TOROIDAL_SURFACE ( 'NONE', #3941, 0.03937007874015747977, 0.01968503937007873988 ) ;
#942=EDGE_LOOP ( 'NONE', ( #5409, #11759, #13942 ) ) ;
#946=ORIENTED_EDGE ( 'NONE', *, *, #3969, .F. ) ;
#953=CARTESIAN_POINT ( 'NONE',  ( -1.985311755390326782, -2.772329397582949717, -0.1771653543307079026 ) ) ;
#959=DIRECTION ( 'NONE',  ( -1.000000000000000000, 0.000000000000000000, 0.000000000000000000 ) ) ;
#962=CARTESIAN_POINT ( 'NONE',  ( -0.008251140381529234111, 0.1525182358981298780, 0.01646613645217641017 ) ) ;
#969=ORIENTED_EDGE ( 'NONE', *, *, #11355, .T. ) ;
#978=CARTESIAN_POINT ( 'NONE',  ( -1.941057606383688183, -2.905071431831486528, -0.1180179303142062930 ) ) ;
#993=CARTESIAN_POINT ( 'NONE',  ( -1.897883522938190959, -2.949475805367709480, 0.01220870853311090999 ) ) ;
#1000=DIRECTION ( 'NONE',  ( -0.000000000000000000, 0.000000000000000000, 1.000000000000000000 ) ) ;
#1010=DIRECTION ( 'NONE',  ( 0.000000000000000000, -1.000000000000000000, 0.000000000000000000 ) ) ;
#1011=CARTESIAN_POINT ( 'NONE',  ( -0.03726199245315515995, 0.1489178558047651590, 0.04781523662142502656 ) ) ;
#1012=EDGE_CURVE ( 'NONE', #6200, #9631, #5093, .T. ) ;
#1020=ORIENTED_EDGE ( 'NONE', *, *, #4376, .F. ) ;
#1022=EDGE_LOOP ( 'NONE', ( #5341, #2667 ) ) ;
#1025=CARTESIAN_POINT ( 'NONE',  ( -1.925013044204064050, -2.949504264475041992, 0.005679328437135281946 ) ) ;
#1033=CARTESIAN_POINT ( 'NONE',  ( -0.06155496847469425076, 0.1461038053415525118, 0.05764730824460247843 ) ) ;
#1036=ADVANCED_FACE ( 'NONE', ( #15374 ), #11609, .F. ) ;
#1049=EDGE_LOOP ( 'NONE', ( #4952, #1462, #9924, #12331 ) ) ;
#1050=DIRECTION ( 'NONE',  ( -0.000000000000000000, 0.000000000000000000, 1.000000000000000000 ) ) ;
#1060=CARTESIAN_POINT ( 'NONE',  ( -1.929388278599686757, -2.859527306003167624, -0.1546535441990251891 ) ) ;
#1062=DIMENSIONAL_EXPONENTS ( 1.000000000000000000, 0.000000000000000000, 0.000000000000000000, 0.000000000000000000, 0.000000000000000000, 0.000000000000000000, 0.000000000000000000 ) ;
#1063=CARTESIAN_POINT ( 'NONE',  ( -1.959562225762719878, -2.764756976402351185, -0.1771653543306641321 ) ) ;
#1068=EDGE_CURVE ( 'NONE', #14001, #14806, #7204, .T. ) ;
#1071=EDGE_CURVE ( 'NONE', #3617, #14001, #11, .T. ) ;
#1073=ORIENTED_EDGE ( 'NONE', *, *, #4324, .F. ) ;
#1076=EDGE_CURVE ( 'NONE', #9943, #13968, #6081, .T. ) ;
#1078=DIRECTION ( 'NONE',  ( -0.000000000000000000, -2.212657494868377674E-16, -1.000000000000000000 ) ) ;
#1092=ADVANCED_FACE ( 'NONE', ( #13387 ), #3589, .T. ) ;
#1096=FACE_OUTER_BOUND ( 'NONE', #3085, .T. ) ;
#1097=VECTOR ( 'NONE', #5408, 39.37007874015748143 ) ;
#1099=CYLINDRICAL_SURFACE ( 'NONE', #1860, 0.1771653543307079026 ) ;
#1102=CARTESIAN_POINT ( 'NONE',  ( -1.938117758475286001, -2.767509491613813655, 0.1578460832164983174 ) ) ;
#1110=EDGE_CURVE ( 'NONE', #5248, #14646, #12526, .T. ) ;
#1111=CARTESIAN_POINT ( 'NONE',  ( -1.598024000616091067, 0.1108860284103144050, 0.04651097583972436250 ) ) ;
#1126=CARTESIAN_POINT ( 'NONE',  ( -1.607606114292111199, 0.09732815221480045631, -0.07874015748031495954 ) ) ;
#1128=AXIS2_PLACEMENT_3D ( 'NONE', #12813, #11885, #4676 ) ;
#1134=EDGE_LOOP ( 'NONE', ( #4813, #11868, #6038, #12518 ) ) ;
#1135=CARTESIAN_POINT ( 'NONE',  ( -1.596293587998450780, 0.1133155780026439408, -0.04477369844320916448 ) ) ;
#1137=DIRECTION ( 'NONE',  ( 0.9926610512904576744, 0.1209298856814283729, -0.000000000000000000 ) ) ;
#1139=CIRCLE ( 'NONE', #12894, 2.214566929133857887 ) ;
#1142=ORIENTED_EDGE ( 'NONE', *, *, #7498, .T. ) ;
#1146=ORIENTED_EDGE ( 'NONE', *, *, #3577, .T. ) ;
#1150=CARTESIAN_POINT ( 'NONE',  ( -1.939652992539211640, -2.828352525160966024, 0.1684558939921211862 ) ) ;
#1151=( NAMED_UNIT ( * ) PLANE_ANGLE_UNIT ( ) SI_UNIT ( $, .RADIAN. ) );
#1152=AXIS2_PLACEMENT_3D ( 'NONE', #15103, #770, #15035 ) ;
#1164=CIRCLE ( 'NONE', #7652, 2.795275590551181466 ) ;
#1169=CARTESIAN_POINT ( 'NONE',  ( -0.02344272421052690653, 0.1505984473678075031, 0.03705048130897044961 ) ) ;
#1182=CIRCLE ( 'NONE', #3924, 0.01968503937007875723 ) ;
#1185=DIRECTION ( 'NONE',  ( -0.8144815189573203495, 0.5801894994542524664, -0.000000000000000000 ) ) ;
#1186=CARTESIAN_POINT ( 'NONE',  ( -1.927081998786787986, -2.943867889510814795, 0.04476392992596674864 ) ) ;
#1187=CIRCLE ( 'NONE', #14183, 0.01968503937007875723 ) ;
#1190=CARTESIAN_POINT ( 'NONE',  ( 0.9851651268172137987, -1.725292181286280480, 0.1968503937007874127 ) ) ;
#1193=CARTESIAN_POINT ( 'NONE',  ( -1.945358927863352072, -2.810530894188501883, 0.1731069454022728660 ) ) ;
#1195=CARTESIAN_POINT ( 'NONE',  ( -1.947553218330493774, -2.926780783575864131, -0.05681056732657507186 ) ) ;
#1208=CARTESIAN_POINT ( 'NONE',  ( -1.596293587998450780, 0.1133155780026439408, -0.04477369844320916448 ) ) ;
#1210=AXIS2_PLACEMENT_3D ( 'NONE', #11174, #13373, #11016 ) ;
#1237=ORIENTED_EDGE ( 'NONE', *, *, #15345, .T. ) ;
#1242=CARTESIAN_POINT ( 'NONE',  ( -2.107117561417118701, -2.011956994529711995, -0.1111970799389148945 ) ) ;
#1257=CARTESIAN_POINT ( 'NONE',  ( -0.02018259705034725071, -0.1802452534892125813, 1.049219007154695292E-17 ) ) ;
#1258=DIRECTION ( 'NONE',  ( -0.000000000000000000, -0.000000000000000000, -1.000000000000000000 ) ) ;
#1261=CARTESIAN_POINT ( 'NONE',  ( -1.943861602385431375, -2.935750972982893447, 0.02297894316446263269 ) ) ;
#1263=DIRECTION ( 'NONE',  ( 1.349229370204184172E-15, 1.000000000000000000, 0.000000000000000000 ) ) ;
#1264=ORIENTED_EDGE ( 'NONE', *, *, #10230, .T. ) ;
#1267=ORIENTED_EDGE ( 'NONE', *, *, #5390, .F. ) ;
#1283=EDGE_CURVE ( 'NONE', #14180, #10993, #4357, .T. ) ;
#1286=ORIENTED_EDGE ( 'NONE', *, *, #2735, .F. ) ;
#1290=EDGE_CURVE ( 'NONE', #532, #10983, #3267, .T. ) ;
#1293=CARTESIAN_POINT ( 'NONE',  ( -1.939653092248158073, -2.828352430279280405, -0.1684573650302815528 ) ) ;
#1297=CARTESIAN_POINT ( 'NONE',  ( -1.511943070284283097, 0.2262540267724839904, -0.03937007874015747977 ) ) ;
#1307=CARTESIAN_POINT ( 'NONE',  ( -2.110117738960459732, -1.869206010357609138, -0.1064927656600950512 ) ) ;
#1310=EDGE_CURVE ( 'NONE', #10983, #14128, #2903, .T. ) ;
#1321=CARTESIAN_POINT ( 'NONE',  ( -1.063205505495480097, 0.7941372572243097228, -0.05905511811023622659 ) ) ;
#1325=CARTESIAN_POINT ( 'NONE',  ( -2.099929645851249305, -2.385360057864538419, 0.1341722008959284895 ) ) ;
#1327=CARTESIAN_POINT ( 'NONE',  ( -1.908398435458060760, -2.849708334410140154, 0.1334289122196857802 ) ) ;
#1328=EDGE_LOOP ( 'NONE', ( #10548, #501, #5156, #7523, #3720 ) ) ;
#1335=AXIS2_PLACEMENT_3D ( 'NONE', #10250, #13616, #7667 ) ;
#1344=AXIS2_PLACEMENT_3D ( 'NONE', #14460, #10919, #11875 ) ;
#1345=CARTESIAN_POINT ( 'NONE',  ( -0.03802712947489396422, 0.1704066588063142818, -0.02158149019474813607 ) ) ;
#1347=CARTESIAN_POINT ( 'NONE',  ( -1.596214514713377719, 0.1135332889814023166, -0.07874015748031495954 ) ) ;
#1370=EDGE_CURVE ( 'NONE', #5863, #7929, #9298, .T. ) ;
#1373=DIRECTION ( 'NONE',  ( 0.1408070410764336311, -0.9900370584898827708, 0.000000000000000000 ) ) ;
#1374=AXIS2_PLACEMENT_3D ( 'NONE', #14211, #4317, #888 ) ;
#1390=CARTESIAN_POINT ( 'NONE',  ( -1.607606114292111199, 0.09732815221480045631, 0.1968503937007874127 ) ) ;
#1391=AXIS2_PLACEMENT_3D ( 'NONE', #4365, #6870, #2183 ) ;
#1393=DIRECTION ( 'NONE',  ( 0.000000000000000000, -0.000000000000000000, 1.000000000000000000 ) ) ;
#1395=DIRECTION ( 'NONE',  ( -0.5750876580239486779, -0.8180917953313858737, 4.257489128596104324E-15 ) ) ;
#1403=ORIENTED_EDGE ( 'NONE', *, *, #8453, .F. ) ;
#1405=VECTOR ( 'NONE', #11986, 39.37007874015748143 ) ;
#1409=EDGE_LOOP ( 'NONE', ( #10744, #181, #7674, #8724 ) ) ;
#1410=CARTESIAN_POINT ( 'NONE',  ( -2.163017314575554462, -1.630597114118274238, 0.1033464566929129663 ) ) ;
#1412=AXIS2_PLACEMENT_3D ( 'NONE', #3432, #14237, #13126 ) ;
#1414=CARTESIAN_POINT ( 'NONE',  ( -0.04711866733795024020, -0.1840656518295272215, -0.03212400068286348082 ) ) ;
#1415=FACE_OUTER_BOUND ( 'NONE', #2478, .T. ) ;
#1418=CARTESIAN_POINT ( 'NONE',  ( -1.881677119634339812, -2.917705953332184965, -0.1022915504730082664 ) ) ;
#1432=CARTESIAN_POINT ( 'NONE',  ( -0.2362204724409448231, -0.02638708502139245488, -0.05905511811023622659 ) ) ;
#1438=CARTESIAN_POINT ( 'NONE',  ( -1.527714331928839098, 0.2380340132385416752, 0.05905511811023622659 ) ) ;
#1439=CARTESIAN_POINT ( 'NONE',  ( -1.591501945092674841, 0.08600752902535288569, -0.08366141732283462196 ) ) ;
#1448=ORIENTED_EDGE ( 'NONE', *, *, #12770, .T. ) ;
#1450=FACE_OUTER_BOUND ( 'NONE', #3414, .T. ) ;
#1455=CARTESIAN_POINT ( 'NONE',  ( -0.05270315828015968707, 0.1680450278838720446, 0.03205052537796105466 ) ) ;
#1462=ORIENTED_EDGE ( 'NONE', *, *, #5234, .T. ) ;
#1465=ADVANCED_FACE ( 'NONE', ( #2945 ), #5641, .T. ) ;
#1466=ORIENTED_EDGE ( 'NONE', *, *, #8268, .F. ) ;
#1470=CARTESIAN_POINT ( 'NONE',  ( -1.947525890741732768, -2.926847465874895526, -0.05663733393484523398 ) ) ;
#1476=CARTESIAN_POINT ( 'NONE',  ( -0.2362204724409448231, -0.02638708502139245488, -0.03937007874015747977 ) ) ;
#1486=ORIENTED_EDGE ( 'NONE', *, *, #3577, .F. ) ;
#1487=CARTESIAN_POINT ( 'NONE',  ( -1.394658405437710913, -0.02432317279348940667, -0.06446726223640240894 ) ) ;
#1493=CARTESIAN_POINT ( 'NONE',  ( -1.879798054437352262, -2.922014039083816073, -0.01138495494166368548 ) ) ;
#1496=( BOUNDED_CURVE ( )  B_SPLINE_CURVE ( 3, ( #4741, #10917, #43, #2693 ),
 .UNSPECIFIED., .F., .T. ) 
 B_SPLINE_CURVE_WITH_KNOTS ( ( 4, 4 ),
 ( 4.712388980384695003, 5.242505698889619481 ),
 .UNSPECIFIED. ) 
 CURVE ( )  GEOMETRIC_REPRESENTATION_ITEM ( )  RATIONAL_B_SPLINE_CURVE ( ( 1.000000000000000000, 0.9767181429391863512, 0.9767181429391863512, 1.000000000000000000 ) ) 
 REPRESENTATION_ITEM ( '' )  );
#1503=DIRECTION ( 'NONE',  ( 1.000000000000000000, 0.000000000000000000, 0.000000000000000000 ) ) ;
#1504=CYLINDRICAL_SURFACE ( 'NONE', #3473, 0.01968503937007877111 ) ;
#1505=FACE_OUTER_BOUND ( 'NONE', #3880, .T. ) ;
#1507=LINE ( 'NONE', #10984, #13420 ) ;
#1508=EDGE_CURVE ( 'NONE', #9996, #3964, #11821, .T. ) ;
#1509=CARTESIAN_POINT ( 'NONE',  ( -1.293236445124221312, 0.1355266887446167634, -0.05905511811023622659 ) ) ;
#1514=VERTEX_POINT ( 'NONE', #6758 ) ;
#1532=CARTESIAN_POINT ( 'NONE',  ( -1.940424138356921180, -2.944104218312575849, -0.04384797139731677618 ) ) ;
#1539=CARTESIAN_POINT ( 'NONE',  ( -1.919185151238703479, -2.820797091852851768, 0.1478778761745188075 ) ) ;
#1545=ORIENTED_EDGE ( 'NONE', *, *, #10385, .F. ) ;
#1551=DIRECTION ( 'NONE',  ( 0.8144815189573204606, -0.5801894994542525774, -1.283760644411384396E-16 ) ) ;
#1553=CARTESIAN_POINT ( 'NONE',  ( -2.163017314575554906, -1.630597114118274238, 0.1033464566929130218 ) ) ;
#1554=CARTESIAN_POINT ( 'NONE',  ( -1.187879871879865767, 0.3305938048772316673, 0.05905511811023621271 ) ) ;
#1555=CARTESIAN_POINT ( 'NONE',  ( -1.902132589539931917, -2.937797416315981458, 0.06363563951555976927 ) ) ;
#1559=CARTESIAN_POINT ( 'NONE',  ( -1.588286453767632000, 0.1240441066494159250, 0.03937007874189642903 ) ) ;
#1560=DIRECTION ( 'NONE',  ( 0.000000000000000000, -0.000000000000000000, -1.000000000000000000 ) ) ;
#1566=( BOUNDED_SURFACE ( )  B_SPLINE_SURFACE ( 3, 2, ( 
 ( #13244, #13476, #318 ),
 ( #8772, #7512, #14743 ),
 ( #3764, #2803, #1559 ),
 ( #2742, #13540, #8612 ) ),
 .UNSPECIFIED., .F., .F., .T. ) 
 B_SPLINE_SURFACE_WITH_KNOTS ( ( 4, 4 ),
 ( 3, 3 ),
 ( 4.182272261839050209, 4.712388980384689674 ),
 ( 0.000000000000000000, 1.000000000000000000 ),
 .UNSPECIFIED. ) 
 GEOMETRIC_REPRESENTATION_ITEM ( )  RATIONAL_B_SPLINE_SURFACE ( (
 ( 1.000000000000000000, 0.7111298678012015761, 1.000000000000000000),
 ( 1.000000000000000000, 0.7099209393060977868, 1.000000000000000000),
 ( 1.000000000000000000, 0.7085172298915587419, 1.000000000000000000),
 ( 1.000000000000000000, 0.7071067811865475727, 1.000000000000000000) ) ) 
 REPRESENTATION_ITEM ( '' )  SURFACE ( )  );
#1567=FACE_OUTER_BOUND ( 'NONE', #8723, .T. ) ;
#1568=CARTESIAN_POINT ( 'NONE',  ( -2.163017314575554462, -1.630597114118274238, -0.08366141732283423338 ) ) ;
#1569=CARTESIAN_POINT ( 'NONE',  ( -0.06327586242532841354, -0.1861954285973654311, -0.03830155300069465474 ) ) ;
#1572=CARTESIAN_POINT ( 'NONE',  ( -2.077963565069627982, -2.158389492283137479, 0.09850863663452619212 ) ) ;
#1576=CARTESIAN_POINT ( 'NONE',  ( -1.234181327013985197, 0.1355266887446167634, -0.05905511811023622659 ) ) ;
#1579=CARTESIAN_POINT ( 'NONE',  ( -1.419615703680148000, -0.01226548409420231273, -0.07874015748031495954 ) ) ;
#1580=CIRCLE ( 'NONE', #8334, 0.2165354330708662012 ) ;
#1582=ORIENTED_EDGE ( 'NONE', *, *, #8272, .F. ) ;
#1594=CARTESIAN_POINT ( 'NONE',  ( -1.992382107315057160, -2.749515453455444014, -0.1756903148397123138 ) ) ;
#1606=AXIS2_PLACEMENT_3D ( 'NONE', #9961, #1648, #6406 ) ;
#1609=ORIENTED_EDGE ( 'NONE', *, *, #2027, .F. ) ;
#1612=CARTESIAN_POINT ( 'NONE',  ( -1.940983278890547004, -2.905281415726287619, 0.1177841364776334443 ) ) ;
#1619=CARTESIAN_POINT ( 'NONE',  ( -2.003351654124630343, -2.780426454911686829, -0.1578453099020075412 ) ) ;
#1624=CARTESIAN_POINT ( 'NONE',  ( -1.417802900492933782, -0.04287136159519136513, 0.08366141732283458032 ) ) ;
#1625=CYLINDRICAL_SURFACE ( 'NONE', #6824, 0.2106299212598417292 ) ;
#1645=CARTESIAN_POINT ( 'NONE',  ( -1.890104583037259589, -2.896615591685024249, 0.08668355014530308711 ) ) ;
#1648=DIRECTION ( 'NONE',  ( 0.5984233124757313282, 0.8011800915434514891, 0.000000000000000000 ) ) ;
#1650=DIRECTION ( 'NONE',  ( 0.000000000000000000, -1.000000000000000000, 0.000000000000000000 ) ) ;
#1651=ORIENTED_EDGE ( 'NONE', *, *, #5556, .F. ) ;
#1652=ORIENTED_EDGE ( 'NONE', *, *, #2355, .F. ) ;
#1657=VECTOR ( 'NONE', #10481, 39.37007874015748143 ) ;
#1662=CARTESIAN_POINT ( 'NONE',  ( -0.07874015748031520934, 1.062385330869439640E-16, -0.01968503937007873988 ) ) ;
#1664=ORIENTED_EDGE ( 'NONE', *, *, #2711, .T. ) ;
#1666=CARTESIAN_POINT ( 'NONE',  ( -1.596030944582063960, 0.1136756404979306911, -0.04477369844321314740 ) ) ;
#1667=CARTESIAN_POINT ( 'NONE',  ( 0.9851651268172137987, -1.725292181286280480, 0.08366141732283420562 ) ) ;
#1674=ORIENTED_EDGE ( 'NONE', *, *, #13331, .T. ) ;
#1675=EDGE_CURVE ( 'NONE', #7280, #9631, #15001, .T. ) ;
#1681=CARTESIAN_POINT ( 'NONE',  ( -1.961142902483386852, -2.698831051917248480, 0.1691401727068858885 ) ) ;
#1683=AXIS2_PLACEMENT_3D ( 'NONE', #14080, #939, #3352 ) ;
#1684=CARTESIAN_POINT ( 'NONE',  ( -1.987685136288601218, -2.764754373406230314, -0.1771653543307125100 ) ) ;
#1689=EDGE_LOOP ( 'NONE', ( #3630, #60, #946, #5736 ) ) ;
#1697=CARTESIAN_POINT ( 'NONE',  ( -1.944063115746497372, -2.896559852577519134, 0.1269213948424093574 ) ) ;
#1698=EDGE_CURVE ( 'NONE', #7635, #532, #11684, .T. ) ;
#1702=CARTESIAN_POINT ( 'NONE',  ( -2.007605986780809815, -2.768314085474279373, -0.1776672152077323208 ) ) ;
#1706=CARTESIAN_POINT ( 'NONE',  ( -0.01545036047008872468, -0.1795454119435216378, -8.867015126428109484E-14 ) ) ;
#1707=EDGE_CURVE ( 'NONE', #1942, #532, #189, .T. ) ;
#1716=CIRCLE ( 'NONE', #14472, 0.01968503937007873988 ) ;
#1720=CARTESIAN_POINT ( 'NONE',  ( -0.1968503937007873295, -0.02638708502139245141, 0.03937007874015747977 ) ) ;
#1726=CARTESIAN_POINT ( 'NONE',  ( -1.878738707309701272, -2.924867600962848702, -0.09124266643724603110 ) ) ;
#1732=ORIENTED_EDGE ( 'NONE', *, *, #8232, .T. ) ;
#1741=DIRECTION ( 'NONE',  ( -1.000000000000000000, 0.000000000000000000, 0.000000000000000000 ) ) ;
#1750=CARTESIAN_POINT ( 'NONE',  ( -0.08151194962748890827, 0.1637246173173402264, -0.05905511811023622659 ) ) ;
#1754=CARTESIAN_POINT ( 'NONE',  ( -1.990041936606229189, -2.757150128560895475, -0.1766817015956954062 ) ) ;
#1760=EDGE_CURVE ( 'NONE', #6534, #10712, #8315, .T. ) ;
#1763=ORIENTED_EDGE ( 'NONE', *, *, #8788, .T. ) ;
#1764=EDGE_CURVE ( 'NONE', #5035, #11956, #7944, .T. ) ;
#1768=CARTESIAN_POINT ( 'NONE',  ( -1.993480072126341041, -2.602359853078048513, -0.1374116847797290930 ) ) ;
#1770=CARTESIAN_POINT ( 'NONE',  ( -1.965394281685034050, -2.834131647928828546, -0.1664892934202782671 ) ) ;
#1776=CARTESIAN_POINT ( 'NONE',  ( -2.090210618530727871, -1.821590950714383261, -0.1053165596881613930 ) ) ;
#1780=ADVANCED_FACE ( 'NONE', ( #3626 ), #6027, .F. ) ;
#1784=CARTESIAN_POINT ( 'NONE',  ( -1.419615703584982569, -0.01226548416199267633, -0.07606650080514479328 ) ) ;
#1797=VERTEX_POINT ( 'NONE', #5964 ) ;
#1803=DIRECTION ( 'NONE',  ( 0.000000000000000000, 2.212657494868377674E-16, 1.000000000000000000 ) ) ;
#1804=CARTESIAN_POINT ( 'NONE',  ( -0.07635964791965738074, -0.1878198040935885327, -0.03937007874015747977 ) ) ;
#1807=DIRECTION ( 'NONE',  ( -0.8144815189573203495, 0.5801894994542524664, -0.000000000000000000 ) ) ;
#1808=CARTESIAN_POINT ( 'NONE',  ( -0.004461712539986224628, -0.1607679992104108779, 0.007865172455356563355 ) ) ;
#1811=ORIENTED_EDGE ( 'NONE', *, *, #8765, .F. ) ;
#1815=CARTESIAN_POINT ( 'NONE',  ( -2.100501784635051550, -1.630597114118274460, 0.08366141732283423338 ) ) ;
#1816=CARTESIAN_POINT ( 'NONE',  ( -0.06144837730693395589, 0.1461156186057537831, -0.05762996311186197040 ) ) ;
#1817=FACE_OUTER_BOUND ( 'NONE', #11527, .T. ) ;
#1821=ORIENTED_EDGE ( 'NONE', *, *, #1707, .T. ) ;
#1823=CIRCLE ( 'NONE', #14629, 0.05905511811023620578 ) ;
#1833=CIRCLE ( 'NONE', #2832, 0.2106299212598415904 ) ;
#1842=ADVANCED_FACE ( 'NONE', ( #10593 ), #14209, .T. ) ;
#1850=CARTESIAN_POINT ( 'NONE',  ( -2.090430055232860962, -1.869646201002890251, -0.08681428844356724184 ) ) ;
#1851=VECTOR ( 'NONE', #12251, 39.37007874015748143 ) ;
#1860=AXIS2_PLACEMENT_3D ( 'NONE', #13071, #14329, #2497 ) ;
#1867=CARTESIAN_POINT ( 'NONE',  ( -1.352291563234457650, 0.1355266887446167634, 0.05905511811023622659 ) ) ;
#1872=CARTESIAN_POINT ( 'NONE',  ( -1.934019134851861166, -2.845595952726013067, -0.1617770776497191865 ) ) ;
#1873=VERTEX_POINT ( 'NONE', #4487 ) ;
#1877=VECTOR ( 'NONE', #11584, 39.37007874015748143 ) ;
#1878=ORIENTED_EDGE ( 'NONE', *, *, #5390, .T. ) ;
#1883=CARTESIAN_POINT ( 'NONE',  ( -1.352291563234457650, 0.1355266887446167634, -0.03937007874015747977 ) ) ;
#1884=CIRCLE ( 'NONE', #12650, 0.01968503937007879193 ) ;
#1895=CARTESIAN_POINT ( 'NONE',  ( -1.990519559797095939, -2.601568177549060668, 0.1382274484396485426 ) ) ;
#1897=ADVANCED_FACE ( 'NONE', ( #6913 ), #3399, .T. ) ;
#1900=ADVANCED_FACE ( 'NONE', ( #14671 ), #3775, .F. ) ;
#1909=LINE ( 'NONE', #11533, #4663 ) ;
#1911=CARTESIAN_POINT ( 'NONE',  ( -0.02897706919690611060, 0.1719584017861309766, -0.007005952774887016718 ) ) ;
#1916=CARTESIAN_POINT ( 'NONE',  ( -1.572611271870161920, 0.1123963381035097825, 0.05997718891489349502 ) ) ;
#1917=ORIENTED_EDGE ( 'NONE', *, *, #10166, .F. ) ;
#1918=DIRECTION ( 'NONE',  ( -0.5984233124757303290, -0.8011800915434521553, 0.000000000000000000 ) ) ;
#1920=VECTOR ( 'NONE', #8565, 39.37007874015748143 ) ;
#1927=CARTESIAN_POINT ( 'NONE',  ( -1.981861006536024927, -2.839447705569534186, 0.1644972641858484519 ) ) ;
#1929=CARTESIAN_POINT ( 'NONE',  ( -1.962410390378336977, -2.889890278503658649, -0.1129139997297211734 ) ) ;
#1935=CARTESIAN_POINT ( 'NONE',  ( -2.087366308036623597, -1.727041808514125254, -0.08405390020912445470 ) ) ;
#1942=VERTEX_POINT ( 'NONE', #13486 ) ;
#1950=CARTESIAN_POINT ( 'NONE',  ( -0.06154672136187318982, -0.1666784585780658190, -0.05764611276129244510 ) ) ;
#1952=FACE_OUTER_BOUND ( 'NONE', #942, .T. ) ;
#1953=ORIENTED_EDGE ( 'NONE', *, *, #5096, .T. ) ;
#1956=B_SPLINE_CURVE_WITH_KNOTS ( 'NONE', 3,
 ( #10535, #15314, #9000, #7074 ),
 .UNSPECIFIED., .F., .F.,
 ( 4, 4 ),
 ( 0.000000000000000000, 0.005704847486038692669 ),
 .UNSPECIFIED. ) ;
#1960=ORIENTED_EDGE ( 'NONE', *, *, #6942, .T. ) ;
#1962=AXIS2_PLACEMENT_3D ( 'NONE', #12007, #1263, #7351 ) ;
#1963=ADVANCED_FACE ( 'NONE', ( #13867 ), #10265, .F. ) ;
#1970=DIRECTION ( 'NONE',  ( 0.8144815189573204606, -0.5801894994542525774, 0.000000000000000000 ) ) ;
#1977=CARTESIAN_POINT ( 'NONE',  ( -1.185590514512987692, 0.3351394516327975692, 0.05695402452142334787 ) ) ;
#1980=ORIENTED_EDGE ( 'NONE', *, *, #12028, .F. ) ;
#1982=ADVANCED_FACE ( 'NONE', ( #3140 ), #941, .T. ) ;
#1983=ORIENTED_EDGE ( 'NONE', *, *, #7087, .T. ) ;
#1987=CARTESIAN_POINT ( 'NONE',  ( -0.02344272421051980110, 0.1505984473677600133, -0.03705048130896489156 ) ) ;
#1990=CARTESIAN_POINT ( 'NONE',  ( -0.1968503937007873295, -0.02638708502139245141, 0.05905511811023622659 ) ) ;
#1996=DIRECTION ( 'NONE',  ( 1.000000000000000000, 0.000000000000000000, 0.000000000000000000 ) ) ;
#1997=ORIENTED_EDGE ( 'NONE', *, *, #505, .F. ) ;
#2005=CARTESIAN_POINT ( 'NONE',  ( -1.945459748359984697, -2.745801194614593488, -0.1561691687464119294 ) ) ;
#2016=CARTESIAN_POINT ( 'NONE',  ( -1.182291936362779738, 0.3416838286731589402, 0.04963174987406704375 ) ) ;
#2017=CARTESIAN_POINT ( 'NONE',  ( -1.932501772242613214, -2.783625412848802938, -0.1565638296097948412 ) ) ;
#2024=ORIENTED_EDGE ( 'NONE', *, *, #9588, .T. ) ;
#2026=DIRECTION ( 'NONE',  ( -1.000000000000000000, 0.000000000000000000, 0.000000000000000000 ) ) ;
#2027=EDGE_CURVE ( 'NONE', #4567, #7635, #6431, .T. ) ;
#2030=CARTESIAN_POINT ( 'NONE',  ( -1.933898541317984776, -2.925115481561290309, 0.09044664578863767512 ) ) ;
#2037=CARTESIAN_POINT ( 'NONE',  ( -0.002500327830562678200, 0.1532658568795227105, 0.000000000000000000 ) ) ;
#2038=CARTESIAN_POINT ( 'NONE',  ( -1.580259682937477539, 0.1018956540319142512, 0.04477369844320258641 ) ) ;
#2040=FACE_OUTER_BOUND ( 'NONE', #8942, .T. ) ;
#2047=EDGE_CURVE ( 'NONE', #924, #8242, #12203, .T. ) ;
#2053=CARTESIAN_POINT ( 'NONE',  ( -1.276200637803905691, -0.1988000726501942539, -0.08366141732283455257 ) ) ;
#2056=DIRECTION ( 'NONE',  ( 1.000000000000000000, 0.000000000000000000, 0.000000000000000000 ) ) ;
#2059=EDGE_LOOP ( 'NONE', ( #10098, #11722, #12011, #10474 ) ) ;
#2065=ORIENTED_EDGE ( 'NONE', *, *, #10422, .T. ) ;
#2087=CARTESIAN_POINT ( 'NONE',  ( -1.115439883890946726, -0.06270839865334708330, 0.1968503937007874127 ) ) ;
#2090=AXIS2_PLACEMENT_3D ( 'NONE', #4200, #12434, #13517 ) ;
#2091=CARTESIAN_POINT ( 'NONE',  ( -0.02897706919691097130, 0.1719584017861302827, 0.007005952774883386809 ) ) ;
#2093=CARTESIAN_POINT ( 'NONE',  ( -1.527714331928839098, 0.2380340132385416752, 0.03937007874015747977 ) ) ;
#2094=CARTESIAN_POINT ( 'NONE',  ( -0.002500327830563101039, -0.1605493263772690415, 0.000000000000000000 ) ) ;
#2096=DIRECTION ( 'NONE',  ( -0.000000000000000000, 0.000000000000000000, 1.000000000000000000 ) ) ;
#2097=CARTESIAN_POINT ( 'NONE',  ( -1.898397756988851715, -2.875673457072045025, -0.1127397473705673697 ) ) ;
#2112=CARTESIAN_POINT ( 'NONE',  ( -1.933937248003420262, -2.925008321567649894, -0.09063602501266794509 ) ) ;
#2113=AXIS2_PLACEMENT_3D ( 'NONE', #15147, #12871, #10596 ) ;
#2118=CARTESIAN_POINT ( 'NONE',  ( -0.1968503937007873295, -0.02638708502139245141, -0.03937007874015747977 ) ) ;
#2121=CARTESIAN_POINT ( 'NONE',  ( -0.004690417658706403335, 0.1529805375610461537, 0.008482181431098844218 ) ) ;
#2122=DIRECTION ( 'NONE',  ( 1.000000000000000000, 0.000000000000000000, 0.000000000000000000 ) ) ;
#2128=CIRCLE ( 'NONE', #11391, 0.01968503937007871907 ) ;
#2132=AXIS2_PLACEMENT_3D ( 'NONE', #12060, #10877, #14557 ) ;
#2133=ADVANCED_FACE ( 'NONE', ( #8463 ), #14902, .T. ) ;
#2134=DIRECTION ( 'NONE',  ( 0.000000000000000000, -1.000000000000000000, 2.183568011719057743E-16 ) ) ;
#2138=DIRECTION ( 'NONE',  ( 1.000000000000000000, -0.000000000000000000, -0.000000000000000000 ) ) ;
#2144=CARTESIAN_POINT ( 'NONE',  ( -1.576201932089460689, 0.1075912864651075579, 0.06349180857236520759 ) ) ;
#2147=DIRECTION ( 'NONE',  ( 0.000000000000000000, 1.000000000000000000, 2.212657494868377674E-16 ) ) ;
#2152=EDGE_CURVE ( 'NONE', #13232, #6564, #1580, .T. ) ;
#2164=CARTESIAN_POINT ( 'NONE',  ( -1.957251767099916107, -2.772329397582958599, 0.1771653543307079026 ) ) ;
#2166=AXIS2_PLACEMENT_3D ( 'NONE', #5800, #15230, #2224 ) ;
#2172=VERTEX_POINT ( 'NONE', #7507 ) ;
#2178=( BOUNDED_SURFACE ( )  B_SPLINE_SURFACE ( 3, 2, ( 
 ( #3440, #3344, #14168 ),
 ( #15331, #6867, #14007 ),
 ( #11749, #14074, #12913 ),
 ( #5610, #6956, #4757 ),
 ( #1011, #3573, #15186 ),
 ( #1169, #8218, #5758 ),
 ( #10552, #139, #4594 ),
 ( #7098, #9234, #2091 ),
 ( #3268, #838, #10482 ),
 ( #9389, #2252, #14245 ) ),
 .UNSPECIFIED., .F., .F., .T. ) 
 B_SPLINE_SURFACE_WITH_KNOTS ( ( 4, 2, 2, 2, 4 ),
 ( 3, 3 ),
 ( 0.004868238565068924370, 0.005367227319713952817, 0.005866216074358981264, 0.006365204829004009711, 0.006864193583649038158 ),
 ( 0.000000000000000000, 1.000000000000000000 ),
 .UNSPECIFIED. ) 
 GEOMETRIC_REPRESENTATION_ITEM ( )  RATIONAL_B_SPLINE_SURFACE ( (
 ( 1.000000000000000000, 0.7071067811865474617, 1.000000000000000000),
 ( 1.000000000000000000, 0.7015640395779101368, 1.000000000000000000),
 ( 1.000000000000000000, 0.6956970733052191269, 1.000000000000000000),
 ( 1.000000000000000000, 0.6834122233792455647, 1.000000000000000000),
 ( 1.000000000000000000, 0.6772899333991025950, 1.000000000000000000),
 ( 1.000000000000000000, 0.6655724472122640512, 1.000000000000000000),
 ( 1.000000000000000000, 0.6602173990144353244, 1.000000000000000000),
 ( 1.000000000000000000, 0.6512508157287528743, 1.000000000000000000),
 ( 1.000000000000000000, 0.6477776718208990703, 1.000000000000000000),
 ( 1.000000000000000000, 0.6456929433798522799, 1.000000000000000000) ) ) 
 REPRESENTATION_ITEM ( '' )  SURFACE ( )  );
#2181=( GEOMETRIC_REPRESENTATION_CONTEXT ( 3 ) GLOBAL_UNCERTAINTY_ASSIGNED_CONTEXT ( ( #4064 ) ) GLOBAL_UNIT_ASSIGNED_CONTEXT ( ( #421, #4240, #14911 ) ) REPRESENTATION_CONTEXT ( 'NONE', 'WORKASPACE' ) );
#2183=DIRECTION ( 'NONE',  ( -1.000000000000000000, 0.000000000000000000, 0.000000000000000000 ) ) ;
#2191=AXIS2_PLACEMENT_3D ( 'NONE', #3287, #8379, #9249 ) ;
#2200=CARTESIAN_POINT ( 'NONE',  ( -1.960325907828584402, -2.849280167418937637, -0.1599823882018511501 ) ) ;
#2202=CIRCLE ( 'NONE', #4197, 0.01968503937007873641 ) ;
#2203=CARTESIAN_POINT ( 'NONE',  ( -1.187879871879820026, 0.3305938048772318893, -0.05905511811023619190 ) ) ;
#2213=ORIENTED_EDGE ( 'NONE', *, *, #2047, .T. ) ;
#2218=DIRECTION ( 'NONE',  ( 0.8144815189573204606, -0.5801894994542525774, 1.283760644411384396E-16 ) ) ;
#2221=ADVANCED_FACE ( 'NONE', ( #1415 ), #12589, .T. ) ;
#2222=FACE_OUTER_BOUND ( 'NONE', #5425, .T. ) ;
#2224=DIRECTION ( 'NONE',  ( -0.1408070410764336311, 0.9900370584898827708, 0.000000000000000000 ) ) ;
#2232=ORIENTED_EDGE ( 'NONE', *, *, #7982, .F. ) ;
#2235=CYLINDRICAL_SURFACE ( 'NONE', #11137, 0.1771653543307079026 ) ;
#2243=CARTESIAN_POINT ( 'NONE',  ( -1.391747264127679351, -0.02263456418309609669, 0.06141688777630970042 ) ) ;
#2244=EDGE_CURVE ( 'NONE', #11495, #4530, #12100, .T. ) ;
#2245=CARTESIAN_POINT ( 'NONE',  ( -1.398125690441303304, -0.003404927804347070153, -0.05905511811023622659 ) ) ;
#2252=CARTESIAN_POINT ( 'NONE',  ( -0.002557446713253788174, 0.1765481709910070307, 0.0002437469044495125788 ) ) ;
#2255=DIRECTION ( 'NONE',  ( -0.000000000000000000, 0.000000000000000000, 1.000000000000000000 ) ) ;
#2266=CARTESIAN_POINT ( 'NONE',  ( -2.755905511811024056, -1.630597114118274238, -0.1033464566929129386 ) ) ;
#2270=CARTESIAN_POINT ( 'NONE',  ( -1.993155558009506167, -2.659219082276543578, 0.1643228695458794353 ) ) ;
#2271=ORIENTED_EDGE ( 'NONE', *, *, #317, .F. ) ;
#2275=CARTESIAN_POINT ( 'NONE',  ( -1.596293587998444563, 0.1133155780026525727, 0.04477369844320282927 ) ) ;
#2289=CARTESIAN_POINT ( 'NONE',  ( -1.180847381051876699, 0.3433074774306786314, 0.04457071048068597663 ) ) ;
#2292=CARTESIAN_POINT ( 'NONE',  ( -2.755905511811024056, -2.749515453455444014, -0.1756903148397123138 ) ) ;
#2294=ORIENTED_EDGE ( 'NONE', *, *, #14633, .F. ) ;
#2299=CARTESIAN_POINT ( 'NONE',  ( -1.985311755390326782, -2.772329397582949717, -0.1771653543307079026 ) ) ;
#2302=CARTESIAN_POINT ( 'NONE',  ( -1.911369061871032837, -2.911955715286031143, -0.1096748193019170953 ) ) ;
#2304=CARTESIAN_POINT ( 'NONE',  ( -1.577626109319076653, 0.1055621384249483125, -0.06600777036499150263 ) ) ;
#2314=CARTESIAN_POINT ( 'NONE',  ( -1.574484809660005480, 0.1100025355994810050, -0.06175692796176410898 ) ) ;
#2316=CARTESIAN_POINT ( 'NONE',  ( -1.570515516786257892, 0.1150740656598345651, -0.05905511811023623353 ) ) ;
#2318=AXIS2_PLACEMENT_3D ( 'NONE', #6223, #5044, #9845 ) ;
#2323=CARTESIAN_POINT ( 'NONE',  ( -0.2362204724409448231, -0.02638708502139245488, 0.05905511811023622659 ) ) ;
#2328=EDGE_LOOP ( 'NONE', ( #12487, #9014, #13076, #9177 ) ) ;
#2333=CARTESIAN_POINT ( 'NONE',  ( -1.990041431622598944, -2.757151776041542046, 0.1766819155262782659 ) ) ;
#2334=CIRCLE ( 'NONE', #11601, 0.2165354330708662012 ) ;
#2337=CARTESIAN_POINT ( 'NONE',  ( -1.953876537811547465, -2.911231419079650440, -0.08677724235065008285 ) ) ;
#2339=CARTESIAN_POINT ( 'NONE',  ( -1.956881466196074948, -2.859458241652981680, 0.1546921351859912863 ) ) ;
#2341=CARTESIAN_POINT ( 'NONE',  ( -1.181342415307386151, 0.3435647566351286430, -0.04453711288980863325 ) ) ;
#2343=CARTESIAN_POINT ( 'NONE',  ( -1.943213732889473411, -2.937317281408696523, -0.01189756183868651701 ) ) ;
#2349=CIRCLE ( 'NONE', #8114, 1.865354330708661745 ) ;
#2355=EDGE_CURVE ( 'NONE', #4854, #6320, #13344, .T. ) ;
#2360=CARTESIAN_POINT ( 'NONE',  ( -1.603601197326160355, 0.1030128816188568691, -0.05620285841715500635 ) ) ;
#2376=ORIENTED_EDGE ( 'NONE', *, *, #11462, .F. ) ;
#2392=CARTESIAN_POINT ( 'NONE',  ( -1.591501945092674175, 0.08600752902535276079, 0.1033464566929133410 ) ) ;
#2394=TOROIDAL_SURFACE ( 'NONE', #5895, 0.05905511811023614333, 0.01968503937007873988 ) ;
#2396=ORIENTED_EDGE ( 'NONE', *, *, #422, .F. ) ;
#2402=VERTEX_POINT ( 'NONE', #1297 ) ;
#2404=AXIS2_PLACEMENT_3D ( 'NONE', #5565, #1050, #4649 ) ;
#2406=CARTESIAN_POINT ( 'NONE',  ( -2.104378391724875286, -1.678230452895279612, -0.1033464566929128969 ) ) ;
#2420=EDGE_CURVE ( 'NONE', #9440, #14646, #14588, .T. ) ;
#2429=CARTESIAN_POINT ( 'NONE',  ( -2.073793831555243550, -2.576344762740146788, 0.1326668340823329850 ) ) ;
#2430=LINE ( 'NONE', #7209, #3692 ) ;
#2431=CARTESIAN_POINT ( 'NONE',  ( -1.181342415325283612, 0.3435647566447525558, -0.03937007874014958331 ) ) ;
#2434=CARTESIAN_POINT ( 'NONE',  ( -2.010991777528384983, -2.758467574604075434, 0.1561691687464104861 ) ) ;
#2436=AXIS2_PLACEMENT_3D ( 'NONE', #4997, #12369, #8608 ) ;
#2439=VERTEX_POINT ( 'NONE', #2392 ) ;
#2444=ORIENTED_EDGE ( 'NONE', *, *, #14260, .F. ) ;
#2448=CARTESIAN_POINT ( 'NONE',  ( -1.419113452591957980, -0.01195610050880212445, 0.07344571687920077585 ) ) ;
#2457=CARTESIAN_POINT ( 'NONE',  ( -0.07874015748031543138, -0.1682792322177920907, 0.05905511811023622659 ) ) ;
#2470=CARTESIAN_POINT ( 'NONE',  ( -1.953792993931855904, -2.783665366331675273, -0.1771653543307734335 ) ) ;
#2478=EDGE_LOOP ( 'NONE', ( #14334, #10168, #15041, #24 ) ) ;
#2484=DIRECTION ( 'NONE',  ( 0.000000000000000000, -0.000000000000000000, -1.000000000000000000 ) ) ;
#2486=DIRECTION ( 'NONE',  ( -0.000000000000000000, 0.000000000000000000, 1.000000000000000000 ) ) ;
#2491=ORIENTED_EDGE ( 'NONE', *, *, #14633, .T. ) ;
#2495=CARTESIAN_POINT ( 'NONE',  ( -1.577626107947794232, 0.1055621403655416374, 0.06600776443432196383 ) ) ;
#2497=DIRECTION ( 'NONE',  ( 0.000000000000000000, 0.000000000000000000, -1.000000000000000000 ) ) ;
#2501=CARTESIAN_POINT ( 'NONE',  ( -1.180847381051816525, 0.3433074774307514065, -0.03937007874014958331 ) ) ;
#2513=EDGE_CURVE ( 'NONE', #9857, #13620, #9852, .T. ) ;
#2518=CARTESIAN_POINT ( 'NONE',  ( -0.02641567992992046449, 0.1724028871747071145, 1.853431881210122409E-17 ) ) ;
#2520=CARTESIAN_POINT ( 'NONE',  ( -1.577626107947872613, 0.1055621403655540441, -0.06600776443437042507 ) ) ;
#2534=DIRECTION ( 'NONE',  ( 0.000000000000000000, -0.000000000000000000, -1.000000000000000000 ) ) ;
#2535=CARTESIAN_POINT ( 'NONE',  ( -0.08151194962748883888, 0.1637246173173400876, 0.03937007874015747977 ) ) ;
#2554=DIRECTION ( 'NONE',  ( 0.5163221703362063097, 0.6912615786716231892, 0.5055381748906061512 ) ) ;
#2560=CARTESIAN_POINT ( 'NONE',  ( -2.099922416332451913, -2.385393657770973785, 0.1341751375602837637 ) ) ;
#2565=LINE ( 'NONE', #12147, #7890 ) ;
#2566=CARTESIAN_POINT ( 'NONE',  ( -2.182693454834260027, -1.630005269948474389, 0.08366141732283427501 ) ) ;
#2568=CARTESIAN_POINT ( 'NONE',  ( -1.898433237323783107, -2.875582490238674183, 0.1128268272022943663 ) ) ;
#2569=ORIENTED_EDGE ( 'NONE', *, *, #8368, .T. ) ;
#2582=CARTESIAN_POINT ( 'NONE',  ( -1.605562881068252512, 0.1002320922365774053, -0.06209859025001985416 ) ) ;
#2599=EDGE_CURVE ( 'NONE', #14001, #12118, #9363, .T. ) ;
#2602=ORIENTED_EDGE ( 'NONE', *, *, #1707, .F. ) ;
#2606=TOROIDAL_SURFACE ( 'NONE', #14627, 0.05905511811023614333, 0.01968503937007873988 ) ;
#2607=VECTOR ( 'NONE', #10557, 39.37007874015748143 ) ;
#2615=CARTESIAN_POINT ( 'NONE',  ( -0.05809364415030899426, 0.1671978997630558517, 0.03476146466084937409 ) ) ;
#2628=ORIENTED_EDGE ( 'NONE', *, *, #1290, .F. ) ;
#2636=CARTESIAN_POINT ( 'NONE',  ( -1.925664620590514131, -2.947732113873157811, 0.02576678317052827349 ) ) ;
#2642=CARTESIAN_POINT ( 'NONE',  ( -1.882196081866716275, -2.916170042030258092, -0.04518955602145270645 ) ) ;
#2651=ORIENTED_EDGE ( 'NONE', *, *, #5360, .T. ) ;
#2652=ORIENTED_EDGE ( 'NONE', *, *, #15238, .F. ) ;
#2653=CARTESIAN_POINT ( 'NONE',  ( -0.4722458785514955237, -0.6629481244416842722, 0.05905511811023622659 ) ) ;
#2661=CIRCLE ( 'NONE', #4402, 0.01968503937007874335 ) ;
#2662=CARTESIAN_POINT ( 'NONE',  ( -1.881874822264153035, -2.917190596920589574, 0.1023714699873570499 ) ) ;
#2664=CARTESIAN_POINT ( 'NONE',  ( -1.962487488497034027, -2.889695200659031293, -0.1131027244867615078 ) ) ;
#2665=CARTESIAN_POINT ( 'NONE',  ( -1.431036756819011213, -0.02829858486107875853, -0.08366141732283460808 ) ) ;
#2667=ORIENTED_EDGE ( 'NONE', *, *, #3280, .T. ) ;
#2668=VERTEX_POINT ( 'NONE', #1666 ) ;
#2675=( BOUNDED_SURFACE ( )  B_SPLINE_SURFACE ( 3, 2, ( 
 ( #12392, #5084, #1804 ),
 ( #11282, #5308, #6420 ),
 ( #7592, #6562, #1569 ),
 ( #8714, #555, #14579 ),
 ( #4158, #3845, #8629 ),
 ( #6329, #13411, #2680 ),
 ( #7453, #9892, #6254 ),
 ( #11043, #13488, #11128 ),
 ( #5165, #9972, #4009 ),
 ( #8782, #13550, #2815 ) ),
 .UNSPECIFIED., .F., .F., .T. ) 
 B_SPLINE_SURFACE_WITH_KNOTS ( ( 4, 2, 2, 2, 4 ),
 ( 3, 3 ),
 ( 0.004862229905983068978, 0.005359824983622663366, 0.005857420061262256887, 0.006355015138901850408, 0.006852610216541444796 ),
 ( 0.000000000000000000, 1.000000000000000000 ),
 .UNSPECIFIED. ) 
 GEOMETRIC_REPRESENTATION_ITEM ( )  RATIONAL_B_SPLINE_SURFACE ( (
 ( 1.000000000000000000, 0.7071067811865475727, 1.000000000000000000),
 ( 1.000000000000000000, 0.7118664854617688942, 1.000000000000000000),
 ( 1.000000000000000000, 0.7168001159655631449, 1.000000000000000000),
 ( 1.000000000000000000, 0.7268793899691540217, 1.000000000000000000),
 ( 1.000000000000000000, 0.7317766985259492873, 1.000000000000000000),
 ( 1.000000000000000000, 0.7409494124080542310, 1.000000000000000000),
 ( 1.000000000000000000, 0.7450318297967697401, 1.000000000000000000),
 ( 1.000000000000000000, 0.7517743552594693401, 1.000000000000000000),
 ( 1.000000000000000000, 0.7543262850462577607, 1.000000000000000000),
 ( 1.000000000000000000, 0.7558617697692807669, 1.000000000000000000) ) ) 
 REPRESENTATION_ITEM ( '' )  SURFACE ( )  );
#2676=DIRECTION ( 'NONE',  ( -0.000000000000000000, 0.000000000000000000, 1.000000000000000000 ) ) ;
#2680=CARTESIAN_POINT ( 'NONE',  ( -0.03452177266044149928, -0.1823242888858135624, -0.02287309002717315826 ) ) ;
#2691=ORIENTED_EDGE ( 'NONE', *, *, #505, .T. ) ;
#2693=CARTESIAN_POINT ( 'NONE',  ( -1.596030944582063960, 0.1136756404979306911, -0.04477369844321314740 ) ) ;
#2695=ADVANCED_FACE ( 'NONE', ( #10986 ), #11131, .T. ) ;
#2696=FACE_OUTER_BOUND ( 'NONE', #8737, .T. ) ;
#2697=DIRECTION ( 'NONE',  ( 1.000000000000000000, 0.000000000000000000, 0.000000000000000000 ) ) ;
#2709=ORIENTED_EDGE ( 'NONE', *, *, #3634, .F. ) ;
#2711=EDGE_CURVE ( 'NONE', #6564, #5808, #14860, .T. ) ;
#2715=CARTESIAN_POINT ( 'NONE',  ( -1.942693295529114295, -2.938640948109480178, 0.06141235872390152922 ) ) ;
#2720=CARTESIAN_POINT ( 'NONE',  ( -1.954276836318071364, -2.867108795541001065, -0.1501860367057778201 ) ) ;
#2723=CARTESIAN_POINT ( 'NONE',  ( -1.880688305523271708, -2.919848346818194162, -0.02845389545398609513 ) ) ;
#2729=ORIENTED_EDGE ( 'NONE', *, *, #3949, .T. ) ;
#2731=EDGE_CURVE ( 'NONE', #3678, #9959, #7371, .T. ) ;
#2733=DIRECTION ( 'NONE',  ( 0.000000000000000000, 0.000000000000000000, 1.000000000000000000 ) ) ;
#2735=EDGE_CURVE ( 'NONE', #14790, #14788, #7584, .T. ) ;
#2739=CARTESIAN_POINT ( 'NONE',  ( -1.900558757413772559, -2.942139299165188238, -0.05093160179085944039 ) ) ;
#2742=CARTESIAN_POINT ( 'NONE',  ( -1.568343923620152625, 0.1178486908565804098, 0.05905511811023622659 ) ) ;
#2743=CARTESIAN_POINT ( 'NONE',  ( -1.409031571664937754, -0.006876126661574346287, -0.06053688359312208583 ) ) ;
#2745=EDGE_CURVE ( 'NONE', #15416, #4326, #10336, .T. ) ;
#2751=DIRECTION ( 'NONE',  ( -0.000000000000000000, -0.000000000000000000, 1.000000000000000000 ) ) ;
#2755=CARTESIAN_POINT ( 'NONE',  ( -0.06327586242532841354, -0.1861954285973654311, 0.03830155300069465474 ) ) ;
#2759=ORIENTED_EDGE ( 'NONE', *, *, #13524, .F. ) ;
#2766=CARTESIAN_POINT ( 'NONE',  ( -1.411112778431387937, -0.007856062364883056523, 0.06231671783893451277 ) ) ;
#2773=ORIENTED_EDGE ( 'NONE', *, *, #3664, .T. ) ;
#2776=CARTESIAN_POINT ( 'NONE',  ( -1.953726846202070933, -2.911621419847214121, 0.08674134307398276289 ) ) ;
#2781=CARTESIAN_POINT ( 'NONE',  ( -1.930585417187773434, -2.789123413658596284, -0.1561196149103405983 ) ) ;
#2786=ORIENTED_EDGE ( 'NONE', *, *, #13481, .F. ) ;
#2791=ORIENTED_EDGE ( 'NONE', *, *, #13314, .F. ) ;
#2799=CARTESIAN_POINT ( 'NONE',  ( -1.898411911810662378, -2.948034399344904521, 0.02614368185018839039 ) ) ;
#2800=EDGE_LOOP ( 'NONE', ( #9739, #7019, #10849 ) ) ;
#2803=CARTESIAN_POINT ( 'NONE',  ( -1.586197524891038269, 0.1268408028903934559, 0.05897664633264051298 ) ) ;
#2811=DIRECTION ( 'NONE',  ( 1.000000000000000000, 0.000000000000000000, 0.000000000000000000 ) ) ;
#2813=DIRECTION ( 'NONE',  ( 1.000000000000000000, -0.000000000000000000, -0.000000000000000000 ) ) ;
#2815=CARTESIAN_POINT ( 'NONE',  ( -0.01854992166427318900, -0.1800031784444983685, 0.005378007177148339153 ) ) ;
#2821=CARTESIAN_POINT ( 'NONE',  ( -0.002197004598026061628, -0.1775723205537574900, -0.001204381035045432730 ) ) ;
#2825=EDGE_LOOP ( 'NONE', ( #14455, #6216, #8777 ) ) ;
#2830=DIRECTION ( 'NONE',  ( -0.08093398607328358696, -0.9967194639908912857, 1.383226122518415193E-14 ) ) ;
#2832=AXIS2_PLACEMENT_3D ( 'NONE', #12746, #10068, #462 ) ;
#2833=ADVANCED_FACE ( 'NONE', ( #5483 ), #12478, .T. ) ;
#2838=AXIS2_PLACEMENT_3D ( 'NONE', #1438, #3934, #417 ) ;
#2855=CARTESIAN_POINT ( 'NONE',  ( -1.948408827770508722, -2.924691321014698531, -0.06190742950379295867 ) ) ;
#2865=CARTESIAN_POINT ( 'NONE',  ( -1.887612226072282740, -2.902832404796057197, 0.07695804445277183714 ) ) ;
#2867=CYLINDRICAL_SURFACE ( 'NONE', #10164, 0.01968503937007875723 ) ;
#2869=EDGE_LOOP ( 'NONE', ( #6859, #236, #15192, #15371 ) ) ;
#2876=AXIS2_PLACEMENT_3D ( 'NONE', #8695, #13469, #3757 ) ;
#2877=CARTESIAN_POINT ( 'NONE',  ( -1.397634627758906012, -0.02569727825916744493, -0.06948688383644625877 ) ) ;
#2882=CARTESIAN_POINT ( 'NONE',  ( -2.169366242005649870, -2.077173998931367560, 0.09331536252806132969 ) ) ;
#2889=CARTESIAN_POINT ( 'NONE',  ( -1.884711123585276482, -2.909996678602419173, -0.06153400971538078301 ) ) ;
#2892=CARTESIAN_POINT ( 'NONE',  ( -2.011807227224585048, -2.756102811318752011, -0.1765457041329582810 ) ) ;
#2893=B_SPLINE_CURVE_WITH_KNOTS ( 'NONE', 3,
 ( #13760, #3023, #5513, #3974, #13516, #11169 ),
 .UNSPECIFIED., .F., .F.,
 ( 4, 2, 4 ),
 ( -1.812139438552513428E-05, 0.0003725414720542789089, 0.0007632043384940828809 ),
 .UNSPECIFIED. ) ;
#2900=TOROIDAL_SURFACE ( 'NONE', #11400, 1.885039370078740451, 0.01968503937007873988 ) ;
#2903=CIRCLE ( 'NONE', #3662, 0.2106299212598415904 ) ;
#2910=DIRECTION ( 'NONE',  ( 0.03006568382583901106, 0.9995479251422039191, 0.000000000000000000 ) ) ;
#2911=DIRECTION ( 'NONE',  ( 0.7666137478421605200, -0.6421085279136201640, 0.000000000000000000 ) ) ;
#2920=( LENGTH_UNIT ( ) NAMED_UNIT ( * ) SI_UNIT ( $, .METRE. ) );
#2921=AXIS2_PLACEMENT_3D ( 'NONE', #4472, #9253, #3293 ) ;
#2928=STYLED_ITEM('',(#15519),#9754);
#2930=CARTESIAN_POINT ( 'NONE',  ( -2.111939568874931616, -2.009758264533141769, 0.1096046912080334140 ) ) ;
#2942=CIRCLE ( 'NONE', #11440, 0.01968503937007872948 ) ;
#2943=EDGE_LOOP ( 'NONE', ( #15010, #14056, #14070, #2786 ) ) ;
#2945=FACE_OUTER_BOUND ( 'NONE', #8530, .T. ) ;
#2949=FACE_OUTER_BOUND ( 'NONE', #7696, .T. ) ;
#2954=CIRCLE ( 'NONE', #12224, 0.03937007874015751446 ) ;
#2956=CARTESIAN_POINT ( 'NONE',  ( -1.941802290328372038, -2.756726374736679031, 0.1575978286346828017 ) ) ;
#2958=FACE_OUTER_BOUND ( 'NONE', #338, .T. ) ;
#2960=EDGE_CURVE ( 'NONE', #14556, #7004, #8117, .T. ) ;
#2964=ORIENTED_EDGE ( 'NONE', *, *, #2355, .T. ) ;
#2967=CARTESIAN_POINT ( 'NONE',  ( -1.411805157433859925, -0.008165521224367720821, -0.06278203852593729206 ) ) ;
#2968=CARTESIAN_POINT ( 'NONE',  ( 0.9851651268172137987, -1.725292181286280480, 0.08366141732283420562 ) ) ;
#2975=CARTESIAN_POINT ( 'NONE',  ( -1.880311997174697103, -2.920764059707957383, -0.02288515043993272213 ) ) ;
#2977=CARTESIAN_POINT ( 'NONE',  ( -2.182693454834259139, -1.630005269948474167, -0.1033464566929131884 ) ) ;
#2999=VERTEX_POINT ( 'NONE', #4847 ) ;
#3003=CARTESIAN_POINT ( 'NONE',  ( -0.07278938515219078587, 0.1649651754371201928, -0.05936614484719852924 ) ) ;
#3008=CARTESIAN_POINT ( 'NONE',  ( -2.184126211765463843, -1.902526540362033503, -0.08609155816397313921 ) ) ;
#3010=CARTESIAN_POINT ( 'NONE',  ( -2.464375602680784816, 0.7077922088437123005, 0.1033464566929134798 ) ) ;
#3020=ADVANCED_FACE ( 'NONE', ( #7575 ), #1566, .T. ) ;
#3022=CARTESIAN_POINT ( 'NONE',  ( -1.965385743026580867, -2.834157585141949820, 0.1664812183409376256 ) ) ;
#3023=CARTESIAN_POINT ( 'NONE',  ( -1.187759193896365639, 0.3304858427616815253, -0.05905511811023614333 ) ) ;
#3025=CARTESIAN_POINT ( 'NONE',  ( -2.011807227224585493, -2.756102811318750678, -0.1765457041329570320 ) ) ;
#3030=CARTESIAN_POINT ( 'NONE',  ( -2.065886881322887447, -2.386349482470467187, -0.1342517337147210998 ) ) ;
#3035=EDGE_CURVE ( 'NONE', #880, #14935, #14123, .T. ) ;
#3045=DIRECTION ( 'NONE',  ( 0.8144815189573203495, -0.5801894994542524664, 0.000000000000000000 ) ) ;
#3057=CARTESIAN_POINT ( 'NONE',  ( -1.181845651246067774, 0.3414517841026233902, -0.04963174987412501821 ) ) ;
#3065=ORIENTED_EDGE ( 'NONE', *, *, #8994, .T. ) ;
#3069=CYLINDRICAL_SURFACE ( 'NONE', #9359, 2.795275590551181466 ) ;
#3073=EDGE_CURVE ( 'NONE', #14806, #2402, #6094, .T. ) ;
#3077=AXIS2_PLACEMENT_3D ( 'NONE', #2323, #8225, #12997 ) ;
#3078=DIRECTION ( 'NONE',  ( -0.8011800915434522663, 0.5984233124757303290, 0.000000000000000000 ) ) ;
#3082=( BOUNDED_CURVE ( )  B_SPLINE_CURVE ( 3, ( #11345, #10320, #4223, #9012 ),
 .UNSPECIFIED., .F., .T. ) 
 B_SPLINE_CURVE_WITH_KNOTS ( ( 4, 4 ),
 ( 4.182272261879897535, 4.712388980384695003 ),
 .UNSPECIFIED. ) 
 CURVE ( )  GEOMETRIC_REPRESENTATION_ITEM ( )  RATIONAL_B_SPLINE_CURVE ( ( 1.000000000000000000, 0.9767181429391975644, 0.9767181429391975644, 1.000000000000000000 ) ) 
 REPRESENTATION_ITEM ( '' )  );
#3084=ORIENTED_EDGE ( 'NONE', *, *, #6925, .T. ) ;
#3085=EDGE_LOOP ( 'NONE', ( #12830, #8018, #6164 ) ) ;
#3094=CARTESIAN_POINT ( 'NONE',  ( -2.003349645206483842, -2.780432114833338630, 0.1578450787283683932 ) ) ;
#3097=CARTESIAN_POINT ( 'NONE',  ( -1.969039959700434217, -2.872969167378714772, -0.1271901138548807708 ) ) ;
#3100=CIRCLE ( 'NONE', #15110, 1.885039370078740451 ) ;
#3105=CARTESIAN_POINT ( 'NONE',  ( -2.107119091007230605, -2.011924609756351678, -0.1111957386528079073 ) ) ;
#3116=CARTESIAN_POINT ( 'NONE',  ( -2.163017314575554462, -1.630597114118274238, -0.1033464566929129386 ) ) ;
#3140=FACE_OUTER_BOUND ( 'NONE', #12503, .T. ) ;
#3146=CARTESIAN_POINT ( 'NONE',  ( -0.002345674784311424250, -0.1605320876855827750, -0.0006089964461715403551 ) ) ;
#3147=CARTESIAN_POINT ( 'NONE',  ( -1.431036756819011213, -0.02829858486107887303, -0.07874015748031495954 ) ) ;
#3152=VECTOR ( 'NONE', #2733, 39.37007874015748143 ) ;
#3155=ORIENTED_EDGE ( 'NONE', *, *, #1076, .F. ) ;
#3160=CARTESIAN_POINT ( 'NONE',  ( -0.02636306718620661307, 0.1724112960300225594, -0.0009221601458012943170 ) ) ;
#3168=CARTESIAN_POINT ( 'NONE',  ( -1.181342415325333350, 0.3435647566446739520, -0.03937007874015747977 ) ) ;
#3169=TOROIDAL_SURFACE ( 'NONE', #3425, 0.2303149606299203511, 0.01968503937007873988 ) ;
#3179=EDGE_CURVE ( 'NONE', #13620, #5863, #3082, .T. ) ;
#3180=CARTESIAN_POINT ( 'NONE',  ( -0.07874015748031544526, -0.1771653543307084577, -0.05905511811023622659 ) ) ;
#3185=VECTOR ( 'NONE', #3045, 39.37007874015748854 ) ;
#3187=VECTOR ( 'NONE', #14797, 39.37007874015748143 ) ;
#3189=CARTESIAN_POINT ( 'NONE',  ( -2.107032438837129096, -1.725900680217038463, -0.1037380524286266731 ) ) ;
#3199=EDGE_CURVE ( 'NONE', #8242, #11793, #15430, .T. ) ;
#3200=CARTESIAN_POINT ( 'NONE',  ( -1.590143285778936821, 0.1215581459426987310, -0.06156531251049104925 ) ) ;
#3225=ORIENTED_EDGE ( 'NONE', *, *, #14489, .F. ) ;
#3231=ORIENTED_EDGE ( 'NONE', *, *, #4376, .T. ) ;
#3234=ORIENTED_EDGE ( 'NONE', *, *, #7923, .F. ) ;
#3238=CARTESIAN_POINT ( 'NONE',  ( -0.03726199245316209885, 0.1489178558048124545, -0.04781523662143043890 ) ) ;
#3253=ORIENTED_EDGE ( 'NONE', *, *, #14977, .T. ) ;
#3256=CARTESIAN_POINT ( 'NONE',  ( -2.077672400517819984, -2.160918623940574879, -0.09867007254763489332 ) ) ;
#3262=ORIENTED_EDGE ( 'NONE', *, *, #1764, .T. ) ;
#3267=LINE ( 'NONE', #2087, #1657 ) ;
#3268=CARTESIAN_POINT ( 'NONE',  ( -0.004432333661850347203, 0.1530140478774274504, 0.007791225829902534428 ) ) ;
#3273=CARTESIAN_POINT ( 'NONE',  ( -1.941812372403446618, -2.756696258605407568, -0.1575938902943630204 ) ) ;
#3280=EDGE_CURVE ( 'NONE', #13379, #579, #574, .T. ) ;
#3286=CARTESIAN_POINT ( 'NONE',  ( -1.950247696211656612, -2.878813950563311685, 0.1420638311955204902 ) ) ;
#3287=CARTESIAN_POINT ( 'NONE',  ( -1.293236445124221312, 0.1355266887446167634, 0.03937007874015747977 ) ) ;
#3289=DIRECTION ( 'NONE',  ( -0.8144815189573204606, 0.5801894994542525774, 1.283760644411384396E-16 ) ) ;
#3291=ORIENTED_EDGE ( 'NONE', *, *, #11119, .F. ) ;
#3293=DIRECTION ( 'NONE',  ( -1.000000000000000000, 0.000000000000000000, 0.000000000000000000 ) ) ;
#3295=CARTESIAN_POINT ( 'NONE',  ( -0.01783696211247719210, 0.1513009196653194999, 0.03097470637416573427 ) ) ;
#3297=ORIENTED_EDGE ( 'NONE', *, *, #3431, .F. ) ;
#3307=CARTESIAN_POINT ( 'NONE',  ( -0.07874015748031543138, -0.1682792322177920907, -0.03937007874015747977 ) ) ;
#3310=CARTESIAN_POINT ( 'NONE',  ( -0.02433043306709230594, -0.1808586691373950950, 0.01162756877077189034 ) ) ;
#3313=CARTESIAN_POINT ( 'NONE',  ( -1.574484809660414042, 0.1100025355989073528, 0.06175692796217682051 ) ) ;
#3321=ORIENTED_EDGE ( 'NONE', *, *, #11441, .T. ) ;
#3329=CARTESIAN_POINT ( 'NONE',  ( -1.491640810881974977, 0.2222636556240916994, -0.05905511811023622659 ) ) ;
#3330=CARTESIAN_POINT ( 'NONE',  ( -2.090051324975654268, -1.858423098536573503, -0.08664193191035729491 ) ) ;
#3331=AXIS2_PLACEMENT_3D ( 'NONE', #2968, #7736, #12525 ) ;
#3334=AXIS2_PLACEMENT_3D ( 'NONE', #9692, #14536, #4810 ) ;
#3340=DIRECTION ( 'NONE',  ( 0.000000000000000000, -1.000000000000000000, 2.198945251238206020E-16 ) ) ;
#3344=CARTESIAN_POINT ( 'NONE',  ( -0.08151194962748878337, 0.1637246173173400321, 0.05905511811023621965 ) ) ;
#3350=CARTESIAN_POINT ( 'NONE',  ( -1.929652039733607660, -2.791718527286190188, -0.1763362329223841507 ) ) ;
#3352=DIRECTION ( 'NONE',  ( -0.8011800915434522663, 0.5984233124757303290, 0.000000000000000000 ) ) ;
#3355=ORIENTED_EDGE ( 'NONE', *, *, #2420, .T. ) ;
#3362=AXIS2_PLACEMENT_3D ( 'NONE', #8649, #13428, #2697 ) ;
#3374=CARTESIAN_POINT ( 'NONE',  ( -1.187740243782785310, 0.3305209984255342848, -0.05905511811023626823 ) ) ;
#3378=DIRECTION ( 'NONE',  ( 0.000000000000000000, 1.000000000000000000, 2.224004456380530778E-16 ) ) ;
#3379=AXIS2_PLACEMENT_3D ( 'NONE', #191, #14751, #5080 ) ;
#3382=ORIENTED_EDGE ( 'NONE', *, *, #1068, .T. ) ;
#3397=DIRECTION ( 'NONE',  ( -1.000000000000000000, 0.000000000000000000, 0.000000000000000000 ) ) ;
#3399=CYLINDRICAL_SURFACE ( 'NONE', #10936, 0.01968503937007875723 ) ;
#3400=CARTESIAN_POINT ( 'NONE',  ( -0.07635964791965738074, -0.1878198040935885327, 0.03937007874015747977 ) ) ;
#3402=DIRECTION ( 'NONE',  ( 0.000000000000000000, -1.000000000000000000, 2.212657494868377674E-16 ) ) ;
#3408=ORIENTED_EDGE ( 'NONE', *, *, #4324, .T. ) ;
#3412=ORIENTED_EDGE ( 'NONE', *, *, #271, .T. ) ;
#3414=EDGE_LOOP ( 'NONE', ( #10710, #9050, #12845, #13404 ) ) ;
#3420=EDGE_CURVE ( 'NONE', #4234, #2668, #92, .T. ) ;
#3425=AXIS2_PLACEMENT_3D ( 'NONE', #2053, #9199, #3402 ) ;
#3431=EDGE_CURVE ( 'NONE', #10081, #9980, #10664, .T. ) ;
#3432=CARTESIAN_POINT ( 'NONE',  ( -1.491640810881974977, 0.2222636556240916994, -0.03937007874015747977 ) ) ;
#3440=CARTESIAN_POINT ( 'NONE',  ( -0.07874015748031489015, 0.1442356988431297560, 0.05905511811023622659 ) ) ;
#3444=DIRECTION ( 'NONE',  ( 1.000000000000000000, 0.000000000000000000, 0.000000000000000000 ) ) ;
#3445=ORIENTED_EDGE ( 'NONE', *, *, #4650, .F. ) ;
#3449=ORIENTED_EDGE ( 'NONE', *, *, #6925, .F. ) ;
#3458=CARTESIAN_POINT ( 'NONE',  ( -1.956732843150922774, -2.774109272326283460, 0.1775768436135731765 ) ) ;
#3473=AXIS2_PLACEMENT_3D ( 'NONE', #4071, #12310, #3930 ) ;
#3476=CARTESIAN_POINT ( 'NONE',  ( -1.606329852969329952, 0.09914256429936342541, -0.06530908795646298004 ) ) ;
#3478=CARTESIAN_POINT ( 'NONE',  ( -1.100415514366370306, -0.04998955061625946078, 0.03937007874015747977 ) ) ;
#3479=CARTESIAN_POINT ( 'NONE',  ( -1.181846041278642456, 0.3414510595302567286, 0.04963318180378523820 ) ) ;
#3482=DIRECTION ( 'NONE',  ( 0.5293839892290401750, -0.8483823383050519418, 0.000000000000000000 ) ) ;
#3484=CARTESIAN_POINT ( 'NONE',  ( -1.577626109319266945, 0.1055621384246793470, 0.06600777036542521126 ) ) ;
#3487=DIRECTION ( 'NONE',  ( 1.224646799147353207E-16, 1.000000000000000000, 0.000000000000000000 ) ) ;
#3496=CARTESIAN_POINT ( 'NONE',  ( -1.914045371080042246, -2.904349441506412610, -0.1187067027335292763 ) ) ;
#3497=( LENGTH_UNIT ( ) NAMED_UNIT ( * ) SI_UNIT ( $, .METRE. ) );
#3501=ADVANCED_FACE ( 'NONE', ( #7649 ), #13765, .T. ) ;
#3508=ORIENTED_EDGE ( 'NONE', *, *, #4452, .T. ) ;
#3509=B_SPLINE_CURVE_WITH_KNOTS ( 'NONE', 3,
 ( #10781, #2406, #11982, #13361, #1307, #1242, #12205, #11008, #289, #14542 ),
 .UNSPECIFIED., .F., .F.,
 ( 4, 2, 2, 2, 4 ),
 ( 0.000000000000000000, 0.003638376726563020275, 0.007276753453126040549, 0.01455350690625210018, 0.02910701381250420036 ),
 .UNSPECIFIED. ) ;
#3511=CARTESIAN_POINT ( 'NONE',  ( -1.588298999900090935, 0.1240273096573925177, -0.05983744915167243938 ) ) ;
#3514=FACE_OUTER_BOUND ( 'NONE', #5717, .T. ) ;
#3524=EDGE_CURVE ( 'NONE', #6704, #6873, #6148, .T. ) ;
#3525=CARTESIAN_POINT ( 'NONE',  ( -1.938308666834797522, -2.949171973686980586, 0.01241952892555889601 ) ) ;
#3526=CARTESIAN_POINT ( 'NONE',  ( -1.172017912842092446, 0.3609012623030118383, -0.03937007874015747977 ) ) ;
#3529=CARTESIAN_POINT ( 'NONE',  ( -1.937743059600893769, -2.834246032412025329, 0.1664475769057940369 ) ) ;
#3533=CARTESIAN_POINT ( 'NONE',  ( -0.04509495097506252548, 0.1479884890110656215, 0.05203401519686124549 ) ) ;
#3534=CARTESIAN_POINT ( 'NONE',  ( -1.605558588137308451, 0.1002381878602953691, 0.06208189601213050246 ) ) ;
#3541=CARTESIAN_POINT ( 'NONE',  ( -1.394656322662437775, -0.02432159694977429829, 0.06446741476485348676 ) ) ;
#3542=CARTESIAN_POINT ( 'NONE',  ( -0.07635964791965738074, -0.1878198040935885327, 0.03937007874015747977 ) ) ;
#3548=CARTESIAN_POINT ( 'NONE',  ( -0.02018259705034725071, -0.1802452534892125813, 1.049219007154695292E-17 ) ) ;
#3550=ORIENTED_EDGE ( 'NONE', *, *, #2745, .F. ) ;
#3556=CARTESIAN_POINT ( 'NONE',  ( -0.3441669734936866343, 2.010494531933507467, -0.05905511811023622659 ) ) ;
#3564=CARTESIAN_POINT ( 'NONE',  ( -1.414416440118313689, -0.03985156058301880105, 0.05915390547199540078 ) ) ;
#3570=EDGE_CURVE ( 'NONE', #6704, #8323, #9589, .T. ) ;
#3573=CARTESIAN_POINT ( 'NONE',  ( -0.03967601873943667895, 0.1701129415451466120, 0.04931034005879585819 ) ) ;
#3575=ADVANCED_FACE ( 'NONE', ( #9058 ), #1625, .F. ) ;
#3577=EDGE_CURVE ( 'NONE', #10762, #14238, #13622, .T. ) ;
#3586=DIRECTION ( 'NONE',  ( -0.000000000000000000, -0.000000000000000000, -1.000000000000000000 ) ) ;
#3589=( BOUNDED_SURFACE ( )  B_SPLINE_SURFACE ( 3, 2, ( 
 ( #4770, #9556, #14327 ),
 ( #3597, #6009, #8375 ),
 ( #9640, #8459, #14418 ),
 ( #2495, #7270, #10878 ),
 ( #167, #4052, #3989 ),
 ( #13609, #4134, #12594 ) ),
 .UNSPECIFIED., .F., .F., .T. ) 
 B_SPLINE_SURFACE_WITH_KNOTS ( ( 4, 2, 4 ),
 ( 3, 3 ),
 ( 0.003230360849850193086, 0.003748134328102737875, 0.004265907806355283098 ),
 ( 0.000000000000000000, 1.000000000000000000 ),
 .UNSPECIFIED. ) 
 GEOMETRIC_REPRESENTATION_ITEM ( )  RATIONAL_B_SPLINE_SURFACE ( (
 ( 1.000000000000000000, 0.7048936089935846638, 1.000000000000000000),
 ( 1.000000000000000000, 0.7048811933886807157, 1.000000000000000000),
 ( 1.000000000000000000, 0.7052257929052021534, 1.000000000000000000),
 ( 1.000000000000000000, 0.7061645128347127098, 1.000000000000000000),
 ( 1.000000000000000000, 0.7067576505881709714, 1.000000000000000000),
 ( 1.000000000000000000, 0.7070941911968886551, 1.000000000000000000) ) ) 
 REPRESENTATION_ITEM ( '' )  SURFACE ( )  );
#3597=CARTESIAN_POINT ( 'NONE',  ( -1.580080891959756428, 0.1020406297964638193, 0.07533316186188826480 ) ) ;
#3598=CARTESIAN_POINT ( 'NONE',  ( -1.942764639580312203, -2.938468699076707491, -0.06187511347702391584 ) ) ;
#3604=CARTESIAN_POINT ( 'NONE',  ( -1.945459748359985808, -2.745801194614590823, 0.1561691687464104583 ) ) ;
#3606=CARTESIAN_POINT ( 'NONE',  ( -1.995626487841946295, -2.802056568083358012, -0.1561605048222872716 ) ) ;
#3613=ADVANCED_FACE ( 'NONE', ( #12983 ), #12838, .T. ) ;
#3617=VERTEX_POINT ( 'NONE', #2245 ) ;
#3626=FACE_OUTER_BOUND ( 'NONE', #1328, .T. ) ;
#3627=AXIS2_PLACEMENT_3D ( 'NONE', #7450, #12246, #1503 ) ;
#3630=ORIENTED_EDGE ( 'NONE', *, *, #3035, .T. ) ;
#3633=CARTESIAN_POINT ( 'NONE',  ( -1.496171808639726875, 0.2144740403064263057, -0.05905511811023622659 ) ) ;
#3634=EDGE_CURVE ( 'NONE', #6948, #5863, #12626, .T. ) ;
#3638=VECTOR ( 'NONE', #7427, 39.37007874015748854 ) ;
#3645=CARTESIAN_POINT ( 'NONE',  ( -1.904703986270961824, -2.930671797127443412, 0.08032951875385678508 ) ) ;
#3657=EDGE_CURVE ( 'NONE', #10478, #10993, #1823, .T. ) ;
#3659=TOROIDAL_SURFACE ( 'NONE', #4140, 0.03937007874015747977, 0.01968503937007873988 ) ;
#3662=AXIS2_PLACEMENT_3D ( 'NONE', #11747, #6864, #10311 ) ;
#3663=ORIENTED_EDGE ( 'NONE', *, *, #720, .F. ) ;
#3664=EDGE_CURVE ( 'NONE', #3964, #9996, #7863, .T. ) ;
#3669=LINE ( 'NONE', #4759, #1405 ) ;
#3673=CARTESIAN_POINT ( 'NONE',  ( -1.607606114292111199, 0.09732815221480045631, 0.1968503937007874127 ) ) ;
#3678=VERTEX_POINT ( 'NONE', #11648 ) ;
#3681=AXIS2_PLACEMENT_3D ( 'NONE', #3940, #8720, #9579 ) ;
#3685=DIRECTION ( 'NONE',  ( 0.000000000000000000, -1.000000000000000000, 2.222614453595283597E-16 ) ) ;
#3688=CARTESIAN_POINT ( 'NONE',  ( -1.924909868815465996, -2.804990923292145499, 0.1525883533589904306 ) ) ;
#3690=CARTESIAN_POINT ( 'NONE',  ( -1.945817195785428888, -2.931010914885669560, 0.04553526292943101822 ) ) ;
#3692=VECTOR ( 'NONE', #1258, 39.37007874015748143 ) ;
#3693=CARTESIAN_POINT ( 'NONE',  ( -0.03749734052841494775, 0.1488898142811246883, -0.04795046931071422075 ) ) ;
#3697=EDGE_CURVE ( 'NONE', #3768, #9440, #8273, .T. ) ;
#3704=CARTESIAN_POINT ( 'NONE',  ( -1.414149037809793619, -0.03961791295443582717, 0.05846194000333194973 ) ) ;
#3712=CARTESIAN_POINT ( 'NONE',  ( -0.04497577134311978031, -0.1837750859334940368, 0.03094209595079721806 ) ) ;
#3714=CIRCLE ( 'NONE', #13723, 0.01968503937007871213 ) ;
#3717=EDGE_CURVE ( 'NONE', #13695, #4234, #5317, .T. ) ;
#3720=ORIENTED_EDGE ( 'NONE', *, *, #5549, .T. ) ;
#3721=CARTESIAN_POINT ( 'NONE',  ( -1.276200637803905691, -0.1988000726501942539, 0.05905511811023622659 ) ) ;
#3722=EDGE_CURVE ( 'NONE', #14128, #5248, #9884, .T. ) ;
#3723=EDGE_CURVE ( 'NONE', #10712, #925, #11567, .T. ) ;
#3729=B_SPLINE_CURVE_WITH_KNOTS ( 'NONE', 3,
 ( #15364, #11837, #11771, #13015, #3534, #12939, #14106, #21, #1111, #2275 ),
 .UNSPECIFIED., .F., .F.,
 ( 4, 2, 2, 2, 4 ),
 ( 0.000000000000000000, 0.0002596010170527390326, 0.0005192020341054780653, 0.0007788030511582170979, 0.001038404068210956131 ),
 .UNSPECIFIED. ) ;
#3731=DIRECTION ( 'NONE',  ( -0.9900370584898828819, -0.1408070410764336311, -0.000000000000000000 ) ) ;
#3733=B_SPLINE_CURVE_WITH_KNOTS ( 'NONE', 3,
 ( #9197, #3310, #11785, #13976, #15228, #9116, #10520, #3400 ),
 .UNSPECIFIED., .F., .F.,
 ( 4, 2, 2, 4 ),
 ( 0.000000000000000000, 0.0009364989265740226044, 0.001404748389861033581, 0.001872997853148044775 ),
 .UNSPECIFIED. ) ;
#3734=CYLINDRICAL_SURFACE ( 'NONE', #13098, 0.01968503937007875723 ) ;
#3738=ORIENTED_EDGE ( 'NONE', *, *, #894, .F. ) ;
#3749=ORIENTED_EDGE ( 'NONE', *, *, #6550, .T. ) ;
#3754=DIRECTION ( 'NONE',  ( 1.000000000000000000, -0.000000000000000000, -0.000000000000000000 ) ) ;
#3756=CARTESIAN_POINT ( 'NONE',  ( -1.293236445124221312, 0.1355266887446167634, 0.05905511811023622659 ) ) ;
#3757=DIRECTION ( 'NONE',  ( 0.9482728725910103407, 0.3174563893009453297, 0.000000000000000000 ) ) ;
#3760=CARTESIAN_POINT ( 'NONE',  ( -1.931769569189934588, -2.785717222541405302, 0.1768902618314421582 ) ) ;
#3762=CARTESIAN_POINT ( 'NONE',  ( -2.080881322745466999, -1.632190302820504479, -0.08366141732283423338 ) ) ;
#3764=CARTESIAN_POINT ( 'NONE',  ( -1.570493619109850858, 0.1151020441255655169, 0.05905511811023620578 ) ) ;
#3768=VERTEX_POINT ( 'NONE', #12399 ) ;
#3773=( BOUNDED_CURVE ( )  B_SPLINE_CURVE ( 3, ( #9844, #13058, #2316, #7099 ),
 .UNSPECIFIED., .F., .T. ) 
 B_SPLINE_CURVE_WITH_KNOTS ( ( 4, 4 ),
 ( 1.040679608290689506, 1.570796326794894560 ),
 .UNSPECIFIED. ) 
 CURVE ( )  GEOMETRIC_REPRESENTATION_ITEM ( )  RATIONAL_B_SPLINE_CURVE ( ( 1.000000000000000000, 0.9767181429392493008, 0.9767181429392493008, 1.000000000000000000 ) ) 
 REPRESENTATION_ITEM ( '' )  );
#3774=FACE_OUTER_BOUND ( 'NONE', #5509, .T. ) ;
#3775=CYLINDRICAL_SURFACE ( 'NONE', #6679, 8.689140419947479543 ) ;
#3782=CARTESIAN_POINT ( 'NONE',  ( -1.187897409289509376, 0.3305577418844916071, -0.05905511811023633761 ) ) ;
#3790=DIRECTION ( 'NONE',  ( 0.000000000000000000, -0.000000000000000000, 1.000000000000000000 ) ) ;
#3794=LINE ( 'NONE', #283, #1920 ) ;
#3805=DIRECTION ( 'NONE',  ( -0.000000000000000000, 0.000000000000000000, 1.000000000000000000 ) ) ;
#3807=CARTESIAN_POINT ( 'NONE',  ( -1.431036756819010769, -0.02829858486107874466, -0.08366141732283458032 ) ) ;
#3825=CARTESIAN_POINT ( 'NONE',  ( -1.895444647785978542, -2.883186813555515648, 0.1048134176421858937 ) ) ;
#3827=CARTESIAN_POINT ( 'NONE',  ( -1.972730759285706181, -2.863434052066349711, -0.1336313644289080227 ) ) ;
#3833=CIRCLE ( 'NONE', #12595, 2.795275590551181466 ) ;
#3839=ADVANCED_FACE ( 'NONE', ( #4898 ), #3734, .F. ) ;
#3845=CARTESIAN_POINT ( 'NONE',  ( -0.03549374849269303772, -0.1824859222442999918, -0.04671604978335693048 ) ) ;
#3852=EDGE_CURVE ( 'NONE', #12093, #9857, #9098, .T. ) ;
#3866=CARTESIAN_POINT ( 'NONE',  ( -1.964126537190517885, -2.749515453455440905, 0.1756903148397125081 ) ) ;
#3870=CARTESIAN_POINT ( 'NONE',  ( -2.184126211765464287, -1.725292181286298021, 0.08417626406393743932 ) ) ;
#3879=ADVANCED_FACE ( 'NONE', ( #7924 ), #4303, .T. ) ;
#3880=EDGE_LOOP ( 'NONE', ( #11580, #94, #4442, #4403 ) ) ;
#3881=EDGE_LOOP ( 'NONE', ( #586, #11289, #1609, #11068 ) ) ;
#3883=EDGE_CURVE ( 'NONE', #13232, #4530, #5553, .T. ) ;
#3889=CARTESIAN_POINT ( 'NONE',  ( -1.925556412971271669, -2.948029930094562712, -0.02618410116112765071 ) ) ;
#3893=EDGE_CURVE ( 'NONE', #7930, #15252, #2334, .T. ) ;
#3897=CARTESIAN_POINT ( 'NONE',  ( -1.926734873413887383, -2.799953544547113538, 0.1540989716193912062 ) ) ;
#3914=CARTESIAN_POINT ( 'NONE',  ( -1.992382107315058271, -2.749515453455440905, 0.1756903148397124803 ) ) ;
#3917=CARTESIAN_POINT ( 'NONE',  ( -1.880695783986644498, -2.919830138821126297, -0.02855755338539034058 ) ) ;
#3918=ORIENTED_EDGE ( 'NONE', *, *, #12662, .F. ) ;
#3924=AXIS2_PLACEMENT_3D ( 'NONE', #4656, #3487, #8259 ) ;
#3928=DIRECTION ( 'NONE',  ( 0.5984233124757303290, 0.8011800915434521553, 0.000000000000000000 ) ) ;
#3930=DIRECTION ( 'NONE',  ( 0.8011800915434506010, -0.5984233124757325495, 0.000000000000000000 ) ) ;
#3934=DIRECTION ( 'NONE',  ( 0.000000000000000000, -0.000000000000000000, -1.000000000000000000 ) ) ;
#3937=CARTESIAN_POINT ( 'NONE',  ( -0.04507696108106435534, -0.1650637432014245565, 0.05202626060216886117 ) ) ;
#3940=CARTESIAN_POINT ( 'NONE',  ( -2.755905511811024056, 0.2985367441494412022, -0.1033464566929133965 ) ) ;
#3941=AXIS2_PLACEMENT_3D ( 'NONE', #10111, #4156, #4386 ) ;
#3949=EDGE_CURVE ( 'NONE', #9786, #14935, #13961, .T. ) ;
#3950=CARTESIAN_POINT ( 'NONE',  ( -2.096257313159167968, -1.821548935441466677, 0.1033814208906759513 ) ) ;
#3953=CARTESIAN_POINT ( 'NONE',  ( -1.419029514950140625, -0.01190400850868964661, 0.07305840954582080993 ) ) ;
#3962=ORIENTED_EDGE ( 'NONE', *, *, #8579, .T. ) ;
#3964=VERTEX_POINT ( 'NONE', #12629 ) ;
#3969=EDGE_CURVE ( 'NONE', #14915, #9786, #4838, .T. ) ;
#3971=CARTESIAN_POINT ( 'NONE',  ( -1.935472858800945994, -2.920743354953669879, 0.09758401094301728806 ) ) ;
#3974=CARTESIAN_POINT ( 'NONE',  ( -1.181846040523323538, 0.3414510609348502257, -0.04963317811004215596 ) ) ;
#3978=CARTESIAN_POINT ( 'NONE',  ( -1.898348652445378981, -2.875798882032482240, 0.1126135460449128739 ) ) ;
#3988=CARTESIAN_POINT ( 'NONE',  ( -1.415641383055952440, -0.01001468546970056897, -0.06638871894587755618 ) ) ;
#3989=CARTESIAN_POINT ( 'NONE',  ( -1.599731447215819058, 0.1084887237744113775, 0.04822519498664557674 ) ) ;
#3993=FACE_BOUND ( 'NONE', #452, .T. ) ;
#3994=CARTESIAN_POINT ( 'NONE',  ( -1.873911309327628949, -2.936534521027843070, -0.06698651620721371436 ) ) ;
#3995=ORIENTED_EDGE ( 'NONE', *, *, #14260, .T. ) ;
#3996=CARTESIAN_POINT ( 'NONE',  ( -2.176528721281673739, -2.014897391718464714, -0.1098265554925635934 ) ) ;
#4000=ORIENTED_EDGE ( 'NONE', *, *, #13102, .F. ) ;
#4003=EDGE_CURVE ( 'NONE', #9812, #9857, #3729, .T. ) ;
#4005=LINE ( 'NONE', #8709, #5328 ) ;
#4008=CYLINDRICAL_SURFACE ( 'NONE', #14725, 0.07874015748031495954 ) ;
#4009=CARTESIAN_POINT ( 'NONE',  ( -0.02015118043373552090, -0.1802412052441877965, -0.0009776059035733464502 ) ) ;
#4013=CARTESIAN_POINT ( 'NONE',  ( -0.02281238468002976319, -0.1806356120156163148, 0.007039490205851098130 ) ) ;
#4023=LINE ( 'NONE', #11388, #10675 ) ;
#4033=DIRECTION ( 'NONE',  ( -0.8144815189573204606, 0.5801894994542525774, -1.283760644411384396E-16 ) ) ;
#4034=CARTESIAN_POINT ( 'NONE',  ( -1.935621620635804785, -2.920307329271410790, -0.09762439764854415059 ) ) ;
#4039=CARTESIAN_POINT ( 'NONE',  ( -0.01089193232087468620, -0.1772239411783215757, 5.880576042184872077E-16 ) ) ;
#4040=DIRECTION ( 'NONE',  ( 0.5801894994542512451, 0.8144815189573213488, 0.000000000000000000 ) ) ;
#4044=EDGE_LOOP ( 'NONE', ( #5367, #10990, #9323, #1073 ) ) ;
#4049=CARTESIAN_POINT ( 'NONE',  ( -1.404141343084615912, -0.005156784085991158832, -0.05951157569786713619 ) ) ;
#4052=CARTESIAN_POINT ( 'NONE',  ( -1.592259916642357442, 0.1190110821474778119, 0.06350111023902092755 ) ) ;
#4057=CARTESIAN_POINT ( 'NONE',  ( -1.883471559757083913, -2.913266620391066208, 0.1077232328358656566 ) ) ;
#4064=UNCERTAINTY_MEASURE_WITH_UNIT (LENGTH_MEASURE( 1.000000000000000082E-05 ), #421, 'distance_accuracy_value', 'NONE');
#4070=DIRECTION ( 'NONE',  ( 0.7402970580929170152, 0.6722799013647308142, 0.000000000000000000 ) ) ;
#4071=CARTESIAN_POINT ( 'NONE',  ( -1.063205505495480097, 0.7941372572243097228, -0.03937007874015747977 ) ) ;
#4076=CARTESIAN_POINT ( 'NONE',  ( -0.07874015748031520934, 1.062385330869439640E-16, 0.05905511811023622659 ) ) ;
#4082=FACE_OUTER_BOUND ( 'NONE', #14179, .T. ) ;
#4101=DIRECTION ( 'NONE',  ( 0.9453712468369984689, 0.3259957141648626711, 0.000000000000000000 ) ) ;
#4112=CARTESIAN_POINT ( 'NONE',  ( -1.972615538042427286, -2.863733741840190028, 0.1334472478180623312 ) ) ;
#4120=DIRECTION ( 'NONE',  ( 1.000000000000000000, 0.000000000000000000, 0.000000000000000000 ) ) ;
#4121=CARTESIAN_POINT ( 'NONE',  ( -1.908282260581757761, -2.850014880722915755, -0.1332367027562576245 ) ) ;
#4128=CIRCLE ( 'NONE', #10633, 0.01968503937007875723 ) ;
#4129=ORIENTED_EDGE ( 'NONE', *, *, #14675, .T. ) ;
#4134=CARTESIAN_POINT ( 'NONE',  ( -1.590519080053494516, 0.1214231549357709661, 0.06175753274847662483 ) ) ;
#4140=AXIS2_PLACEMENT_3D ( 'NONE', #14483, #2255, #12917 ) ;
#4141=CARTESIAN_POINT ( 'NONE',  ( -1.181096721277162365, 0.3434326092093347715, 0.03937007874014959025 ) ) ;
#4143=CARTESIAN_POINT ( 'NONE',  ( -1.873991930927511040, -2.936340581383783732, 0.06745920558762338870 ) ) ;
#4146=VERTEX_POINT ( 'NONE', #7080 ) ;
#4156=DIRECTION ( 'NONE',  ( -0.000000000000000000, 0.000000000000000000, 1.000000000000000000 ) ) ;
#4158=CARTESIAN_POINT ( 'NONE',  ( -0.03726694595799353443, -0.1642704670929807653, -0.04781780748315901663 ) ) ;
#4171=ORIENTED_EDGE ( 'NONE', *, *, #3697, .F. ) ;
#4175=CARTESIAN_POINT ( 'NONE',  ( -2.100501784635051550, -1.630597114118274238, 0.1033464566929129663 ) ) ;
#4180=CARTESIAN_POINT ( 'NONE',  ( -1.431036756819010769, -0.02829858486107857465, 0.08366141732283458032 ) ) ;
#4183=( BOUNDED_SURFACE ( )  B_SPLINE_SURFACE ( 3, 2, ( 
 ( #5219, #7660, #12524 ),
 ( #8760, #11261, #10015 ),
 ( #13530, #6297, #4049 ),
 ( #9861, #1487, #475 ),
 ( #5285, #13604, #2967 ),
 ( #11094, #2877, #3988 ),
 ( #6236, #6475, #8924 ),
 ( #10082, #14870, #12226 ),
 ( #14648, #388, #1784 ),
 ( #7562, #6394, #12357 ) ),
 .UNSPECIFIED., .F., .F., .T. ) 
 B_SPLINE_SURFACE_WITH_KNOTS ( ( 4, 2, 2, 2, 4 ),
 ( 3, 3 ),
 ( 0.000000000000000000, 0.0004011259949119783835, 0.0008022519898239567670, 0.001203377984735935205, 0.001604503979647913534 ),
 ( 0.000000000000000000, 1.000000000000000000 ),
 .UNSPECIFIED. ) 
 GEOMETRIC_REPRESENTATION_ITEM ( )  RATIONAL_B_SPLINE_SURFACE ( (
 ( 1.000000000000000000, 0.7071067811865476838, 1.000000000000000000),
 ( 1.000000000000000000, 0.6902033478571758529, 1.000000000000000000),
 ( 1.000000000000000000, 0.6755035747093588450, 1.000000000000000000),
 ( 1.000000000000000000, 0.6523092178238821814, 1.000000000000000000),
 ( 1.000000000000000000, 0.6440979550411551902, 1.000000000000000000),
 ( 1.000000000000000000, 0.6332442468201355812, 1.000000000000000000),
 ( 1.000000000000000000, 0.6305611707286850054, 1.000000000000000000),
 ( 1.000000000000000000, 0.6276691513331230654, 1.000000000000000000),
 ( 1.000000000000000000, 0.6273773519528882403, 1.000000000000000000),
 ( 1.000000000000000000, 0.6273322353868016066, 1.000000000000000000) ) ) 
 REPRESENTATION_ITEM ( '' )  SURFACE ( )  );
#4186=EDGE_LOOP ( 'NONE', ( #7515, #10438, #8783, #11463 ) ) ;
#4190=ORIENTED_EDGE ( 'NONE', *, *, #2152, .T. ) ;
#4194=EDGE_CURVE ( 'NONE', #5049, #8019, #13054, .T. ) ;
#4196=CARTESIAN_POINT ( 'NONE',  ( -2.011807227224586825, -2.756102811318747126, 0.1765457041329565879 ) ) ;
#4197=AXIS2_PLACEMENT_3D ( 'NONE', #915, #5671, #15247 ) ;
#4200=CARTESIAN_POINT ( 'NONE',  ( 0.000000000000000000, 0.000000000000000000, -0.05905511811023622659 ) ) ;
#4215=LINE ( 'NONE', #538, #3187 ) ;
#4220=CARTESIAN_POINT ( 'NONE',  ( -1.925369493808086974, -2.803727943723343774, -0.1746073045697247028 ) ) ;
#4223=CARTESIAN_POINT ( 'NONE',  ( -1.588328939002293660, 0.1239872266390858180, 0.03937007874015745895 ) ) ;
#4234=VERTEX_POINT ( 'NONE', #7471 ) ;
#4240=( NAMED_UNIT ( * ) PLANE_ANGLE_UNIT ( ) SI_UNIT ( $, .RADIAN. ) );
#4247=EDGE_CURVE ( 'NONE', #4854, #9785, #2349, .T. ) ;
#4249=DIRECTION ( 'NONE',  ( -1.000000000000000000, 0.000000000000000000, 0.000000000000000000 ) ) ;
#4250=PRODUCT_CONTEXT ( 'NONE', #8399, 'mechanical' ) ;
#4255=DIRECTION ( 'NONE',  ( 0.5984233124757297739, 0.8011800915434527104, 2.779651826571349572E-15 ) ) ;
#4263=CARTESIAN_POINT ( 'NONE',  ( -1.995574620099673124, -2.802153887077456940, 0.1558670272671928148 ) ) ;
#4264=DIRECTION ( 'NONE',  ( 0.000000000000000000, 0.000000000000000000, 1.000000000000000000 ) ) ;
#4265=EDGE_CURVE ( 'NONE', #15416, #6036, #6690, .T. ) ;
#4267=( BOUNDED_SURFACE ( )  B_SPLINE_SURFACE ( 3, 2, ( 
 ( #4539, #9321, #14098 ),
 ( #3374, #12933, #2203 ),
 ( #6976, #11767, #13792 ),
 ( #3057, #7828, #12622 ),
 ( #4935, #5778, #2341 ),
 ( #2501, #14264, #2431 ) ),
 .UNSPECIFIED., .F., .F., .T. ) 
 B_SPLINE_SURFACE_WITH_KNOTS ( ( 4, 2, 4 ),
 ( 3, 3 ),
 ( -3.623019766860193592E-05, 0.0007449614524473009095, 0.001526153102563203735 ),
 ( 0.000000000000000000, 1.000000000000000000 ),
 .UNSPECIFIED. ) 
 GEOMETRIC_REPRESENTATION_ITEM ( )  RATIONAL_B_SPLINE_SURFACE ( (
 ( 1.000000000000000000, 1.000000000000000000, 1.000000000000000000),
 ( 1.000000000000000000, 1.000000656565404711, 1.000000000000000000),
 ( 1.000000000000000000, 0.9999739034942860538, 1.000000000000000000),
 ( 1.000000000000000000, 0.9999216474068313154, 1.000000000000000000),
 ( 1.000000000000000000, 0.9998986130898210867, 1.000000000000000000),
 ( 1.000000000000000000, 0.9998995914418474795, 1.000000000000000000) ) ) 
 REPRESENTATION_ITEM ( '' )  SURFACE ( )  );
#4268=CARTESIAN_POINT ( 'NONE',  ( -1.955396564714622976, -2.907528569965089460, -0.1152285774067266372 ) ) ;
#4270=DIRECTION ( 'NONE',  ( -0.000000000000000000, 0.000000000000000000, 1.000000000000000000 ) ) ;
#4272=DIRECTION ( 'NONE',  ( -0.3235667741753706084, 0.9383274424966834282, 0.1218447918762960436 ) ) ;
#4273=CARTESIAN_POINT ( 'NONE',  ( -2.080881322745466555, -1.632190302820504701, -0.1033464566929128137 ) ) ;
#4277=ORIENTED_EDGE ( 'NONE', *, *, #3420, .F. ) ;
#4285=CARTESIAN_POINT ( 'NONE',  ( -1.926829032957098509, -2.799642034967062543, -0.1538761875634443999 ) ) ;
#4300=CARTESIAN_POINT ( 'NONE',  ( -1.580259682937507515, 0.1018956540318727566, 0.1968503937007874127 ) ) ;
#4303=CYLINDRICAL_SURFACE ( 'NONE', #8344, 0.01968503937007877111 ) ;
#4304=EDGE_LOOP ( 'NONE', ( #11415, #14431, #11497, #5051, #8034, #11069 ) ) ;
#4313=FACE_OUTER_BOUND ( 'NONE', #12269, .T. ) ;
#4317=DIRECTION ( 'NONE',  ( 0.4005670834070333974, 0.9162674345903507600, -5.558984986317924027E-15 ) ) ;
#4324=EDGE_CURVE ( 'NONE', #11956, #3678, #15111, .T. ) ;
#4326=VERTEX_POINT ( 'NONE', #8949 ) ;
#4327=ORIENTED_EDGE ( 'NONE', *, *, #12395, .T. ) ;
#4334=AXIS2_PLACEMENT_3D ( 'NONE', #9815, #8633, #14518 ) ;
#4336=CARTESIAN_POINT ( 'NONE',  ( -1.980019913028319367, -2.844306626094838641, 0.1438463815136533930 ) ) ;
#4347=CARTESIAN_POINT ( 'NONE',  ( -2.087493674894419282, -2.010784418770093840, -0.1111536532825547208 ) ) ;
#4354=ORIENTED_EDGE ( 'NONE', *, *, #5667, .T. ) ;
#4357=CIRCLE ( 'NONE', #8412, 0.01968503937007873988 ) ;
#4358=VECTOR ( 'NONE', #9219, 39.37007874015748143 ) ;
#4362=CARTESIAN_POINT ( 'NONE',  ( -0.1771653543307086243, -0.02638708502139245488, 0.03937007874015747977 ) ) ;
#4365=CARTESIAN_POINT ( 'NONE',  ( -1.431036756819011213, -0.02829858486107876200, 0.1968503937007874127 ) ) ;
#4367=DIRECTION ( 'NONE',  ( 5.457303053353514501E-25, 1.000000000000000000, -6.049848122469114742E-13 ) ) ;
#4376=EDGE_CURVE ( 'NONE', #10028, #9980, #4005, .T. ) ;
#4377=AXIS2_PLACEMENT_3D ( 'NONE', #13237, #11026, #3685 ) ;
#4385=CARTESIAN_POINT ( 'NONE',  ( -1.931900750301128511, -2.930638880368575006, -0.08039528988028955825 ) ) ;
#4386=DIRECTION ( 'NONE',  ( 1.000000000000000000, 0.000000000000000000, 0.000000000000000000 ) ) ;
#4391=CARTESIAN_POINT ( 'NONE',  ( -1.431036756819011213, -0.02829858486107871343, 0.07874015748031495954 ) ) ;
#4395=VERTEX_POINT ( 'NONE', #14669 ) ;
#4402=AXIS2_PLACEMENT_3D ( 'NONE', #14213, #11787, #3482 ) ;
#4403=ORIENTED_EDGE ( 'NONE', *, *, #12961, .F. ) ;
#4406=CARTESIAN_POINT ( 'NONE',  ( -0.007954450877559391536, 0.1525563742224383124, -0.01590295032065047048 ) ) ;
#4418=ORIENTED_EDGE ( 'NONE', *, *, #3570, .T. ) ;
#4423=ORIENTED_EDGE ( 'NONE', *, *, #3199, .T. ) ;
#4431=CARTESIAN_POINT ( 'NONE',  ( -1.576201932089153157, 0.1075912864655425849, -0.06349180857188843619 ) ) ;
#4432=ADVANCED_FACE ( 'NONE', ( #12473 ), #11279, .T. ) ;
#4437=CARTESIAN_POINT ( 'NONE',  ( -2.080881322745466999, -1.632190302820504479, -0.08366141732283406685 ) ) ;
#4442=ORIENTED_EDGE ( 'NONE', *, *, #12186, .F. ) ;
#4447=CARTESIAN_POINT ( 'NONE',  ( -1.584115185264708403, 0.1296286773226378863, -0.03937007874015747977 ) ) ;
#4449=AXIS2_PLACEMENT_3D ( 'NONE', #5658, #13982, #2147 ) ;
#4452=EDGE_CURVE ( 'NONE', #15344, #14180, #6347, .T. ) ;
#4455=CARTESIAN_POINT ( 'NONE',  ( -1.937736976485135987, -2.834264970500691039, -0.1664422342211422379 ) ) ;
#4457=DIRECTION ( 'NONE',  ( -1.000000000000000000, 2.168404344971007142E-16, 0.000000000000000000 ) ) ;
#4462=CIRCLE ( 'NONE', #12738, 0.01968503937007871213 ) ;
#4472=CARTESIAN_POINT ( 'NONE',  ( -1.293236445124221312, 0.1355266887446167634, 0.05905511811023622659 ) ) ;
#4475=CARTESIAN_POINT ( 'NONE',  ( -1.181342415325336237, 0.3435647566446753398, 0.04457061940634219482 ) ) ;
#4477=ADVANCED_FACE ( 'NONE', ( #9017 ), #2606, .T. ) ;
#4479=EDGE_LOOP ( 'NONE', ( #1020, #4989, #3962, #12878, #6811, #7941, #13011, #15052, #2569, #15036 ) ) ;
#4487=CARTESIAN_POINT ( 'NONE',  ( -1.181342415325333350, 0.3435647566446739520, -0.03937007874015747977 ) ) ;
#4492=DIRECTION ( 'NONE',  ( 0.000000000000000000, 2.212657494868377674E-16, 1.000000000000000000 ) ) ;
#4498=EDGE_LOOP ( 'NONE', ( #7072, #14000, #495, #9334 ) ) ;
#4501=FACE_OUTER_BOUND ( 'NONE', #12134, .T. ) ;
#4519=FACE_OUTER_BOUND ( 'NONE', #4479, .T. ) ;
#4523=CARTESIAN_POINT ( 'NONE',  ( -1.956731389022586809, -2.774113956945879700, -0.1775764214674195041 ) ) ;
#4526=EDGE_CURVE ( 'NONE', #4567, #3617, #11363, .T. ) ;
#4530=VERTEX_POINT ( 'NONE', #7990 ) ;
#4536=CARTESIAN_POINT ( 'NONE',  ( -1.960310522231513364, -2.849326065546125886, 0.1599618923947356830 ) ) ;
#4539=CARTESIAN_POINT ( 'NONE',  ( -1.190198933766848155, 0.3259758027579587325, -0.05905511811023622659 ) ) ;
#4550=ORIENTED_EDGE ( 'NONE', *, *, #5058, .F. ) ;
#4554=DIRECTION ( 'NONE',  ( -0.000000000000000000, -0.000000000000000000, -1.000000000000000000 ) ) ;
#4558=DIRECTION ( 'NONE',  ( -0.000000000000000000, -0.000000000000000000, -1.000000000000000000 ) ) ;
#4560=ORIENTED_EDGE ( 'NONE', *, *, #5076, .F. ) ;
#4561=FACE_OUTER_BOUND ( 'NONE', #8405, .T. ) ;
#4562=CARTESIAN_POINT ( 'NONE',  ( -2.010991777528384095, -2.758467574604078543, -0.1561691687464109024 ) ) ;
#4567=VERTEX_POINT ( 'NONE', #12771 ) ;
#4574=AXIS2_PLACEMENT_3D ( 'NONE', #70, #2554, #9850 ) ;
#4576=CARTESIAN_POINT ( 'NONE',  ( -1.943198498587445755, -2.817349890850887384, 0.1717294883501950531 ) ) ;
#4578=CARTESIAN_POINT ( 'NONE',  ( -1.964126537190516331, -2.749515453455444014, -0.1756903148397123138 ) ) ;
#4582=CARTESIAN_POINT ( 'NONE',  ( -1.404179464191384508, -0.005170306204214139036, 0.05952236574397579832 ) ) ;
#4593=AXIS2_PLACEMENT_3D ( 'NONE', #8619, #3790, #8559 ) ;
#4594=CARTESIAN_POINT ( 'NONE',  ( -0.03608642540484582190, 0.1707537476062198356, 0.01804586331702636229 ) ) ;
#4604=ORIENTED_EDGE ( 'NONE', *, *, #9806, .T. ) ;
#4606=AXIS2_PLACEMENT_3D ( 'NONE', #3756, #8525, #13300 ) ;
#4607=AXIS2_PLACEMENT_3D ( 'NONE', #884, #2218, #15061 ) ;
#4610=ORIENTED_EDGE ( 'NONE', *, *, #4801, .T. ) ;
#4613=PRODUCT_DEFINITION_FORMATION_WITH_SPECIFIED_SOURCE ( 'ANY', '', #8027, .NOT_KNOWN. ) ;
#4617=CARTESIAN_POINT ( 'NONE',  ( -1.947159199436097277, -2.887700558226605541, -0.1349403422227760663 ) ) ;
#4637=ORIENTED_EDGE ( 'NONE', *, *, #12702, .F. ) ;
#4643=CARTESIAN_POINT ( 'NONE',  ( -1.417802900492933782, -0.04287136159519128881, 0.07874015748031495954 ) ) ;
#4647=LINE ( 'NONE', #1990, #15390 ) ;
#4649=DIRECTION ( 'NONE',  ( 1.000000000000000000, 0.000000000000000000, 0.000000000000000000 ) ) ;
#4650=EDGE_CURVE ( 'NONE', #9785, #1873, #369, .T. ) ;
#4651=LINE ( 'NONE', #2292, #15136 ) ;
#4655=VECTOR ( 'NONE', #1185, 39.37007874015748854 ) ;
#4656=CARTESIAN_POINT ( 'NONE',  ( -1.352291563234457650, 0.1355266887446167634, 0.03937007874015747977 ) ) ;
#4663=VECTOR ( 'NONE', #5557, 39.37007874015748143 ) ;
#4664=CARTESIAN_POINT ( 'NONE',  ( -0.1771653543307086243, -0.02638708502139245488, 0.05905511811023622659 ) ) ;
#4667=CARTESIAN_POINT ( 'NONE',  ( -1.901321527450506199, -2.940045583547485020, -0.05830387289541953677 ) ) ;
#4676=DIRECTION ( 'NONE',  ( 1.000000000000000000, 0.000000000000000000, 0.000000000000000000 ) ) ;
#4688=CIRCLE ( 'NONE', #13440, 0.01968503937007875723 ) ;
#4693=ORIENTED_EDGE ( 'NONE', *, *, #8994, .F. ) ;
#4707=CARTESIAN_POINT ( 'NONE',  ( -1.919260770607501332, -2.820590578998671827, 0.1479534017216286024 ) ) ;
#4709=CARTESIAN_POINT ( 'NONE',  ( -2.003372420862888248, -2.780367306954143469, -0.1578439213240402372 ) ) ;
#4711=DIRECTION ( 'NONE',  ( 1.000000000000000000, 0.000000000000000000, 0.000000000000000000 ) ) ;
#4721=ADVANCED_FACE ( 'NONE', ( #7040 ), #1099, .T. ) ;
#4724=CARTESIAN_POINT ( 'NONE',  ( -1.397636319231197355, -0.02569771174688303961, 0.06949204706528756825 ) ) ;
#4732=DIRECTION ( 'NONE',  ( -0.1209298856814280260, 0.9926610512904576744, 0.000000000000000000 ) ) ;
#4741=CARTESIAN_POINT ( 'NONE',  ( -1.584115185264708625, 0.1296286773226378586, -0.03937007874015747977 ) ) ;
#4742=CARTESIAN_POINT ( 'NONE',  ( -1.234181327013985197, 0.1355266887446167634, 0.03937007874015747977 ) ) ;
#4748=CARTESIAN_POINT ( 'NONE',  ( -0.2362204724409448231, -0.02638708502139245488, 0.03937007874015747977 ) ) ;
#4757=CARTESIAN_POINT ( 'NONE',  ( -0.05639125304298656799, 0.1674615591801701664, 0.03403793048618138084 ) ) ;
#4759=CARTESIAN_POINT ( 'NONE',  ( -1.437672431148612429, -0.06355280397547365123, 0.1968503937007874127 ) ) ;
#4769=LINE ( 'NONE', #2266, #6117 ) ;
#4770=CARTESIAN_POINT ( 'NONE',  ( -1.580080891953811628, 0.1020406297922291511, 0.07874015748031495954 ) ) ;
#4771=CARTESIAN_POINT ( 'NONE',  ( -1.927122758893819121, -2.943756582367311747, -0.04519362198192262287 ) ) ;
#4778=CARTESIAN_POINT ( 'NONE',  ( -1.991673489327364432, -2.812934328829368003, 0.1541855436941547697 ) ) ;
#4784=CARTESIAN_POINT ( 'NONE',  ( -1.399712684983831723, -0.02644324255144274438, 0.07681107545239827805 ) ) ;
#4785=DIRECTION ( 'NONE',  ( 0.1209298856814283590, -0.9926610512904576744, 0.000000000000000000 ) ) ;
#4791=CARTESIAN_POINT ( 'NONE',  ( -0.3441669734936866343, 2.010494531933507467, 0.03937007874015747977 ) ) ;
#4792=CARTESIAN_POINT ( 'NONE',  ( -0.05074681685833758865, -0.1845569960845552526, 0.03403827111684314816 ) ) ;
#4800=CARTESIAN_POINT ( 'NONE',  ( -1.898742709278110841, -2.947125287889049261, -0.02947887163950623987 ) ) ;
#4801=EDGE_CURVE ( 'NONE', #4326, #3768, #478, .T. ) ;
#4809=ADVANCED_FACE ( 'NONE', ( #10018 ), #8365, .T. ) ;
#4810=DIRECTION ( 'NONE',  ( 0.000000000000000000, 0.5840537863397233798, -0.8117149589986825120 ) ) ;
#4813=ORIENTED_EDGE ( 'NONE', *, *, #9610, .T. ) ;
#4814=EDGE_LOOP ( 'NONE', ( #533, #5643, #4190, #1664, #1448, #2691, #5597, #3408 ) ) ;
#4828=ADVANCED_FACE ( 'NONE', ( #13613 ), #6480, .F. ) ;
#4829=CARTESIAN_POINT ( 'NONE',  ( -2.182693454834259139, -1.630005269948474389, -0.08366141732283423338 ) ) ;
#4838=CIRCLE ( 'NONE', #13591, 0.01968503937007875723 ) ;
#4842=CARTESIAN_POINT ( 'NONE',  ( -2.156938452685383645, -2.012428322114202306, 0.1097289591314137142 ) ) ;
#4844=CARTESIAN_POINT ( 'NONE',  ( -1.926823381055724260, -2.799657869570562063, 0.1538728403396771027 ) ) ;
#4846=DIRECTION ( 'NONE',  ( -0.9482728725910103407, -0.3174563893009453297, 0.000000000000000000 ) ) ;
#4847=CARTESIAN_POINT ( 'NONE',  ( -2.080881322745466999, -1.632190302820504479, 0.08366141732283424726 ) ) ;
#4851=CARTESIAN_POINT ( 'NONE',  ( -0.06155496847469428545, 0.1461038053415527060, -0.05764730824460249231 ) ) ;
#4854=VERTEX_POINT ( 'NONE', #10405 ) ;
#4864=CARTESIAN_POINT ( 'NONE',  ( -1.406518536868439195, -0.03328691616031433792, 0.04686241403499121633 ) ) ;
#4869=AXIS2_PLACEMENT_3D ( 'NONE', #13866, #491, #4070 ) ;
#4872=DIRECTION ( 'NONE',  ( -0.8144815189573203495, 0.5801894994542524664, -1.283760644411384396E-16 ) ) ;
#4874=CARTESIAN_POINT ( 'NONE',  ( -0.06762554849860653861, -0.1867557816141674765, 0.05879187219561141792 ) ) ;
#4891=CARTESIAN_POINT ( 'NONE',  ( -0.03802712947489397116, 0.1704066588063142818, 0.02158149019474815342 ) ) ;
#4895=DIRECTION ( 'NONE',  ( -0.9967194639908912857, 0.08093398607328357308, 0.000000000000000000 ) ) ;
#4898=FACE_OUTER_BOUND ( 'NONE', #10170, .T. ) ;
#4902=VERTEX_POINT ( 'NONE', #1867 ) ;
#4922=AXIS2_PLACEMENT_3D ( 'NONE', #7772, #10136, #13664 ) ;
#4926=CARTESIAN_POINT ( 'NONE',  ( -1.580259682937477539, 0.1018956540319142512, 0.04477369844320258641 ) ) ;
#4929=AXIS2_PLACEMENT_3D ( 'NONE', #7745, #13712, #12535 ) ;
#4935=CARTESIAN_POINT ( 'NONE',  ( -1.180847381077431146, 0.3433074774436084553, -0.04453711288976486965 ) ) ;
#4951=CARTESIAN_POINT ( 'NONE',  ( -0.05809364415030902895, 0.1671978997630559072, -0.03476146466084938796 ) ) ;
#4952=ORIENTED_EDGE ( 'NONE', *, *, #12225, .F. ) ;
#4956=CARTESIAN_POINT ( 'NONE',  ( -0.03726694595799353443, -0.1642704670929807653, 0.04781780748315901663 ) ) ;
#4958=ORIENTED_EDGE ( 'NONE', *, *, #165, .F. ) ;
#4962=SPHERICAL_SURFACE ( 'NONE', #6386, 0.01968503937007873988 ) ;
#4969=CARTESIAN_POINT ( 'NONE',  ( -1.957251767100264495, -2.772329397581817734, -0.1771653543307079026 ) ) ;
#4981=DIRECTION ( 'NONE',  ( -0.000000000000000000, 0.000000000000000000, 1.000000000000000000 ) ) ;
#4985=ORIENTED_EDGE ( 'NONE', *, *, #2244, .F. ) ;
#4989=ORIENTED_EDGE ( 'NONE', *, *, #5076, .T. ) ;
#4990=ORIENTED_EDGE ( 'NONE', *, *, #165, .T. ) ;
#4997=CARTESIAN_POINT ( 'NONE',  ( 0.000000000000000000, 0.000000000000000000, 0.05905511811023622659 ) ) ;
#4998=CARTESIAN_POINT ( 'NONE',  ( -1.882391615595319756, -2.915690172171810257, 0.04572057578730489430 ) ) ;
#4999=EDGE_CURVE ( 'NONE', #7929, #11495, #5845, .T. ) ;
#5001=CARTESIAN_POINT ( 'NONE',  ( -1.950427925093563220, -2.919740984733180333, -0.07234829986380927891 ) ) ;
#5010=DIRECTION ( 'NONE',  ( 0.8011800915434521553, -0.5984233124757303290, 0.000000000000000000 ) ) ;
#5011=FACE_OUTER_BOUND ( 'NONE', #10273, .T. ) ;
#5020=ORIENTED_EDGE ( 'NONE', *, *, #10108, .F. ) ;
#5022=ORIENTED_EDGE ( 'NONE', *, *, #13524, .T. ) ;
#5026=FACE_OUTER_BOUND ( 'NONE', #6966, .T. ) ;
#5031=DIRECTION ( 'NONE',  ( 1.000000000000000000, 0.000000000000000000, 0.000000000000000000 ) ) ;
#5035=VERTEX_POINT ( 'NONE', #7171 ) ;
#5040=CARTESIAN_POINT ( 'NONE',  ( -1.943332415744267072, -2.937030685955435594, 0.01138609156041062685 ) ) ;
#5044=DIRECTION ( 'NONE',  ( 0.000000000000000000, -0.000000000000000000, 1.000000000000000000 ) ) ;
#5046=CARTESIAN_POINT ( 'NONE',  ( -1.938095037791507824, -2.767575974228406732, 0.1578476300086600059 ) ) ;
#5049=VERTEX_POINT ( 'NONE', #48 ) ;
#5051=ORIENTED_EDGE ( 'NONE', *, *, #5670, .T. ) ;
#5058=EDGE_CURVE ( 'NONE', #877, #10762, #13433, .T. ) ;
#5063=FACE_OUTER_BOUND ( 'NONE', #4814, .T. ) ;
#5064=CARTESIAN_POINT ( 'NONE',  ( -1.883899324821880272, -2.911992577559399109, 0.05656501291315504942 ) ) ;
#5065=EDGE_LOOP ( 'NONE', ( #4327, #12283 ) ) ;
#5068=CARTESIAN_POINT ( 'NONE',  ( -0.07874015748031501505, 0.1442356988431298948, -0.05905511811023622659 ) ) ;
#5076=EDGE_CURVE ( 'NONE', #10028, #14086, #14930, .T. ) ;
#5080=DIRECTION ( 'NONE',  ( 1.000000000000000000, 0.000000000000000000, 0.000000000000000000 ) ) ;
#5081=AXIS2_PLACEMENT_3D ( 'NONE', #7786, #5268, #13757 ) ;
#5084=CARTESIAN_POINT ( 'NONE',  ( -0.07635964791965739462, -0.1878198040935885327, -0.05905511811023622659 ) ) ;
#5093=B_SPLINE_CURVE_WITH_KNOTS ( 'NONE', 3,
 ( #10351, #13021, #6813, #10515, #5558, #9265 ),
 .UNSPECIFIED., .F., .F.,
 ( 4, 2, 4 ),
 ( -5.605548034552286995E-06, 0.0004410309859948809271, 0.0008876675200243141616 ),
 .UNSPECIFIED. ) ;
#5096=EDGE_CURVE ( 'NONE', #14806, #7930, #12863, .T. ) ;
#5097=AXIS2_PLACEMENT_3D ( 'NONE', #14734, #310, #12227 ) ;
#5119=TOROIDAL_SURFACE ( 'NONE', #8896, 2.194881889763779181, 0.01968503937007873988 ) ;
#5127=CARTESIAN_POINT ( 'NONE',  ( -1.946977922026294605, -2.928246735464111072, -0.08439612660844164616 ) ) ;
#5128=CARTESIAN_POINT ( 'NONE',  ( -1.419615703680148000, -0.01226548409420231273, 0.07874015748031495954 ) ) ;
#5133=DIRECTION ( 'NONE',  ( 0.8180917953313872060, -0.5750876580239463465, 0.000000000000000000 ) ) ;
#5135=EDGE_CURVE ( 'NONE', #13899, #6200, #10055, .T. ) ;
#5143=ORIENTED_EDGE ( 'NONE', *, *, #13797, .T. ) ;
#5150=CARTESIAN_POINT ( 'NONE',  ( -1.868497805385690214, -2.949470162837682707, 0.01421723262671847204 ) ) ;
#5154=CARTESIAN_POINT ( 'NONE',  ( -1.403645773789551576, -0.004863036735870162816, -0.05905511811023622659 ) ) ;
#5156=ORIENTED_EDGE ( 'NONE', *, *, #11338, .T. ) ;
#5161=DIRECTION ( 'NONE',  ( 1.000000000000000000, 0.000000000000000000, 0.000000000000000000 ) ) ;
#5165=CARTESIAN_POINT ( 'NONE',  ( -0.004461712539986224628, -0.1607679992104108779, -0.007865172455356563355 ) ) ;
#5167=EDGE_CURVE ( 'NONE', #2172, #925, #8654, .T. ) ;
#5174=CARTESIAN_POINT ( 'NONE',  ( -2.755905511811024056, -1.630597114118275348, 8.792486876640390747 ) ) ;
#5186=CARTESIAN_POINT ( 'NONE',  ( -1.417802900492933782, -0.04287136159519133044, 0.07874015748031495954 ) ) ;
#5189=DIRECTION ( 'NONE',  ( -3.645101222232083416E-12, -4.880852986322028827E-12, -1.000000000000000000 ) ) ;
#5193=FACE_OUTER_BOUND ( 'NONE', #14322, .T. ) ;
#5194=AXIS2_PLACEMENT_3D ( 'NONE', #12465, #1560, #14744 ) ;
#5202=FACE_OUTER_BOUND ( 'NONE', #502, .T. ) ;
#5203=CARTESIAN_POINT ( 'NONE',  ( -1.947458820971768256, -2.927011135189118374, 0.05621523865303355155 ) ) ;
#5211=CARTESIAN_POINT ( 'NONE',  ( -1.276200637803905691, -0.1988000726501942539, 0.1968503937007874127 ) ) ;
#5212=DIRECTION ( 'NONE',  ( -0.000000000000000000, -2.212657494868377674E-16, 1.000000000000000000 ) ) ;
#5219=CARTESIAN_POINT ( 'NONE',  ( -1.387704745771440207, -0.02010536753476140082, -0.03937007874015747977 ) ) ;
#5222=DIRECTION ( 'NONE',  ( 0.000000000000000000, 0.000000000000000000, -1.000000000000000000 ) ) ;
#5226=PLANE ( 'NONE',  #2436 ) ;
#5227=CARTESIAN_POINT ( 'NONE',  ( -1.868482444096062789, -2.949506639258173024, -0.006642451843458160692 ) ) ;
#5229=LINE ( 'NONE', #7511, #8945 ) ;
#5234=EDGE_CURVE ( 'NONE', #631, #6704, #911, .T. ) ;
#5243=B_SPLINE_CURVE_WITH_KNOTS ( 'NONE', 3,
 ( #13390, #244, #6083, #14330, #1414, #8378, #13164, #1257 ),
 .UNSPECIFIED., .F., .F.,
 ( 4, 2, 2, 4 ),
 ( 0.000000000000000000, 0.0004641946399066459767, 0.0009283892798132919533, 0.001856778559626583907 ),
 .UNSPECIFIED. ) ;
#5248=VERTEX_POINT ( 'NONE', #5186 ) ;
#5251=CARTESIAN_POINT ( 'NONE',  ( -2.080881322745466999, -1.632190302820504257, 0.08366141732283423338 ) ) ;
#5259=CARTESIAN_POINT ( 'NONE',  ( -0.2362204724409448231, -0.02638708502139245488, -0.03937007874015747977 ) ) ;
#5262=EDGE_LOOP ( 'NONE', ( #15135, #10752, #11575, #2964 ) ) ;
#5265=ORIENTED_EDGE ( 'NONE', *, *, #12761, .F. ) ;
#5268=DIRECTION ( 'NONE',  ( -0.5801894994542525774, -0.8144815189573204606, 0.000000000000000000 ) ) ;
#5269=CARTESIAN_POINT ( 'NONE',  ( -1.938169220489598832, -2.949504990652386027, 0.006020211170025131266 ) ) ;
#5273=CARTESIAN_POINT ( 'NONE',  ( -1.997526618581371816, -2.796735537175909503, -0.1565704719341493578 ) ) ;
#5276=CARTESIAN_POINT ( 'NONE',  ( -1.904797909729390337, -2.859137677581157000, 0.1269363942893919350 ) ) ;
#5279=ORIENTED_EDGE ( 'NONE', *, *, #5473, .T. ) ;
#5285=CARTESIAN_POINT ( 'NONE',  ( -1.406483596012642945, -0.03325901290046209824, -0.04682391966548175855 ) ) ;
#5292=CARTESIAN_POINT ( 'NONE',  ( -1.181096721695571894, 0.3434326084030802084, 0.04453596627282299658 ) ) ;
#5293=CARTESIAN_POINT ( 'NONE',  ( -1.877572016762099727, -2.927690193651851569, 0.08555793721333695978 ) ) ;
#5308=CARTESIAN_POINT ( 'NONE',  ( -0.06762554849860662187, -0.1867557816141671156, -0.05879187219561133465 ) ) ;
#5314=CARTESIAN_POINT ( 'NONE',  ( -1.415033785308578818, -0.04025034750195270045, -0.05842314581460250622 ) ) ;
#5317=CIRCLE ( 'NONE', #3334, 0.01968503937007874682 ) ;
#5322=EDGE_LOOP ( 'NONE', ( #1267, #8169, #7556, #3508 ) ) ;
#5328=VECTOR ( 'NONE', #14575, 39.37007874015748143 ) ;
#5335=DIRECTION ( 'NONE',  ( 0.7402970580929290056, 0.6722799013647177135, 1.457774659155935170E-16 ) ) ;
#5337=LINE ( 'NONE', #3010, #11121 ) ;
#5339=AXIS2_PLACEMENT_3D ( 'NONE', #2093, #14878, #13706 ) ;
#5341=ORIENTED_EDGE ( 'NONE', *, *, #10108, .T. ) ;
#5346=ORIENTED_EDGE ( 'NONE', *, *, #13764, .T. ) ;
#5349=CARTESIAN_POINT ( 'NONE',  ( -1.950663589855595736, -2.877608764542115782, 0.1430332175041234555 ) ) ;
#5355=CARTESIAN_POINT ( 'NONE',  ( -1.983835277982623380, -2.834152059666824375, -0.1479904830673641758 ) ) ;
#5360=EDGE_CURVE ( 'NONE', #9606, #12240, #3733, .T. ) ;
#5363=ADVANCED_FACE ( 'NONE', ( #2222 ), #15064, .F. ) ;
#5367=ORIENTED_EDGE ( 'NONE', *, *, #1764, .F. ) ;
#5373=CIRCLE ( 'NONE', #2876, 0.01968503937007880233 ) ;
#5377=CARTESIAN_POINT ( 'NONE',  ( -2.184126211765464287, -1.725292181286298021, 0.08417626406393743932 ) ) ;
#5382=CARTESIAN_POINT ( 'NONE',  ( -1.182069932165816351, 0.3415656170894307286, 0.04962985469508127828 ) ) ;
#5384=FACE_OUTER_BOUND ( 'NONE', #9295, .T. ) ;
#5387=CARTESIAN_POINT ( 'NONE',  ( -1.992382107315056716, -2.749515453455444902, -0.1756903148397133130 ) ) ;
#5390=EDGE_CURVE ( 'NONE', #9996, #14180, #4647, .T. ) ;
#5395=AXIS2_PLACEMENT_3D ( 'NONE', #15139, #13740, #2134 ) ;
#5397=AXIS2_PLACEMENT_3D ( 'NONE', #5749, #8339, #15325 ) ;
#5407=CARTESIAN_POINT ( 'NONE',  ( -1.417802900492933782, -0.04287136159519135820, -0.07874015748031495954 ) ) ;
#5408=DIRECTION ( 'NONE',  ( -0.000000000000000000, -0.000000000000000000, -1.000000000000000000 ) ) ;
#5409=ORIENTED_EDGE ( 'NONE', *, *, #2027, .T. ) ;
#5416=CARTESIAN_POINT ( 'NONE',  ( -1.491640810881974755, 0.2222636556240916161, 0.05905511811023622659 ) ) ;
#5420=CARTESIAN_POINT ( 'NONE',  ( -0.004867930653580591037, 0.1761271985362268533, -0.009096853601410393939 ) ) ;
#5425=EDGE_LOOP ( 'NONE', ( #13576, #12089, #1146, #1960, #4000, #14760 ) ) ;
#5432=AXIS2_PLACEMENT_3D ( 'NONE', #4362, #11189, #5222 ) ;
#5438=EDGE_CURVE ( 'NONE', #11495, #6564, #7360, .T. ) ;
#5440=CARTESIAN_POINT ( 'NONE',  ( -1.978999946204262006, -2.792301496701129704, 0.1761415058630058927 ) ) ;
#5441=DIRECTION ( 'NONE',  ( 1.000000000000000000, 0.000000000000000000, 0.000000000000000000 ) ) ;
#5463=CARTESIAN_POINT ( 'NONE',  ( -1.180847381051831180, 0.3433074774307591781, 0.03937007874014957637 ) ) ;
#5464=CYLINDRICAL_SURFACE ( 'NONE', #1152, 0.01968503937007875723 ) ;
#5473=EDGE_CURVE ( 'NONE', #6948, #12093, #5768, .T. ) ;
#5481=CARTESIAN_POINT ( 'NONE',  ( -2.026798844142627676, -2.454534756249174166, 0.1228056342163675041 ) ) ;
#5483=FACE_OUTER_BOUND ( 'NONE', #2943, .T. ) ;
#5500=CARTESIAN_POINT ( 'NONE',  ( -2.184126211765464287, -1.725292181286280258, -0.08417626406393655114 ) ) ;
#5504=B_SPLINE_CURVE_WITH_KNOTS ( 'NONE', 3,
 ( #5550, #12683, #11265, #2882, #7808, #5377 ),
 .UNSPECIFIED., .F., .F.,
 ( 4, 2, 4 ),
 ( 0.000000000000000000, 0.01333398518358727691, 0.02666797036717455383 ),
 .UNSPECIFIED. ) ;
#5509=EDGE_LOOP ( 'NONE', ( #10848, #3995, #12970, #4610 ) ) ;
#5511=CARTESIAN_POINT ( 'NONE',  ( -1.969687200836069740, -2.871348872261489493, 0.1474822870563181620 ) ) ;
#5513=CARTESIAN_POINT ( 'NONE',  ( -1.185322952774772842, 0.3350001135380079043, -0.05695403133965425829 ) ) ;
#5516=DIRECTION ( 'NONE',  ( -0.9453712468369984689, -0.3259957141648626711, 0.000000000000000000 ) ) ;
#5517=CARTESIAN_POINT ( 'NONE',  ( -2.006299088073100201, -2.563573505072143099, -0.1516713583102864971 ) ) ;
#5523=CARTESIAN_POINT ( 'NONE',  ( -1.387074828437381280, -0.01127692237434234704, -0.07874015748031495954 ) ) ;
#5529=CARTESIAN_POINT ( 'NONE',  ( -1.938021061366714815, -2.767805340190703678, -0.1776219654715974205 ) ) ;
#5549=EDGE_CURVE ( 'NONE', #6200, #4854, #13598, .T. ) ;
#5550=CARTESIAN_POINT ( 'NONE',  ( -2.010991777528384983, -2.758467574604075434, 0.1561691687464104861 ) ) ;
#5553=B_SPLINE_CURVE_WITH_KNOTS ( 'NONE', 3,
 ( #11457, #12718, #1977, #651, #4475, #15215 ),
 .UNSPECIFIED., .F., .F.,
 ( 4, 2, 4 ),
 ( -1.812136377038870460E-05, 0.0003725347987152521890, 0.0007631909612008931469 ),
 .UNSPECIFIED. ) ;
#5556=EDGE_CURVE ( 'NONE', #10031, #13232, #7256, .T. ) ;
#5557=DIRECTION ( 'NONE',  ( 0.000000000000000000, 0.000000000000000000, 1.000000000000000000 ) ) ;
#5558=CARTESIAN_POINT ( 'NONE',  ( -0.002500327830562646542, 0.1591396728618060807, 8.151557182427766114E-17 ) ) ;
#5563=CARTESIAN_POINT ( 'NONE',  ( -1.574484809660414042, 0.1100025355989073528, 0.06175692796217682051 ) ) ;
#5565=CARTESIAN_POINT ( 'NONE',  ( -0.3441669734936866343, 2.010494531933507467, -0.03937007874015747977 ) ) ;
#5569=CARTESIAN_POINT ( 'NONE',  ( -1.579560458409220658, 0.1027931408840447314, 0.07190451969771766150 ) ) ;
#5583=CARTESIAN_POINT ( 'NONE',  ( -2.010991777528384983, -2.758467574604075434, 0.1561691687464104861 ) ) ;
#5585=CARTESIAN_POINT ( 'NONE',  ( -0.2952755905511810219, -0.02638708502139244100, -0.05905511811023622659 ) ) ;
#5592=CARTESIAN_POINT ( 'NONE',  ( -2.046508481693990689, -2.384357855454588115, -0.1146367095086625459 ) ) ;
#5597=ORIENTED_EDGE ( 'NONE', *, *, #720, .T. ) ;
#5598=EDGE_LOOP ( 'NONE', ( #2773, #1878, #6162, #7159 ) ) ;
#5599=ORIENTED_EDGE ( 'NONE', *, *, #8374, .F. ) ;
#5606=CARTESIAN_POINT ( 'NONE',  ( -0.1771653543307086243, -0.02638708502139245488, -0.03937007874015747977 ) ) ;
#5610=CARTESIAN_POINT ( 'NONE',  ( -0.04489243112415021442, 0.1480120765563121277, 0.05194558739574919176 ) ) ;
#5615=CARTESIAN_POINT ( 'NONE',  ( -1.916733123353825841, -2.896650666303147492, -0.1268322157999333955 ) ) ;
#5625=AXIS2_PLACEMENT_3D ( 'NONE', #1667, #6424, #12397 ) ;
#5627=CARTESIAN_POINT ( 'NONE',  ( -1.276200637803905691, -0.1988000726501942539, -0.05905511811023622659 ) ) ;
#5628=CARTESIAN_POINT ( 'NONE',  ( -1.967323444231620533, -2.828292283972135390, 0.1684768507627448786 ) ) ;
#5641=TOROIDAL_SURFACE ( 'NONE', #14420, 2.814960629921260171, 0.01968503937007873988 ) ;
#5643=ORIENTED_EDGE ( 'NONE', *, *, #7042, .T. ) ;
#5648=EDGE_CURVE ( 'NONE', #10031, #4530, #14652, .T. ) ;
#5658=CARTESIAN_POINT ( 'NONE',  ( -2.755905511811024056, 0.2985367441494412022, 0.1033464566929133965 ) ) ;
#5667=EDGE_CURVE ( 'NONE', #10393, #14556, #1884, .T. ) ;
#5669=CARTESIAN_POINT ( 'NONE',  ( -1.983826685957652103, -2.834175259062820640, 0.1479833052181933617 ) ) ;
#5670=EDGE_CURVE ( 'NONE', #2668, #13620, #14753, .T. ) ;
#5671=DIRECTION ( 'NONE',  ( 0.6461174802832408970, -0.7632379718491709708, 0.000000000000000000 ) ) ;
#5685=CARTESIAN_POINT ( 'NONE',  ( -1.572630165645363398, 0.1123721976955502078, -0.05999513677271276629 ) ) ;
#5693=CARTESIAN_POINT ( 'NONE',  ( -1.938116314515752947, -2.767513626600481835, -0.1578457079742228708 ) ) ;
#5695=DIRECTION ( 'NONE',  ( 0.8483823383050430600, 0.5293839892290546079, -3.673339335687577446E-15 ) ) ;
#5702=ADVANCED_FACE ( 'NONE', ( #1505 ), #2675, .T. ) ;
#5706=CARTESIAN_POINT ( 'NONE',  ( -1.985311755390524624, -2.772329397582317778, 0.1771653543307079026 ) ) ;
#5717=EDGE_LOOP ( 'NONE', ( #15178, #1264, #4277 ) ) ;
#5720=CARTESIAN_POINT ( 'NONE',  ( -1.253866366384063902, 0.1355266887446167634, 0.03937007874015747977 ) ) ;
#5726=CARTESIAN_POINT ( 'NONE',  ( -1.958689581535855373, -2.899312375919938400, -0.1241928182215008836 ) ) ;
#5736=ORIENTED_EDGE ( 'NONE', *, *, #6481, .F. ) ;
#5737=ORIENTED_EDGE ( 'NONE', *, *, #5167, .T. ) ;
#5741=CARTESIAN_POINT ( 'NONE',  ( -1.906721773844014534, -2.925049931903382916, 0.09056425822888818089 ) ) ;
#5742=SHAPE_REPRESENTATION_RELATIONSHIP ( 'NONE' , 'NONE' ,  #12105, #14739 ) ;
#5748=CARTESIAN_POINT ( 'NONE',  ( -0.2362204724409448231, -0.02638708502139245488, -0.05905511811023622659 ) ) ;
#5749=CARTESIAN_POINT ( 'NONE',  ( 0.7052242655755273093, -1.858423098537180129, 0.1033464566929129108 ) ) ;
#5758=CARTESIAN_POINT ( 'NONE',  ( -0.04047196874988589349, 0.1700209211169187440, 0.02286660095798146927 ) ) ;
#5759=CARTESIAN_POINT ( 'NONE',  ( -0.03747986570939450257, -0.1642921853714506275, -0.04794034192644638925 ) ) ;
#5766=PRODUCT_DEFINITION_SHAPE ( 'NONE', 'NONE',  #561 ) ;
#5767=EDGE_LOOP ( 'NONE', ( #3262, #2065, #2791 ) ) ;
#5768=( BOUNDED_CURVE ( )  B_SPLINE_CURVE ( 3, ( #8180, #12645, #1916, #5563 ),
 .UNSPECIFIED., .F., .T. ) 
 B_SPLINE_CURVE_WITH_KNOTS ( ( 4, 4 ),
 ( 1.570796326794899667, 2.100913045340505825 ),
 .UNSPECIFIED. ) 
 CURVE ( )  GEOMETRIC_REPRESENTATION_ITEM ( )  RATIONAL_B_SPLINE_CURVE ( ( 1.000000000000000000, 0.9767181429356339706, 0.9767181429356339706, 1.000000000000000000 ) ) 
 REPRESENTATION_ITEM ( '' )  );
#5772=DIRECTION ( 'NONE',  ( 1.000000000000000000, 0.000000000000000000, 0.000000000000000000 ) ) ;
#5775=CARTESIAN_POINT ( 'NONE',  ( -1.928549775957746570, -2.939860280416023652, -0.05881069861817015548 ) ) ;
#5778=CARTESIAN_POINT ( 'NONE',  ( -1.181096721701077046, 0.3434326084059158846, -0.04453596627218543019 ) ) ;
#5796=CARTESIAN_POINT ( 'NONE',  ( -2.755905511811024056, -2.772329397582842248, 0.1771653543307079026 ) ) ;
#5800=CARTESIAN_POINT ( 'NONE',  ( -0.07874015748031494566, 0.1442356988431297837, 0.03937007874015747977 ) ) ;
#5801=EDGE_CURVE ( 'NONE', #7004, #9440, #2128, .T. ) ;
#5808=VERTEX_POINT ( 'NONE', #11591 ) ;
#5813=CARTESIAN_POINT ( 'NONE',  ( -1.957251767100264495, -2.772329397581817734, -0.1771653543307079026 ) ) ;
#5818=CARTESIAN_POINT ( 'NONE',  ( -2.090051324975637836, -1.782906609499567585, -0.08465180024024840377 ) ) ;
#5823=VECTOR ( 'NONE', #10391, 39.37007874015748854 ) ;
#5825=AXIS2_PLACEMENT_3D ( 'NONE', #4300, #13957, #1741 ) ;
#5826=ORIENTED_EDGE ( 'NONE', *, *, #12561, .T. ) ;
#5828=DIRECTION ( 'NONE',  ( -0.5801894994542512451, -0.8144815189573213488, 0.000000000000000000 ) ) ;
#5833=AXIS2_PLACEMENT_3D ( 'NONE', #552, #6251, #8778 ) ;
#5838=ADVANCED_FACE ( 'NONE', ( #10500 ), #4267, .F. ) ;
#5843=EDGE_CURVE ( 'NONE', #925, #13968, #5933, .T. ) ;
#5845=CIRCLE ( 'NONE', #5339, 0.01968503937007875723 ) ;
#5848=AXIS2_PLACEMENT_3D ( 'NONE', #7961, #15250, #13996 ) ;
#5855=CARTESIAN_POINT ( 'NONE',  ( -1.925023804306413622, -2.949475017834376711, -0.01222676651384939014 ) ) ;
#5858=AXIS2_PLACEMENT_3D ( 'NONE', #11788, #13980, #2056 ) ;
#5860=FACE_OUTER_BOUND ( 'NONE', #13525, .T. ) ;
#5862=AXIS2_PLACEMENT_3D ( 'NONE', #14508, #8538, #13313 ) ;
#5863=VERTEX_POINT ( 'NONE', #16 ) ;
#5864=CARTESIAN_POINT ( 'NONE',  ( -2.003370110189420572, -2.780373828034933492, 0.1578437203291705448 ) ) ;
#5865=( BOUNDED_SURFACE ( )  B_SPLINE_SURFACE ( 3, 2, ( 
 ( #8728, #1750, #12324 ),
 ( #11293, #3003, #9985 ),
 ( #7769, #14764, #1816 ),
 ( #6581, #7935, #14121 ),
 ( #13972, #6992, #3238 ),
 ( #661, #12641, #1987 ),
 ( #15296, #6747, #11704 ),
 ( #1911, #6815, #4406 ),
 ( #3160, #5420, #739 ),
 ( #11536, #8175, #13807 ) ),
 .UNSPECIFIED., .F., .F., .T. ) 
 B_SPLINE_SURFACE_WITH_KNOTS ( ( 4, 2, 2, 2, 4 ),
 ( 3, 3 ),
 ( 0.004868238565068919166, 0.005367227319713948480, 0.005866216074358976927, 0.006365204829004005374, 0.006864193583649034688 ),
 ( 0.000000000000000000, 1.000000000000000000 ),
 .UNSPECIFIED. ) 
 GEOMETRIC_REPRESENTATION_ITEM ( )  RATIONAL_B_SPLINE_SURFACE ( (
 ( 1.000000000000000000, 0.7071067811865475727, 1.000000000000000000),
 ( 1.000000000000000000, 0.7015640395779025873, 1.000000000000000000),
 ( 1.000000000000000000, 0.6956970733052282307, 1.000000000000000000),
 ( 1.000000000000000000, 0.6834122233792360168, 1.000000000000000000),
 ( 1.000000000000000000, 0.6772899333991397874, 1.000000000000000000),
 ( 1.000000000000000000, 0.6655724472122266366, 1.000000000000000000),
 ( 1.000000000000000000, 0.6602173990144631910, 1.000000000000000000),
 ( 1.000000000000000000, 0.6512508157287247856, 1.000000000000000000),
 ( 1.000000000000000000, 0.6477776718209199425, 1.000000000000000000),
 ( 1.000000000000000000, 0.6456929433798523910, 1.000000000000000000) ) ) 
 REPRESENTATION_ITEM ( '' )  SURFACE ( )  );
#5870=ORIENTED_EDGE ( 'NONE', *, *, #12365, .F. ) ;
#5871=ADVANCED_FACE ( 'NONE', ( #5860 ), #564, .T. ) ;
#5873=ORIENTED_EDGE ( 'NONE', *, *, #6481, .T. ) ;
#5874=ORIENTED_EDGE ( 'NONE', *, *, #1698, .F. ) ;
#5882=CARTESIAN_POINT ( 'NONE',  ( -1.419615703517932426, -0.01226548420975529831, 0.07609966981162474831 ) ) ;
#5895=AXIS2_PLACEMENT_3D ( 'NONE', #7537, #7311, #10770 ) ;
#5896=ORIENTED_EDGE ( 'NONE', *, *, #1675, .T. ) ;
#5900=ADVANCED_FACE ( 'NONE', ( #1952 ), #6634, .T. ) ;
#5901=ORIENTED_EDGE ( 'NONE', *, *, #8788, .F. ) ;
#5905=CARTESIAN_POINT ( 'NONE',  ( -1.953792234680448159, -2.783667854742955416, 0.1771653543307004364 ) ) ;
#5908=AXIS2_PLACEMENT_3D ( 'NONE', #4180, #5335, #744 ) ;
#5918=ADVANCED_FACE ( 'NONE', ( #5384 ), #5464, .T. ) ;
#5919=CARTESIAN_POINT ( 'NONE',  ( -0.2952755905511810219, -0.02638708502139244794, 0.03937007874015747977 ) ) ;
#5925=AXIS2_PLACEMENT_3D ( 'NONE', #7904, #5695, #12690 ) ;
#5927=ORIENTED_EDGE ( 'NONE', *, *, #1012, .F. ) ;
#5933=B_SPLINE_CURVE_WITH_KNOTS ( 'NONE', 3,
 ( #7125, #9728, #2270, #10735, #14499, #85, #11832, #14333, #13075, #13240 ),
 .UNSPECIFIED., .F., .F.,
 ( 4, 2, 2, 2, 4 ),
 ( 0.000000000000000000, 0.003638111460239016465, 0.007276222920478032929, 0.01455244584095600514, 0.02910489168191195131 ),
 .UNSPECIFIED. ) ;
#5941=CARTESIAN_POINT ( 'NONE',  ( -1.933241136925626824, -2.926924945584949533, -0.08676524546727019949 ) ) ;
#5943=CARTESIAN_POINT ( 'NONE',  ( -1.967325247738501703, -2.828286626395489556, -0.1684772211806224995 ) ) ;
#5946=B_SPLINE_CURVE_WITH_KNOTS ( 'NONE', 3,
 ( #2037, #2121, #962, #3295, #8065, #6897, #3533, #1033, #15284, #10505 ),
 .UNSPECIFIED., .F., .F.,
 ( 4, 2, 2, 2, 4 ),
 ( 7.655474390655438337E-20, 0.0006605458767770998286, 0.001321091753554199440, 0.001981637630331298944, 0.002642183507108398881 ),
 .UNSPECIFIED. ) ;
#5947=ORIENTED_EDGE ( 'NONE', *, *, #1310, .F. ) ;
#5948=CARTESIAN_POINT ( 'NONE',  ( -1.946003491706560506, -2.930556585132634506, -0.04593750474734910327 ) ) ;
#5949=CARTESIAN_POINT ( 'NONE',  ( -1.276200637803905691, -0.1988000726501942539, 0.1033464566929132716 ) ) ;
#5951=FACE_OUTER_BOUND ( 'NONE', #2869, .T. ) ;
#5964=CARTESIAN_POINT ( 'NONE',  ( -1.580080891953811628, 0.1020406297922293454, -0.07874015748031495954 ) ) ;
#5988=CARTESIAN_POINT ( 'NONE',  ( -1.407046561513447758, -0.03370566694352346293, 0.04739997601650549480 ) ) ;
#5991=ORIENTED_EDGE ( 'NONE', *, *, #7982, .T. ) ;
#5992=ORIENTED_EDGE ( 'NONE', *, *, #3524, .T. ) ;
#5994=DIRECTION ( 'NONE',  ( 1.000000000000000000, 0.000000000000000000, 0.000000000000000000 ) ) ;
#5999=B_SPLINE_CURVE_WITH_KNOTS ( 'NONE', 3,
 ( #5706, #15206, #14023, #10425, #5628, #4536, #2339, #3286, #11588, #11923, #12772, #2030, #10497, #15354, #9248, #8233, #861, #8057, #1025, #5855, #9318, #12842, #5775, #4385, #2112, #10568, #6889, #4617, #13072, #11683, #2200, #5943, #6974, #6797, #15116, #953 ),
 .UNSPECIFIED., .F., .F.,
 ( 4, 2, 2, 2, 2, 2, 2, 2, 2, 2, 2, 2, 2, 2, 2, 2, 2, 4 ),
 ( 0.0006039794861555876143, 0.001506811385715726981, 0.002409643285275866239, 0.003312475184836005931, 0.004215307084396146056, 0.005118138983956285748, 0.006020970883516425440, 0.006923802783076565999, 0.007375218732856640182, 0.007826634682636715232, 0.008729466582196863597, 0.009632298481757010228, 0.01053513038131715859, 0.01143796228087730696, 0.01234079418043745706, 0.01324362607999760716, 0.01414645797955775379, 0.01504928987911790389 ),
 .UNSPECIFIED. ) ;
#6000=ORIENTED_EDGE ( 'NONE', *, *, #3723, .F. ) ;
#6009=CARTESIAN_POINT ( 'NONE',  ( -1.596214514379725946, 0.1135332894431583389, 0.07535569387264980101 ) ) ;
#6010=DIRECTION ( 'NONE',  ( 0.000000000000000000, 0.000000000000000000, -1.000000000000000000 ) ) ;
#6014=CARTESIAN_POINT ( 'NONE',  ( -1.951076232067097349, -2.792370830351091904, 0.1761340083271971391 ) ) ;
#6017=DIRECTION ( 'NONE',  ( 0.000000000000000000, 2.212657494868377674E-16, -1.000000000000000000 ) ) ;
#6024=CARTESIAN_POINT ( 'NONE',  ( -1.398374251180654060, -0.02596405602755174485, 0.07123060654724291951 ) ) ;
#6027=CYLINDRICAL_SURFACE ( 'NONE', #7681, 1.865354330708661745 ) ;
#6030=ADVANCED_FACE ( 'NONE', ( #9708 ), #8901, .T. ) ;
#6031=CARTESIAN_POINT ( 'NONE',  ( -1.595687817112585005, 0.1142625427333565924, -0.07194693897044758535 ) ) ;
#6033=CARTESIAN_POINT ( 'NONE',  ( -0.06154672136187318982, -0.1666784585780658190, 0.05764611276129245204 ) ) ;
#6036=VERTEX_POINT ( 'NONE', #10787 ) ;
#6037=ADVANCED_FACE ( 'NONE', ( #9624 ), #3659, .T. ) ;
#6038=ORIENTED_EDGE ( 'NONE', *, *, #14685, .F. ) ;
#6067=AXIS2_PLACEMENT_3D ( 'NONE', #4748, #11804, #10623 ) ;
#6068=CARTESIAN_POINT ( 'NONE',  ( -2.184126211765464287, -1.725292181286280258, -0.08417626406393655114 ) ) ;
#6070=AXIS2_PLACEMENT_3D ( 'NONE', #13850, #1000, #10093 ) ;
#6075=AXIS2_PLACEMENT_3D ( 'NONE', #5919, #7095, #14310 ) ;
#6079=ADVANCED_FACE ( 'NONE', ( #14784 ), #6885, .T. ) ;
#6081=LINE ( 'NONE', #80, #12661 ) ;
#6083=CARTESIAN_POINT ( 'NONE',  ( -0.06425120930260366792, -0.1863186860285575008, -0.03845354371037630614 ) ) ;
#6086=CARTESIAN_POINT ( 'NONE',  ( -1.899889809402484087, -2.871954297241456455, 0.1472027794511626131 ) ) ;
#6088=CARTESIAN_POINT ( 'NONE',  ( -1.962446787563433270, -2.889798350705808705, 0.1130053219567358630 ) ) ;
#6089=AXIS2_PLACEMENT_3D ( 'NONE', #7310, #214, #5031 ) ;
#6091=ORIENTED_EDGE ( 'NONE', *, *, #13678, .F. ) ;
#6094=CIRCLE ( 'NONE', #1606, 0.01968503937007875376 ) ;
#6095=CIRCLE ( 'NONE', #6338, 0.01968503937007875723 ) ;
#6109=VECTOR ( 'NONE', #11764, 39.37007874015748854 ) ;
#6112=CARTESIAN_POINT ( 'NONE',  ( -1.579560462701998569, 0.1027931347612302260, -0.07190453453446270238 ) ) ;
#6117=VECTOR ( 'NONE', #7039, 39.37007874015748143 ) ;
#6132=CARTESIAN_POINT ( 'NONE',  ( -0.02641567992992046449, 0.1724028871747071145, 1.853431881210122409E-17 ) ) ;
#6135=CARTESIAN_POINT ( 'NONE',  ( -1.431036756819011213, -0.02829858486107871343, 0.08366141732283458032 ) ) ;
#6137=CIRCLE ( 'NONE', #11405, 0.01968503937007872254 ) ;
#6138=B_SPLINE_CURVE_WITH_KNOTS ( 'NONE', 3,
 ( #5068, #89, #4851, #9654, #3693, #14430, #8471, #12068, #6488, #13626 ),
 .UNSPECIFIED., .F., .F.,
 ( 4, 2, 2, 2, 4 ),
 ( 0.000000000000000000, 0.0006582318843486420663, 0.001316463768697284133, 0.001974695653045926199, 0.002632927537394568265 ),
 .UNSPECIFIED. ) ;
#6139=CARTESIAN_POINT ( 'NONE',  ( -1.417126644544185021, -0.04224944786056485102, 0.06861491064343343271 ) ) ;
#6143=ORIENTED_EDGE ( 'NONE', *, *, #4526, .T. ) ;
#6148=B_SPLINE_CURVE_WITH_KNOTS ( 'NONE', 3,
 ( #14786, #466, #14949, #7881, #6612, #690 ),
 .UNSPECIFIED., .F., .F.,
 ( 4, 2, 4 ),
 ( 0.000000000000000000, 0.01440388436194932689, 0.02880776872389865378 ),
 .UNSPECIFIED. ) ;
#6162=ORIENTED_EDGE ( 'NONE', *, *, #7283, .T. ) ;
#6163=ORIENTED_EDGE ( 'NONE', *, *, #15276, .F. ) ;
#6164=ORIENTED_EDGE ( 'NONE', *, *, #2513, .F. ) ;
#6167=CARTESIAN_POINT ( 'NONE',  ( -1.992382107315058271, -2.749515453455440905, 0.1756903148397124803 ) ) ;
#6171=DIRECTION ( 'NONE',  ( -0.5984233124757303290, -0.8011800915434521553, 0.000000000000000000 ) ) ;
#6173=CARTESIAN_POINT ( 'NONE',  ( -1.889963351875279196, -2.896989719539225572, -0.08666351837760270793 ) ) ;
#6175=CARTESIAN_POINT ( 'NONE',  ( -2.010991777528384095, -2.758467574604078543, -0.1561691687464109024 ) ) ;
#6191=CARTESIAN_POINT ( 'NONE',  ( -0.03044903239804774148, 0.1717056406757088149, -0.01152843233334087045 ) ) ;
#6195=CARTESIAN_POINT ( 'NONE',  ( -0.03747986570939449563, -0.1642921853714506830, 0.04794034192644637538 ) ) ;
#6199=ORIENTED_EDGE ( 'NONE', *, *, #894, .T. ) ;
#6200=VERTEX_POINT ( 'NONE', #12214 ) ;
#6205=DIRECTION ( 'NONE',  ( 0.000000000000000000, 0.000000000000000000, -1.000000000000000000 ) ) ;
#6209=CARTESIAN_POINT ( 'NONE',  ( -1.419615703680148000, -0.01226548409420231273, 0.07874015748031495954 ) ) ;
#6211=FACE_OUTER_BOUND ( 'NONE', #10932, .T. ) ;
#6212=CARTESIAN_POINT ( 'NONE',  ( -1.580259682937499965, 0.1018956540319304049, 0.04477369844320259334 ) ) ;
#6213=CARTESIAN_POINT ( 'NONE',  ( -2.100501784635051550, -1.630597114118274460, -0.08366141732283423338 ) ) ;
#6216=ORIENTED_EDGE ( 'NONE', *, *, #12530, .F. ) ;
#6218=ADVANCED_FACE ( 'NONE', ( #12436 ), #8147, .T. ) ;
#6220=CARTESIAN_POINT ( 'NONE',  ( -1.940380551367184125, -2.944208869897690928, 0.04343028329486892797 ) ) ;
#6221=LINE ( 'NONE', #1390, #12238 ) ;
#6223=CARTESIAN_POINT ( 'NONE',  ( -1.591501945092674841, 0.08600752902535285793, 0.07874015748031495954 ) ) ;
#6231=ORIENTED_EDGE ( 'NONE', *, *, #4999, .F. ) ;
#6232=ORIENTED_EDGE ( 'NONE', *, *, #13183, .T. ) ;
#6236=CARTESIAN_POINT ( 'NONE',  ( -1.414139891776604818, -0.03961000916150922424, -0.05844465851538532125 ) ) ;
#6241=CARTESIAN_POINT ( 'NONE',  ( -1.891382748001904535, -2.893416385725415374, 0.09138685817115685395 ) ) ;
#6243=CARTESIAN_POINT ( 'NONE',  ( -2.176576600059022759, -2.015093358877955154, -0.09005837916855936875 ) ) ;
#6246=ADVANCED_FACE ( 'NONE', ( #12514 ), #2900, .T. ) ;
#6251=DIRECTION ( 'NONE',  ( 0.000000000000000000, 0.000000000000000000, 1.000000000000000000 ) ) ;
#6254=CARTESIAN_POINT ( 'NONE',  ( -0.03005672326763337773, -0.1816858507396494349, -0.01806077797202005480 ) ) ;
#6257=DIRECTION ( 'NONE',  ( -0.000000000000000000, 0.000000000000000000, 1.000000000000000000 ) ) ;
#6259=CARTESIAN_POINT ( 'NONE',  ( -0.01782267696647954827, -0.1622289191103822581, 0.03095755538600573897 ) ) ;
#6260=CARTESIAN_POINT ( 'NONE',  ( -0.002500327830562678200, 0.1532658568795227105, 0.000000000000000000 ) ) ;
#6261=ORIENTED_EDGE ( 'NONE', *, *, #3570, .F. ) ;
#6270=CARTESIAN_POINT ( 'NONE',  ( -2.080881322745466555, -1.632190302820504257, 0.1033464566929129802 ) ) ;
#6277=CARTESIAN_POINT ( 'NONE',  ( -0.07874015748031543138, -0.1682792322177920907, -0.05905511811023622659 ) ) ;
#6279=EDGE_LOOP ( 'NONE', ( #736, #11792, #1651 ) ) ;
#6284=CARTESIAN_POINT ( 'NONE',  ( -1.946824355069869394, -2.928629402500327661, 0.08439192439263279444 ) ) ;
#6286=DIRECTION ( 'NONE',  ( -0.000000000000000000, -0.000000000000000000, -1.000000000000000000 ) ) ;
#6290=CARTESIAN_POINT ( 'NONE',  ( -1.889903596530551733, -2.897138837246827414, -0.08643254935806948813 ) ) ;
#6295=EDGE_LOOP ( 'NONE', ( #1732, #4604, #10685, #10324, #12027 ) ) ;
#6297=CARTESIAN_POINT ( 'NONE',  ( -1.391725923719789426, -0.02262183056853206073, -0.06139678143372313823 ) ) ;
#6300=AXIS2_PLACEMENT_3D ( 'NONE', #8749, #12127, #10859 ) ;
#6307=CARTESIAN_POINT ( 'NONE',  ( -1.187809996375178034, 0.3305575196843282271, 0.05905511802048958592 ) ) ;
#6308=CARTESIAN_POINT ( 'NONE',  ( -1.897884506782005376, -2.949473116112335536, 0.01330914593066468560 ) ) ;
#6310=FACE_OUTER_BOUND ( 'NONE', #14645, .T. ) ;
#6320=VERTEX_POINT ( 'NONE', #757 ) ;
#6329=CARTESIAN_POINT ( 'NONE',  ( -0.02345217991005641225, -0.1628325660491150295, -0.03705913340085396912 ) ) ;
#6331=CARTESIAN_POINT ( 'NONE',  ( -1.969442568012797157, -2.674162197727227408, 0.1468011070627323611 ) ) ;
#6338=AXIS2_PLACEMENT_3D ( 'NONE', #14461, #9037, #14999 ) ;
#6339=CARTESIAN_POINT ( 'NONE',  ( -0.01854992166427318900, -0.1800031784444983685, -0.005378007177148339153 ) ) ;
#6347=CIRCLE ( 'NONE', #9635, 0.03937007874015747977 ) ;
#6352=CARTESIAN_POINT ( 'NONE',  ( -1.974924404908016129, -2.653778228660402139, 0.1636761890514014939 ) ) ;
#6363=( BOUNDED_SURFACE ( )  B_SPLINE_SURFACE ( 3, 2, ( 
 ( #11746, #7025, #4447 ),
 ( #11568, #10403, #6778 ),
 ( #5685, #3511, #9152 ),
 ( #2314, #3200, #15257 ) ),
 .UNSPECIFIED., .F., .F., .T. ) 
 B_SPLINE_SURFACE_WITH_KNOTS ( ( 4, 4 ),
 ( 3, 3 ),
 ( 4.712388980384689674, 5.242505698888894727 ),
 ( 0.000000000000000000, 1.000000000000000000 ),
 .UNSPECIFIED. ) 
 GEOMETRIC_REPRESENTATION_ITEM ( )  RATIONAL_B_SPLINE_SURFACE ( (
 ( 1.000000000000000000, 0.7071067811865471286, 1.000000000000000000),
 ( 1.000000000000000000, 0.7085172298914497180, 1.000000000000000000),
 ( 1.000000000000000000, 0.7099209393058720785, 1.000000000000000000),
 ( 1.000000000000000000, 0.7111298678009152496, 1.000000000000000000) ) ) 
 REPRESENTATION_ITEM ( '' )  SURFACE ( )  );
#6376=CARTESIAN_POINT ( 'NONE',  ( -1.955316446157987276, -2.907727917705189125, 0.1149967193102930108 ) ) ;
#6379=CARTESIAN_POINT ( 'NONE',  ( -1.996857264586939129, -2.798601985277512139, -0.1754253142013137701 ) ) ;
#6386=AXIS2_PLACEMENT_3D ( 'NONE', #7240, #8419, #12184 ) ;
#6392=EDGE_LOOP ( 'NONE', ( #6662, #9729, #7516, #1811 ) ) ;
#6394=CARTESIAN_POINT ( 'NONE',  ( -1.399712685227380460, -0.02644324263748139281, -0.07874015748031495954 ) ) ;
#6403=CARTESIAN_POINT ( 'NONE',  ( -1.902069599514452536, -2.937971526065610295, -0.06318319403201104467 ) ) ;
#6406=DIRECTION ( 'NONE',  ( -0.8011800915434513781, 0.5984233124757313282, 0.000000000000000000 ) ) ;
#6418=DIRECTION ( 'NONE',  ( 1.000000000000000000, 1.040834085586083310E-14, 0.000000000000000000 ) ) ;
#6419=CIRCLE ( 'NONE', #5432, 0.01968503937007873988 ) ;
#6420=CARTESIAN_POINT ( 'NONE',  ( -0.06972667172716363881, -0.1870117487642863896, -0.03937007824553747509 ) ) ;
#6421=ORIENTED_EDGE ( 'NONE', *, *, #634, .F. ) ;
#6424=DIRECTION ( 'NONE',  ( 0.000000000000000000, 2.212657494868377674E-16, -1.000000000000000000 ) ) ;
#6431=CIRCLE ( 'NONE', #10192, 0.01968503937007873295 ) ;
#6437=DIRECTION ( 'NONE',  ( 0.9967194639908912857, -0.08093398607328357308, 0.000000000000000000 ) ) ;
#6438=CARTESIAN_POINT ( 'NONE',  ( -2.018751945719120755, -2.567790922178344371, 0.1539137670609011521 ) ) ;
#6459=CARTESIAN_POINT ( 'NONE',  ( -1.958647179939665639, -2.899418888633596314, 0.1240863880612434328 ) ) ;
#6464=CARTESIAN_POINT ( 'NONE',  ( -1.607606114292111199, 0.09732815221480034529, -0.08366141732283460808 ) ) ;
#6472=ORIENTED_EDGE ( 'NONE', *, *, #13721, .F. ) ;
#6475=CARTESIAN_POINT ( 'NONE',  ( -1.398371068895200908, -0.02596287309409977401, -0.07122367060404551087 ) ) ;
#6480=CYLINDRICAL_SURFACE ( 'NONE', #4606, 0.03937007874015751446 ) ;
#6481=EDGE_CURVE ( 'NONE', #880, #14915, #1909, .T. ) ;
#6485=CARTESIAN_POINT ( 'NONE',  ( -1.887622960209728307, -2.902805997487048373, -0.07702258022142625948 ) ) ;
#6488=CARTESIAN_POINT ( 'NONE',  ( -0.004690417658706399866, 0.1529805375610462648, -0.008482181431098845953 ) ) ;
#6499=CARTESIAN_POINT ( 'NONE',  ( -0.007502606504445189818, -0.1783918715466211447, 0.01493773385587683113 ) ) ;
#6501=DIRECTION ( 'NONE',  ( 1.000000000000000000, -0.000000000000000000, -0.000000000000000000 ) ) ;
#6502=EDGE_LOOP ( 'NONE', ( #3321, #13382, #10226, #13720 ) ) ;
#6521=CYLINDRICAL_SURFACE ( 'NONE', #596, 0.01968503937007871907 ) ;
#6522=CARTESIAN_POINT ( 'NONE',  ( -2.007604201720935677, -2.768319273907016154, 0.1776676917229350894 ) ) ;
#6526=CARTESIAN_POINT ( 'NONE',  ( -1.981870241362710061, -2.839422880978404784, -0.1645059300150371884 ) ) ;
#6529=CARTESIAN_POINT ( 'NONE',  ( -1.915493804681331680, -2.830794960306212360, 0.1437166327912214048 ) ) ;
#6534=VERTEX_POINT ( 'NONE', #13885 ) ;
#6550=EDGE_CURVE ( 'NONE', #12673, #14162, #664, .T. ) ;
#6562=CARTESIAN_POINT ( 'NONE',  ( -0.05916619364927751951, -0.1856756262235988719, -0.05712045715993030459 ) ) ;
#6564=VERTEX_POINT ( 'NONE', #5416 ) ;
#6569=CARTESIAN_POINT ( 'NONE',  ( -0.007978440472143270498, -0.1611588996411620900, 0.01594766689393424530 ) ) ;
#6570=DIRECTION ( 'NONE',  ( 0.000000000000000000, -0.000000000000000000, -1.000000000000000000 ) ) ;
#6581=CARTESIAN_POINT ( 'NONE',  ( -0.05639125304298477775, 0.1674615591801703607, -0.03403793048618272005 ) ) ;
#6582=CARTESIAN_POINT ( 'NONE',  ( -1.293236445124221312, 0.1355266887446167634, 0.05905511811023622659 ) ) ;
#6587=ORIENTED_EDGE ( 'NONE', *, *, #546, .F. ) ;
#6588=CARTESIAN_POINT ( 'NONE',  ( -2.169366242005652534, -2.077173998931358234, -0.09331536252806053866 ) ) ;
#6605=AXIS2_PLACEMENT_3D ( 'NONE', #12735, #4492, #15130 ) ;
#6608=CARTESIAN_POINT ( 'NONE',  ( -1.988607233356104009, -2.761830767068704784, -0.1772894973384211703 ) ) ;
#6612=CARTESIAN_POINT ( 'NONE',  ( -2.168820329264121494, -1.823085014281403682, -0.1033464566929124112 ) ) ;
#6613=CARTESIAN_POINT ( 'NONE',  ( -2.080682670864669515, -2.105520006804255218, -0.09620997013695481437 ) ) ;
#6618=ORIENTED_EDGE ( 'NONE', *, *, #15256, .F. ) ;
#6627=CARTESIAN_POINT ( 'NONE',  ( -2.010991777528384983, -2.758467574604075434, 0.1561691687464104861 ) ) ;
#6634=SPHERICAL_SURFACE ( 'NONE', #393, 0.01968503937007873988 ) ;
#6637=DIRECTION ( 'NONE',  ( -0.000000000000000000, 0.000000000000000000, 1.000000000000000000 ) ) ;
#6658=CARTESIAN_POINT ( 'NONE',  ( -0.03005672326763337773, -0.1816858507396494349, 0.01806077797202005480 ) ) ;
#6662=ORIENTED_EDGE ( 'NONE', *, *, #10181, .F. ) ;
#6664=ORIENTED_EDGE ( 'NONE', *, *, #14396, .T. ) ;
#6678=CARTESIAN_POINT ( 'NONE',  ( -1.568343923620152625, 0.1178486908565802016, -0.03937007874015747977 ) ) ;
#6679=AXIS2_PLACEMENT_3D ( 'NONE', #261, #2813, #13319 ) ;
#6681=CARTESIAN_POINT ( 'NONE',  ( -1.419615703680148000, -0.01226548409420230579, 0.08366141732283458032 ) ) ;
#6689=CARTESIAN_POINT ( 'NONE',  ( -2.003332662134895248, -2.780495179851753207, 0.1775193625598680269 ) ) ;
#6690=B_SPLINE_CURVE_WITH_KNOTS ( 'NONE', 3,
 ( #6209, #14694, #3953, #13500, #10921, #2766, #8730, #11149, #9987, #12102 ),
 .UNSPECIFIED., .F., .F.,
 ( 4, 2, 2, 2, 4 ),
 ( 0.000000000000000000, 0.0002149660118259327313, 0.0004299320236518654626, 0.0006448980354777981939, 0.0008598640473037309252 ),
 .UNSPECIFIED. ) ;
#6694=CARTESIAN_POINT ( 'NONE',  ( -1.972648348582522360, -2.863648286116795116, -0.1334986992619453527 ) ) ;
#6695=DIRECTION ( 'NONE',  ( -0.000000000000000000, -0.000000000000000000, -1.000000000000000000 ) ) ;
#6699=DIRECTION ( 'NONE',  ( -0.000000000000000000, -0.000000000000000000, -1.000000000000000000 ) ) ;
#6700=ORIENTED_EDGE ( 'NONE', *, *, #7283, .F. ) ;
#6704=VERTEX_POINT ( 'NONE', #9432 ) ;
#6714=CARTESIAN_POINT ( 'NONE',  ( -1.904013713778871963, -2.861285413342554040, -0.1538978722022966983 ) ) ;
#6717=CARTESIAN_POINT ( 'NONE',  ( -1.437672431148612429, -0.06355280397547365123, -0.08366141732283455257 ) ) ;
#6736=DIRECTION ( 'NONE',  ( -0.000000000000000000, 0.000000000000000000, 1.000000000000000000 ) ) ;
#6737=DIRECTION ( 'NONE',  ( -0.5005078764080090892, -0.7027276007401488389, 0.5056340423780217863 ) ) ;
#6738=EDGE_LOOP ( 'NONE', ( #15047, #5947, #12904, #3663 ) ) ;
#6741=ORIENTED_EDGE ( 'NONE', *, *, #8268, .T. ) ;
#6747=CARTESIAN_POINT ( 'NONE',  ( -0.01899774626693294735, 0.1736125314593147118, -0.03244910060854599987 ) ) ;
#6758=CARTESIAN_POINT ( 'NONE',  ( -1.431036756819010769, -0.02829858486107881405, -0.1033464566929133133 ) ) ;
#6771=CARTESIAN_POINT ( 'NONE',  ( -2.087354244661867142, -1.726823559470685332, -0.1037499983681600124 ) ) ;
#6778=CARTESIAN_POINT ( 'NONE',  ( -1.588286453767307593, 0.1240441066498496892, -0.03937007874189642903 ) ) ;
#6793=ADVANCED_FACE ( 'NONE', ( #13841 ), #13339, .T. ) ;
#6794=DIRECTION ( 'NONE',  ( 0.000000000000000000, -0.000000000000000000, -1.000000000000000000 ) ) ;
#6797=CARTESIAN_POINT ( 'NONE',  ( -1.978180062195354694, -2.794907819778010616, -0.1760901428592002160 ) ) ;
#6800=CARTESIAN_POINT ( 'NONE',  ( -1.431036756819011213, -0.02829858486107871343, 0.08366141732283458032 ) ) ;
#6811=ORIENTED_EDGE ( 'NONE', *, *, #4003, .T. ) ;
#6813=CARTESIAN_POINT ( 'NONE',  ( -0.01449560339480800153, 0.1719786949496021622, 3.288862647277781903E-16 ) ) ;
#6815=CARTESIAN_POINT ( 'NONE',  ( -0.008695292838831351900, 0.1754324108224426804, -0.01747077667449336777 ) ) ;
#6823=LINE ( 'NONE', #8256, #8414 ) ;
#6824=AXIS2_PLACEMENT_3D ( 'NONE', #5211, #10007, #12901 ) ;
#6841=DIRECTION ( 'NONE',  ( -1.000000000000000000, 0.000000000000000000, 0.000000000000000000 ) ) ;
#6843=LENGTH_MEASURE_WITH_UNIT ( LENGTH_MEASURE( 0.02539999999999999897 ), #3497 );
#6847=VECTOR ( 'NONE', #14798, 39.37007874015748143 ) ;
#6859=ORIENTED_EDGE ( 'NONE', *, *, #7400, .F. ) ;
#6864=DIRECTION ( 'NONE',  ( -0.000000000000000000, 0.000000000000000000, 1.000000000000000000 ) ) ;
#6866=AXIS2_PLACEMENT_3D ( 'NONE', #15044, #8779, #13548 ) ;
#6867=CARTESIAN_POINT ( 'NONE',  ( -0.07278938515218676131, 0.1649651754370965173, 0.05936614484719628104 ) ) ;
#6870=DIRECTION ( 'NONE',  ( -0.000000000000000000, -0.000000000000000000, -1.000000000000000000 ) ) ;
#6872=CARTESIAN_POINT ( 'NONE',  ( -1.904866376297139841, -2.858959339525115162, -0.1270709863631420411 ) ) ;
#6873=VERTEX_POINT ( 'NONE', #3116 ) ;
#6885=TOROIDAL_SURFACE ( 'NONE', #405, 0.05905511811023621271, 0.01968503937007873988 ) ;
#6886=CIRCLE ( 'NONE', #11392, 0.01968503937007875029 ) ;
#6889=CARTESIAN_POINT ( 'NONE',  ( -1.941383621697627682, -2.904153198872124975, -0.1189196622982612861 ) ) ;
#6897=CARTESIAN_POINT ( 'NONE',  ( -0.03749734052841491999, 0.1488898142811245495, 0.04795046931071418606 ) ) ;
#6906=ORIENTED_EDGE ( 'NONE', *, *, #14219, .T. ) ;
#6913=FACE_OUTER_BOUND ( 'NONE', #6392, .T. ) ;
#6925=EDGE_CURVE ( 'NONE', #5035, #7635, #15182, .T. ) ;
#6933=CARTESIAN_POINT ( 'NONE',  ( -1.898417150026649125, -2.948016320718355399, -0.02360795789488797508 ) ) ;
#6937=ADVANCED_FACE ( 'NONE', ( #930 ), #6363, .T. ) ;
#6942=EDGE_CURVE ( 'NONE', #14238, #14453, #3833, .T. ) ;
#6948=VERTEX_POINT ( 'NONE', #9232 ) ;
#6956=CARTESIAN_POINT ( 'NONE',  ( -0.04751022371102618658, 0.1688405673728185230, 0.05319490010182049977 ) ) ;
#6965=ORIENTED_EDGE ( 'NONE', *, *, #11441, .F. ) ;
#6966=EDGE_LOOP ( 'NONE', ( #3918, #12180, #6965 ) ) ;
#6970=ADVANCED_FACE ( 'NONE', ( #9387 ), #14167, .F. ) ;
#6974=CARTESIAN_POINT ( 'NONE',  ( -1.970940144590390908, -2.817289869702642946, -0.1717442269998073201 ) ) ;
#6976=CARTESIAN_POINT ( 'NONE',  ( -1.185322244937984104, 0.3350014259194302180, -0.05695314934227149739 ) ) ;
#6978=CARTESIAN_POINT ( 'NONE',  ( -2.182693454834259139, -1.630005269948474389, 0.08366141732283424726 ) ) ;
#6979=( BOUNDED_SURFACE ( )  B_SPLINE_SURFACE ( 3, 2, ( 
 ( #11272, #2977, #14884 ),
 ( #11106, #399, #7672 ),
 ( #544, #3996, #6243 ),
 ( #8701, #485, #13783 ),
 ( #8842, #7815, #9960 ),
 ( #5387, #2892, #13621 ) ),
 .UNSPECIFIED., .F., .F., .T. ) 
 B_SPLINE_SURFACE_WITH_KNOTS ( ( 4, 2, 4 ),
 ( 3, 3 ),
 ( 0.000000000000000000, 0.01443577820670504351, 0.02887155641341008702 ),
 ( 0.000000000000000000, 1.000000000000000000 ),
 .UNSPECIFIED. ) 
 GEOMETRIC_REPRESENTATION_ITEM ( )  RATIONAL_B_SPLINE_SURFACE ( (
 ( 1.000000000000000000, 0.7071067811865425767, 1.000000000000000000),
 ( 1.000000000000000000, 0.7073403273941961666, 1.000000000000000000),
 ( 1.000000000000000000, 0.7061401876396929955, 1.000000000000000000),
 ( 1.000000000000000000, 0.7010830952601875277, 1.000000000000000000),
 ( 1.000000000000000000, 0.6972252234842747365, 1.000000000000000000),
 ( 1.000000000000000000, 0.6921057963906817045, 1.000000000000000000) ) ) 
 REPRESENTATION_ITEM ( '' )  SURFACE ( )  );
#6992=CARTESIAN_POINT ( 'NONE',  ( -0.03967601873944331947, 0.1701129415451921312, -0.04931034005880049337 ) ) ;
#7004=VERTEX_POINT ( 'NONE', #7257 ) ;
#7015=CARTESIAN_POINT ( 'NONE',  ( -0.07874015748031501505, 0.1442356988431299225, -0.03937007874015747977 ) ) ;
#7019=ORIENTED_EDGE ( 'NONE', *, *, #13615, .T. ) ;
#7025=CARTESIAN_POINT ( 'NONE',  ( -1.584115185264708403, 0.1296286773226378863, -0.05905511811023624047 ) ) ;
#7027=EDGE_CURVE ( 'NONE', #13379, #3964, #15361, .T. ) ;
#7028=FACE_OUTER_BOUND ( 'NONE', #14020, .T. ) ;
#7039=DIRECTION ( 'NONE',  ( 1.000000000000000000, -0.000000000000000000, -0.000000000000000000 ) ) ;
#7040=FACE_OUTER_BOUND ( 'NONE', #1049, .T. ) ;
#7042=EDGE_CURVE ( 'NONE', #9959, #13232, #10605, .T. ) ;
#7047=CYLINDRICAL_SURFACE ( 'NONE', #2921, 0.2362204724409451007 ) ;
#7059=CARTESIAN_POINT ( 'NONE',  ( -1.607347794336916103, 0.09769578488571013797, -0.07191154586943661331 ) ) ;
#7063=ORIENTED_EDGE ( 'NONE', *, *, #4526, .F. ) ;
#7072=ORIENTED_EDGE ( 'NONE', *, *, #128, .F. ) ;
#7074=CARTESIAN_POINT ( 'NONE',  ( -2.090051324975654268, -1.858423098537180129, 0.08664193191037310171 ) ) ;
#7075=CIRCLE ( 'NONE', #2318, 0.01968503937007875723 ) ;
#7078=CARTESIAN_POINT ( 'NONE',  ( -1.932774803826795784, -2.849358176375062612, 0.1599454478317489103 ) ) ;
#7080=CARTESIAN_POINT ( 'NONE',  ( -1.607606114292110977, 0.09732815221480034529, 0.08366141732283462196 ) ) ;
#7087=EDGE_CURVE ( 'NONE', #14162, #5049, #3509, .T. ) ;
#7095=DIRECTION ( 'NONE',  ( 1.224646799147353207E-16, 1.000000000000000000, 0.000000000000000000 ) ) ;
#7097=VECTOR ( 'NONE', #12743, 39.37007874015748143 ) ;
#7098=CARTESIAN_POINT ( 'NONE',  ( -0.007954450877556133725, 0.1525563742223925434, 0.01590295032064549530 ) ) ;
#7099=CARTESIAN_POINT ( 'NONE',  ( -1.568343923620152180, 0.1178486908565801600, -0.05905511811023622659 ) ) ;
#7114=EDGE_CURVE ( 'NONE', #1873, #7239, #12848, .T. ) ;
#7116=CIRCLE ( 'NONE', #13875, 0.01968503937007871907 ) ;
#7119=CARTESIAN_POINT ( 'NONE',  ( -1.950386452976718976, -2.919842877483835419, -0.07215111381683911307 ) ) ;
#7121=CARTESIAN_POINT ( 'NONE',  ( -2.464375602680784816, 0.7077922088437120784, -0.1033464566929134798 ) ) ;
#7125=CARTESIAN_POINT ( 'NONE',  ( -1.964126537190518107, -2.749515453455440905, 0.1756903148397124803 ) ) ;
#7126=AXIS2_PLACEMENT_3D ( 'NONE', #13863, #6794, #5772 ) ;
#7128=CARTESIAN_POINT ( 'NONE',  ( -1.948440798307840227, -2.924613150232347802, -0.06209002033771690576 ) ) ;
#7130=AXIS2_PLACEMENT_3D ( 'NONE', #10314, #10638, #15424 ) ;
#7144=ADVANCED_FACE ( 'NONE', ( #2949 ), #519, .F. ) ;
#7148=DIRECTION ( 'NONE',  ( -0.000000000000000000, -0.000000000000000000, -1.000000000000000000 ) ) ;
#7158=ORIENTED_EDGE ( 'NONE', *, *, #10934, .T. ) ;
#7159=ORIENTED_EDGE ( 'NONE', *, *, #11600, .F. ) ;
#7163=ORIENTED_EDGE ( 'NONE', *, *, #11563, .F. ) ;
#7171=CARTESIAN_POINT ( 'NONE',  ( -1.107198012490790306, -0.06846922848666056605, 0.03937007874015747977 ) ) ;
#7173=DIRECTION ( 'NONE',  ( -1.000000000000000000, 0.000000000000000000, -8.673617379884028570E-16 ) ) ;
#7181=CIRCLE ( 'NONE', #9185, 0.01968503937007880233 ) ;
#7188=DIRECTION ( 'NONE',  ( 0.7402970580929162381, 0.6722799013647318134, -1.027368548696278368E-14 ) ) ;
#7192=DIRECTION ( 'NONE',  ( -0.000000000000000000, 0.000000000000000000, 1.000000000000000000 ) ) ;
#7196=AXIS2_PLACEMENT_3D ( 'NONE', #10519, #13093, #11943 ) ;
#7204=LINE ( 'NONE', #1321, #11402 ) ;
#7209=CARTESIAN_POINT ( 'NONE',  ( -1.253866366384063902, 0.1355266887446167634, 0.05905511811023622659 ) ) ;
#7212=ORIENTED_EDGE ( 'NONE', *, *, #13174, .T. ) ;
#7213=CARTESIAN_POINT ( 'NONE',  ( -1.983894532046819537, -2.833993371773555037, 0.1480485534673108006 ) ) ;
#7220=FACE_OUTER_BOUND ( 'NONE', #4498, .T. ) ;
#7221=ADVANCED_FACE ( 'NONE', ( #5202 ), #6521, .T. ) ;
#7228=CARTESIAN_POINT ( 'NONE',  ( -1.437672431148612429, -0.06355280397547365123, 0.08366141732283458032 ) ) ;
#7230=ORIENTED_EDGE ( 'NONE', *, *, #8495, .T. ) ;
#7231=CARTESIAN_POINT ( 'NONE',  ( -0.08151194962748883888, 0.1637246173173400876, 0.03937007874015747977 ) ) ;
#7234=CARTESIAN_POINT ( 'NONE',  ( -0.04489327544264908737, -0.1650454269528150719, 0.05194604157257243227 ) ) ;
#7239=VERTEX_POINT ( 'NONE', #681 ) ;
#7240=CARTESIAN_POINT ( 'NONE',  ( -1.591501945092674175, 0.08600752902535276079, 0.08366141732283462196 ) ) ;
#7242=CARTESIAN_POINT ( 'NONE',  ( -1.904663734566028888, -2.930783973356453576, -0.08012620074318213548 ) ) ;
#7255=ORIENTED_EDGE ( 'NONE', *, *, #3073, .F. ) ;
#7256=B_SPLINE_CURVE_WITH_KNOTS ( 'NONE', 3,
 ( #12078, #2289, #3479, #15467, #14514, #8254 ),
 .UNSPECIFIED., .F., .F.,
 ( 4, 2, 4 ),
 ( 2.168404344971008868E-19, 0.0003906568843879350858, 0.0007813137687758699547 ),
 .UNSPECIFIED. ) ;
#7257=CARTESIAN_POINT ( 'NONE',  ( -1.431036756819010769, -0.02829858486107867874, 0.1033464566929133133 ) ) ;
#7270=CARTESIAN_POINT ( 'NONE',  ( -1.593720380426979499, 0.1169877005562640487, 0.06604764719690611741 ) ) ;
#7272=CARTESIAN_POINT ( 'NONE',  ( -1.591501945092674175, 0.08600752902535263589, 0.08366141732283462196 ) ) ;
#7275=CARTESIAN_POINT ( 'NONE',  ( -1.904045375254802996, -2.861202609515447026, 0.1539435876055646746 ) ) ;
#7277=CARTESIAN_POINT ( 'NONE',  ( -1.983904060594682051, -2.833967658977468052, -0.1480566138544802401 ) ) ;
#7280=VERTEX_POINT ( 'NONE', #9931 ) ;
#7283=EDGE_CURVE ( 'NONE', #14180, #15344, #101, .T. ) ;
#7300=ORIENTED_EDGE ( 'NONE', *, *, #10025, .T. ) ;
#7303=ORIENTED_EDGE ( 'NONE', *, *, #3634, .T. ) ;
#7305=CARTESIAN_POINT ( 'NONE',  ( -0.07635964791965738074, -0.1878198040935885327, -0.03937007874015747977 ) ) ;
#7310=CARTESIAN_POINT ( 'NONE',  ( -1.527714331928839098, 0.2380340132385416752, -0.05905511811023622659 ) ) ;
#7311=DIRECTION ( 'NONE',  ( -0.000000000000000000, 0.000000000000000000, 1.000000000000000000 ) ) ;
#7313=CARTESIAN_POINT ( 'NONE',  ( -1.957251767099916107, -2.772329397582958599, 0.1771653543307079026 ) ) ;
#7345=CARTESIAN_POINT ( 'NONE',  ( -1.913759217590492057, -2.905162717098710434, 0.1179150947973677116 ) ) ;
#7351=DIRECTION ( 'NONE',  ( -1.000000000000000000, 1.349229370204184172E-15, 0.000000000000000000 ) ) ;
#7358=ORIENTED_EDGE ( 'NONE', *, *, #15293, .F. ) ;
#7360=CIRCLE ( 'NONE', #1374, 0.01968503937007870172 ) ;
#7371=LINE ( 'NONE', #4076, #1851 ) ;
#7380=( BOUNDED_SURFACE ( )  B_SPLINE_SURFACE ( 3, 2, ( 
 ( #12276, #3025, #11313 ),
 ( #6608, #1702, #7549 ),
 ( #11248, #12342, #1619 ),
 ( #13452, #6379, #5273 ),
 ( #13686, #11407, #11170 ),
 ( #524, #10067, #14851 ),
 ( #10236, #8909, #12512 ),
 ( #1770, #6526, #5355 ),
 ( #8988, #7791, #12579 ),
 ( #2720, #10522, #6694 ),
 ( #12667, #11712, #3097 ),
 ( #7877, #5726, #1929 ),
 ( #978, #4268, #9055 ),
 ( #13825, #13582, #12 ),
 ( #4034, #9557, #2337 ),
 ( #5941, #5127, #10065 ),
 ( #10730, #520, #7119 ),
 ( #8376, #12206, #2855 ),
 ( #14328, #3598, #1470 ),
 ( #11245, #11009, #7641 ),
 ( #4771, #1532, #8809 ),
 ( #3889, #11166, #290 ),
 ( #457, #7546, #14779 ),
 ( #13161, #5269, #365 ),
 ( #12432, #3525, #5040 ),
 ( #2636, #8295, #7408 ),
 ( #11918, #9932, #13070 ),
 ( #1186, #6220, #9841 ),
 ( #14621, #8670, #14711 ),
 ( #13448, #2715, #5203 ),
 ( #13514, #7485, #12340 ),
 ( #12273, #6284, #11077 ),
 ( #3971, #8744, #2776 ),
 ( #1612, #6376, #9998 ),
 ( #1697, #6459, #8026 ),
 ( #5349, #12664, #15016 ),
 ( #11309, #5511, #4112 ),
 ( #11488, #13758, #4336 ),
 ( #3022, #1927, #5669 ),
 ( #12509, #14848, #591 ),
 ( #10297, #13991, #682 ),
 ( #8986, #10154, #4263 ),
 ( #5440, #10234, #11404 ),
 ( #15079, #6689, #3094 ),
 ( #7787, #6522, #14941 ),
 ( #9053, #4196, #5583 ) ),
 .UNSPECIFIED., .F., .F., .T. ) 
 B_SPLINE_SURFACE_WITH_KNOTS ( ( 4, 2, 2, 2, 2, 2, 2, 2, 2, 2, 2, 2, 2, 2, 2, 2, 2, 2, 2, 2, 2, 2, 4 ),
 ( 3, 3 ),
 ( 0.000000000000000000, 0.0008763647898916152512, 0.001314547184837422823, 0.001752729579783230502, 0.002629094369674845645, 0.003505459159566461005, 0.004381823949458076364, 0.004820006344403883827, 0.005258188739349691290, 0.005696371134295498753, 0.006134553529241306216, 0.007010918319132922009, 0.007449100714078730340, 0.007887283109024537803, 0.008325465503970345266, 0.008763647898916152729, 0.009640012688807767655, 0.01051637747869938258, 0.01139274226859099751, 0.01226910705848261243, 0.01270728945342841990, 0.01314547184837422736, 0.01402183663826584402 ),
 ( 0.000000000000000000, 1.000000000000000000 ),
 .UNSPECIFIED. ) 
 GEOMETRIC_REPRESENTATION_ITEM ( )  RATIONAL_B_SPLINE_SURFACE ( (
 ( 1.000000000000000000, 0.6921057963906867005, 1.000000000000000000),
 ( 1.000000000000000000, 0.7001301295292068350, 1.000000000000000000),
 ( 1.000000000000000000, 0.7082232347829966468, 1.000000000000000000),
 ( 1.000000000000000000, 0.7204448971599605178, 1.000000000000000000),
 ( 1.000000000000000000, 0.7245324354207898221, 1.000000000000000000),
 ( 1.000000000000000000, 0.7327308554584663902, 1.000000000000000000),
 ( 1.000000000000000000, 0.7368541771550430886, 1.000000000000000000),
 ( 1.000000000000000000, 0.7489861883972682710, 1.000000000000000000),
 ( 1.000000000000000000, 0.7568423250379210376, 1.000000000000000000),
 ( 1.000000000000000000, 0.7720372848817829148, 1.000000000000000000),
 ( 1.000000000000000000, 0.7794153764102734749, 1.000000000000000000),
 ( 1.000000000000000000, 0.7929014218043154427, 1.000000000000000000),
 ( 1.000000000000000000, 0.7990977153083722584, 1.000000000000000000),
 ( 1.000000000000000000, 0.8074742350527349677, 1.000000000000000000),
 ( 1.000000000000000000, 0.8101059552811848974, 1.000000000000000000),
 ( 1.000000000000000000, 0.8149080692666150760, 1.000000000000000000),
 ( 1.000000000000000000, 0.8170977687249663113, 1.000000000000000000),
 ( 1.000000000000000000, 0.8210473395081507864, 1.000000000000000000),
 ( 1.000000000000000000, 0.8228072785942259770, 1.000000000000000000),
 ( 1.000000000000000000, 0.8258753710949300331, 1.000000000000000000),
 ( 1.000000000000000000, 0.8271879151802322694, 1.000000000000000000),
 ( 1.000000000000000000, 0.8303186452218207503, 1.000000000000000000),
 ( 1.000000000000000000, 0.8313781188583296844, 1.000000000000000000),
 ( 1.000000000000000000, 0.8314027137259931699, 1.000000000000000000),
 ( 1.000000000000000000, 0.8311425143793390591, 1.000000000000000000),
 ( 1.000000000000000000, 0.8301013997591458748, 1.000000000000000000),
 ( 1.000000000000000000, 0.8293235644851727484, 1.000000000000000000),
 ( 1.000000000000000000, 0.8272694230054146169, 1.000000000000000000),
 ( 1.000000000000000000, 0.8259930828080271903, 1.000000000000000000),
 ( 1.000000000000000000, 0.8229409194359517121, 1.000000000000000000),
 ( 1.000000000000000000, 0.8211588682283366136, 1.000000000000000000),
 ( 1.000000000000000000, 0.8152102375193999162, 1.000000000000000000),
 ( 1.000000000000000000, 0.8104135904785896294, 1.000000000000000000),
 ( 1.000000000000000000, 0.7992487876031277860, 1.000000000000000000),
 ( 1.000000000000000000, 0.7929817278871067465, 1.000000000000000000),
 ( 1.000000000000000000, 0.7794714393159598576, 1.000000000000000000),
 ( 1.000000000000000000, 0.7721045825237821125, 1.000000000000000000),
 ( 1.000000000000000000, 0.7568758627708697118, 1.000000000000000000),
 ( 1.000000000000000000, 0.7490040357394209813, 1.000000000000000000),
 ( 1.000000000000000000, 0.7368512664891039288, 1.000000000000000000),
 ( 1.000000000000000000, 0.7327258982120725683, 1.000000000000000000),
 ( 1.000000000000000000, 0.7245321423272259587, 1.000000000000000000),
 ( 1.000000000000000000, 0.7204462382506620077, 1.000000000000000000),
 ( 1.000000000000000000, 0.7082274559817631765, 1.000000000000000000),
 ( 1.000000000000000000, 0.7001335831284237754, 1.000000000000000000),
 ( 1.000000000000000000, 0.6921057963906867005, 1.000000000000000000) ) ) 
 REPRESENTATION_ITEM ( '' )  SURFACE ( )  );
#7393=ADVANCED_FACE ( 'NONE', ( #10379 ), #909, .F. ) ;
#7394=CARTESIAN_POINT ( 'NONE',  ( -2.183651372152203507, -1.661851685721189353, 0.08366141732283367827 ) ) ;
#7400=EDGE_CURVE ( 'NONE', #6320, #9296, #9214, .T. ) ;
#7408=CARTESIAN_POINT ( 'NONE',  ( -1.943857306512870142, -2.935761365336657214, 0.02290380726543173040 ) ) ;
#7418=CARTESIAN_POINT ( 'NONE',  ( 0.7052242655755273093, -1.858423098537180129, 0.08366141732283417787 ) ) ;
#7426=ORIENTED_EDGE ( 'NONE', *, *, #12561, .F. ) ;
#7427=DIRECTION ( 'NONE',  ( 0.8144815189573203495, -0.5801894994542524664, 0.000000000000000000 ) ) ;
#7432=CARTESIAN_POINT ( 'NONE',  ( -2.188531697382432029, -1.824100413744500049, 0.08366141732873445813 ) ) ;
#7434=CARTESIAN_POINT ( 'NONE',  ( -1.884762920069399161, -2.909869073764713487, 0.06183202482754375506 ) ) ;
#7435=ORIENTED_EDGE ( 'NONE', *, *, #2152, .F. ) ;
#7436=CARTESIAN_POINT ( 'NONE',  ( -1.972696907342682326, -2.863522232956755786, 0.1335784024945382287 ) ) ;
#7445=ADVANCED_FACE ( 'NONE', ( #4501 ), #7846, .T. ) ;
#7450=CARTESIAN_POINT ( 'NONE',  ( -1.293236445124221312, 0.1355266887446167634, -0.03937007874015747977 ) ) ;
#7453=CARTESIAN_POINT ( 'NONE',  ( -0.01755170026722350021, -0.1621998028774611911, -0.03064271692327978289 ) ) ;
#7468=CARTESIAN_POINT ( 'NONE',  ( -2.116007383176099044, -1.821120273082415641, 0.1033464566929129524 ) ) ;
#7471=CARTESIAN_POINT ( 'NONE',  ( -1.574484809660005480, 0.1100025355994808662, -0.06175692796176408816 ) ) ;
#7476=( BOUNDED_SURFACE ( )  B_SPLINE_SURFACE ( 3, 2, ( 
 ( #8914, #9145, #2005 ),
 ( #15083, #5517, #13766 ),
 ( #3030, #10240, #5592 ),
 ( #11493, #12671, #6613 ),
 ( #3105, #4347, #12749 ),
 ( #602, #12583, #1850 ),
 ( #7729, #1776, #11318 ),
 ( #3189, #6771, #1935 ),
 ( #11561, #7796, #10072 ),
 ( #10392, #4273, #4437 ) ),
 .UNSPECIFIED., .F., .F., .T. ) 
 B_SPLINE_SURFACE_WITH_KNOTS ( ( 4, 2, 2, 2, 4 ),
 ( 3, 3 ),
 ( -1.040834085586084257E-17, 0.01438982281936204699, 0.02158473422904307742, 0.02518218993388358917, 0.02877964563872410439 ),
 ( 0.000000000000000000, 1.000000000000000000 ),
 .UNSPECIFIED. ) 
 GEOMETRIC_REPRESENTATION_ITEM ( )  RATIONAL_B_SPLINE_SURFACE ( (
 ( 1.000000000000000000, 0.7214151048183972126, 1.000000000000000000),
 ( 1.000000000000000000, 0.7162796536165754180, 1.000000000000000000),
 ( 1.000000000000000000, 0.7123718545348233233, 1.000000000000000000),
 ( 1.000000000000000000, 0.7086903259631885943, 1.000000000000000000),
 ( 1.000000000000000000, 0.7078262380797001319, 1.000000000000000000),
 ( 1.000000000000000000, 0.7071130014577271528, 1.000000000000000000),
 ( 1.000000000000000000, 0.7069727248725110602, 1.000000000000000000),
 ( 1.000000000000000000, 0.7068914992104640138, 1.000000000000000000),
 ( 1.000000000000000000, 0.7069499230734396233, 1.000000000000000000),
 ( 1.000000000000000000, 0.7071067811865475727, 1.000000000000000000) ) ) 
 REPRESENTATION_ITEM ( '' )  SURFACE ( )  );
#7481=ADVANCED_FACE ( 'NONE', ( #14529 ), #9590, .T. ) ;
#7485=CARTESIAN_POINT ( 'NONE',  ( -1.943645325779189470, -2.936341075933833977, 0.06731275603298569887 ) ) ;
#7486=DIRECTION ( 'NONE',  ( -0.03006568382583901106, -0.9995479251422039191, 0.000000000000000000 ) ) ;
#7491=CARTESIAN_POINT ( 'NONE',  ( -1.887573697862731770, -2.902928153145550638, -0.07679814701984788439 ) ) ;
#7498=EDGE_CURVE ( 'NONE', #13738, #924, #12612, .T. ) ;
#7506=DIRECTION ( 'NONE',  ( 0.5801894994542512451, 0.8144815189573213488, 0.000000000000000000 ) ) ;
#7507=CARTESIAN_POINT ( 'NONE',  ( -1.992382107315058271, -2.749515453455440905, 0.1756903148397124803 ) ) ;
#7509=CARTESIAN_POINT ( 'NONE',  ( -1.898906488563334882, -2.946676766132140468, -0.03212724755967235474 ) ) ;
#7511=CARTESIAN_POINT ( 'NONE',  ( -1.419615703680148000, -0.01226548409420232313, 0.07874015748031495954 ) ) ;
#7512=CARTESIAN_POINT ( 'NONE',  ( -1.588298999900524366, 0.1240273096569512873, 0.05983744915181773982 ) ) ;
#7513=CARTESIAN_POINT ( 'NONE',  ( -1.419024763034335335, -0.01190114260487083048, -0.07304054665220574560 ) ) ;
#7515=ORIENTED_EDGE ( 'NONE', *, *, #2244, .T. ) ;
#7516=ORIENTED_EDGE ( 'NONE', *, *, #11462, .T. ) ;
#7519=DIRECTION ( 'NONE',  ( 0.000000000000000000, -0.000000000000000000, -1.000000000000000000 ) ) ;
#7523=ORIENTED_EDGE ( 'NONE', *, *, #5135, .T. ) ;
#7533=CARTESIAN_POINT ( 'NONE',  ( -2.011286886001135255, -2.518997274786896945, 0.1294465814784910018 ) ) ;
#7537=CARTESIAN_POINT ( 'NONE',  ( -1.293236445124221312, 0.1355266887446167634, 0.03937007874015747977 ) ) ;
#7543=EDGE_LOOP ( 'NONE', ( #7303, #10395, #13424, #8293 ) ) ;
#7546=CARTESIAN_POINT ( 'NONE',  ( -1.938182383310145918, -2.949473540663261950, -0.01292403952254523800 ) ) ;
#7549=CARTESIAN_POINT ( 'NONE',  ( -2.007193303979263543, -2.769482957687897873, -0.1575906666632094777 ) ) ;
#7552=EDGE_CURVE ( 'NONE', #15252, #6320, #3100, .T. ) ;
#7556=ORIENTED_EDGE ( 'NONE', *, *, #11600, .T. ) ;
#7558=ORIENTED_EDGE ( 'NONE', *, *, #422, .T. ) ;
#7560=EDGE_LOOP ( 'NONE', ( #5901, #5265, #11160, #254 ) ) ;
#7562=CARTESIAN_POINT ( 'NONE',  ( -1.417802900492933782, -0.04287136159519128187, -0.07874015748031495954 ) ) ;
#7565=AXIS2_PLACEMENT_3D ( 'NONE', #14248, #2096, #8283 ) ;
#7570=CARTESIAN_POINT ( 'NONE',  ( -1.185456167500018365, 0.3350708678533356188, 0.05695194461341470532 ) ) ;
#7571=CARTESIAN_POINT ( 'NONE',  ( -1.869830193481172520, -2.946302503418662511, -0.03424462898272506023 ) ) ;
#7575=FACE_OUTER_BOUND ( 'NONE', #7543, .T. ) ;
#7576=DIRECTION ( 'NONE',  ( 0.000000000000000000, 0.000000000000000000, -1.000000000000000000 ) ) ;
#7584=CIRCLE ( 'NONE', #11603, 0.05905511811023627516 ) ;
#7592=CARTESIAN_POINT ( 'NONE',  ( -0.06145017734370220031, -0.1666692956086705812, -0.05763041683086380512 ) ) ;
#7596=AXIS2_PLACEMENT_3D ( 'NONE', #9968, #8625, #10032 ) ;
#7601=CARTESIAN_POINT ( 'NONE',  ( -1.412372674844927456, -0.03807050201945849643, 0.05475977885638705356 ) ) ;
#7609=CIRCLE ( 'NONE', #12376, 0.01968503937007880233 ) ;
#7613=ADVANCED_FACE ( 'NONE', ( #2696 ), #7984, .T. ) ;
#7617=CARTESIAN_POINT ( 'NONE',  ( -1.107198012490790529, -0.06846922848666055217, -0.03937007874015747977 ) ) ;
#7628=DIRECTION ( 'NONE',  ( 0.3235667741753642801, -0.9383274424966858707, 0.1218447918762963489 ) ) ;
#7635=VERTEX_POINT ( 'NONE', #7617 ) ;
#7639=AXIS2_PLACEMENT_3D ( 'NONE', #3721, #8496, #13269 ) ;
#7641=CARTESIAN_POINT ( 'NONE',  ( -1.945984862809333915, -2.930601869584705366, -0.04578774291266937690 ) ) ;
#7643=B_SPLINE_CURVE_WITH_KNOTS ( 'NONE', 3,
 ( #12279, #2956, #5046, #14635, #3897, #1539, #6529, #296, #5276, #3978, #8677, #14718, #2865, #11252, #13455, #11084, #8751, #525, #374, #10366, #10070, #9940, #2723, #2642, #11316, #7491, #6290, #13690, #8912, #14855, #4121, #465, #13520, #8587, #2781, #8815, #7726, #7648 ),
 .UNSPECIFIED., .F., .F.,
 ( 4, 2, 2, 2, 2, 2, 2, 2, 2, 2, 2, 2, 2, 2, 2, 2, 2, 2, 4 ),
 ( 0.000000000000000000, 0.0008718204131946265560, 0.001743640826389253112, 0.002615461239583880427, 0.003487281652778507959, 0.004359102065973135924, 0.005230922479167762588, 0.005666832685765068114, 0.006102742892362373640, 0.006974563305556972549, 0.007410473512154272004, 0.007846383718751572325, 0.008718204131946159091, 0.009590024545140745857, 0.01046184495833533436, 0.01133366537152992286, 0.01220548578472450962, 0.01307730619791909812, 0.01394912661111368489 ),
 .UNSPECIFIED. ) ;
#7648=CARTESIAN_POINT ( 'NONE',  ( -1.945459748359985142, -2.745801194614594820, -0.1561691687464109024 ) ) ;
#7649=FACE_OUTER_BOUND ( 'NONE', #11822, .T. ) ;
#7652=AXIS2_PLACEMENT_3D ( 'NONE', #7418, #12217, #12281 ) ;
#7660=CARTESIAN_POINT ( 'NONE',  ( -1.387704745771440429, -0.02010536753476140082, -0.05905511811023623353 ) ) ;
#7663=CIRCLE ( 'NONE', #9927, 0.01968503937007868437 ) ;
#7664=CARTESIAN_POINT ( 'NONE',  ( -2.184126211765464287, -1.725292181286280258, -0.08417626406393655114 ) ) ;
#7667=DIRECTION ( 'NONE',  ( 1.000000000000000000, -8.673617379884032514E-16, 0.000000000000000000 ) ) ;
#7670=CARTESIAN_POINT ( 'NONE',  ( -1.869182993986379326, -2.947846950676647371, 0.02785115562066423078 ) ) ;
#7672=CARTESIAN_POINT ( 'NONE',  ( -2.188531697382454677, -1.824100413745272764, -0.08366141732860882252 ) ) ;
#7674=ORIENTED_EDGE ( 'NONE', *, *, #3893, .F. ) ;
#7676=AXIS2_PLACEMENT_3D ( 'NONE', #5174, #6501, #13879 ) ;
#7678=EDGE_LOOP ( 'NONE', ( #6906, #13699, #2232, #1486, #9230 ) ) ;
#7680=ADVANCED_FACE ( 'NONE', ( #14829 ), #5865, .T. ) ;
#7681=AXIS2_PLACEMENT_3D ( 'NONE', #10750, #7148, #9572 ) ;
#7686=AXIS2_PLACEMENT_3D ( 'NONE', #9544, #6286, #12122 ) ;
#7696=EDGE_LOOP ( 'NONE', ( #7780, #2729, #5143, #12318 ) ) ;
#7697=ADVANCED_FACE ( 'NONE', ( #14998 ), #3069, .F. ) ;
#7706=DIRECTION ( 'NONE',  ( 0.000000000000000000, 2.212657494868377674E-16, -1.000000000000000000 ) ) ;
#7717=ORIENTED_EDGE ( 'NONE', *, *, #7798, .F. ) ;
#7726=CARTESIAN_POINT ( 'NONE',  ( -1.941800925136052181, -2.756730452697893963, -0.1575983618999967639 ) ) ;
#7729=CARTESIAN_POINT ( 'NONE',  ( -2.109904382371071918, -1.821337472029024074, -0.1053091407001082030 ) ) ;
#7735=FACE_OUTER_BOUND ( 'NONE', #12591, .T. ) ;
#7736=DIRECTION ( 'NONE',  ( 0.000000000000000000, 2.212657494868377674E-16, -1.000000000000000000 ) ) ;
#7743=CARTESIAN_POINT ( 'NONE',  ( -1.898002436973827756, -2.949150955976388211, -0.01280807431238822208 ) ) ;
#7745=CARTESIAN_POINT ( 'NONE',  ( -1.276200637803905691, -0.1988000726501942539, 0.08366141732283455257 ) ) ;
#7752=DIRECTION ( 'NONE',  ( 1.000000000000000000, 0.000000000000000000, 0.000000000000000000 ) ) ;
#7753=CARTESIAN_POINT ( 'NONE',  ( -1.100415514366347880, -0.04998955061626794705, -0.03937007874015747977 ) ) ;
#7757=EDGE_CURVE ( 'NONE', #11758, #8061, #14117, .T. ) ;
#7760=CARTESIAN_POINT ( 'NONE',  ( -0.004184981454872216226, -0.1778800751599175500, 0.007038468095566932821 ) ) ;
#7769=CARTESIAN_POINT ( 'NONE',  ( -0.06867854503139178557, 0.1655849054964023959, -0.03830121270948787238 ) ) ;
#7772=CARTESIAN_POINT ( 'NONE',  ( -1.100415514366371861, -0.04998955061625905139, -0.03937007874015747977 ) ) ;
#7776=CARTESIAN_POINT ( 'NONE',  ( -1.332606523864378945, 0.1355266887446167634, 0.03937007874015747977 ) ) ;
#7780=ORIENTED_EDGE ( 'NONE', *, *, #11119, .T. ) ;
#7782=CARTESIAN_POINT ( 'NONE',  ( 0.7052242655755273093, -1.858423098537180129, -0.08366141732283417787 ) ) ;
#7786=CARTESIAN_POINT ( 'NONE',  ( -1.398495881576244493, -0.02731002314121873387, 0.1968503937007874127 ) ) ;
#7787=CARTESIAN_POINT ( 'NONE',  ( -1.988605610277403679, -2.761836062270417447, 0.1772901849371437688 ) ) ;
#7791=CARTESIAN_POINT ( 'NONE',  ( -1.977730146514584009, -2.850383346250469518, -0.1596058012727677722 ) ) ;
#7796=CARTESIAN_POINT ( 'NONE',  ( -2.084722658870310941, -1.679497184253527120, -0.1033551916919345920 ) ) ;
#7798=EDGE_CURVE ( 'NONE', #13695, #9820, #122, .T. ) ;
#7808=CARTESIAN_POINT ( 'NONE',  ( -2.184126211765463399, -1.902526540362047491, 0.08609155816397294492 ) ) ;
#7814=ORIENTED_EDGE ( 'NONE', *, *, #5438, .F. ) ;
#7815=CARTESIAN_POINT ( 'NONE',  ( -2.073879752374872432, -2.575632606089756305, -0.1529717276817058880 ) ) ;
#7821=CIRCLE ( 'NONE', #6300, 0.01968503937007879193 ) ;
#7828=CARTESIAN_POINT ( 'NONE',  ( -1.182069932166307291, 0.3415656170906546940, -0.04962985469592846172 ) ) ;
#7834=CARTESIAN_POINT ( 'NONE',  ( -1.392039366404614897, -0.02281013714037220461, -0.03937007874015750752 ) ) ;
#7842=ORIENTED_EDGE ( 'NONE', *, *, #8447, .F. ) ;
#7846=TOROIDAL_SURFACE ( 'NONE', #1344, 0.2165354330708662012, 0.01968503937007873988 ) ;
#7855=ADVANCED_FACE ( 'NONE', ( #14440 ), #9078, .T. ) ;
#7857=DIRECTION ( 'NONE',  ( -0.000000000000000000, -0.000000000000000000, -1.000000000000000000 ) ) ;
#7863=CIRCLE ( 'NONE', #1128, 0.03937007874015747977 ) ;
#7865=AXIS2_PLACEMENT_3D ( 'NONE', #568, #7706, #11537 ) ;
#7870=CARTESIAN_POINT ( 'NONE',  ( -2.090051324975654268, -1.858423098536573503, -0.08664193191035729491 ) ) ;
#7877=CARTESIAN_POINT ( 'NONE',  ( -1.944102467919452959, -2.896447668998575420, -0.1270282496954552864 ) ) ;
#7879=CIRCLE ( 'NONE', #9131, 0.05905511811023620578 ) ;
#7881=CARTESIAN_POINT ( 'NONE',  ( -2.156935286759944503, -2.012462723082549587, -0.1097304796145708444 ) ) ;
#7890=VECTOR ( 'NONE', #6171, 39.37007874015748143 ) ;
#7901=CARTESIAN_POINT ( 'NONE',  ( -1.931770777078986034, -2.785713767061171353, -0.1768904282990497179 ) ) ;
#7902=AXIS2_PLACEMENT_3D ( 'NONE', #1815, #2830, #6437 ) ;
#7904=CARTESIAN_POINT ( 'NONE',  ( -1.398125690441303526, -0.003404927804347302606, 0.03937007874015747977 ) ) ;
#7911=DIRECTION ( 'NONE',  ( 1.224646799147353207E-16, 1.000000000000000000, 0.000000000000000000 ) ) ;
#7923=EDGE_CURVE ( 'NONE', #8061, #1797, #10542, .T. ) ;
#7924=FACE_OUTER_BOUND ( 'NONE', #15328, .T. ) ;
#7929=VERTEX_POINT ( 'NONE', #9533 ) ;
#7930=VERTEX_POINT ( 'NONE', #3329 ) ;
#7935=CARTESIAN_POINT ( 'NONE',  ( -0.04751022371103294506, 0.1688405673728649303, -0.05319490010182324757 ) ) ;
#7941=ORIENTED_EDGE ( 'NONE', *, *, #13481, .T. ) ;
#7944=CIRCLE ( 'NONE', #7196, 0.01968503937007874335 ) ;
#7945=CARTESIAN_POINT ( 'NONE',  ( -1.181342415325335571, 0.3435647566446752288, -0.04457062106905999854 ) ) ;
#7953=DIRECTION ( 'NONE',  ( -0.000000000000000000, -0.000000000000000000, -1.000000000000000000 ) ) ;
#7961=CARTESIAN_POINT ( 'NONE',  ( -1.568343923620152180, 0.1178486908565801600, 0.03937007874015747977 ) ) ;
#7982=EDGE_CURVE ( 'NONE', #14238, #14162, #7609, .T. ) ;
#7983=ORIENTED_EDGE ( 'NONE', *, *, #3722, .T. ) ;
#7984=( BOUNDED_SURFACE ( )  B_SPLINE_SURFACE ( 3, 2, ( 
 ( #4175, #6270, #5251 ),
 ( #7468, #3950, #12410 ),
 ( #2930, #8970, #432 ),
 ( #12491, #345, #14922 ),
 ( #9824, #8795, #11382 ),
 ( #8884, #567, #7533 ),
 ( #6438, #14691, #13563 ),
 ( #14601, #6352, #13427 ),
 ( #13497, #1681, #11230 ),
 ( #3866, #12260, #13661 ) ),
 .UNSPECIFIED., .F., .F., .T. ) 
 B_SPLINE_SURFACE_WITH_KNOTS ( ( 4, 2, 2, 2, 4 ),
 ( 3, 3 ),
 ( 0.000000000000000000, 0.01438918893332945780, 0.02158378339999418583, 0.02518108063332655244, 0.02877837786665891559 ),
 ( 0.000000000000000000, 1.000000000000000000 ),
 .UNSPECIFIED. ) 
 GEOMETRIC_REPRESENTATION_ITEM ( )  RATIONAL_B_SPLINE_SURFACE ( (
 ( 1.000000000000000000, 0.7071067811865475727, 1.000000000000000000),
 ( 1.000000000000000000, 0.7064777154098520473, 1.000000000000000000),
 ( 1.000000000000000000, 0.7074394717099544705, 1.000000000000000000),
 ( 1.000000000000000000, 0.7110974249889780996, 1.000000000000000000),
 ( 1.000000000000000000, 0.7126855531371033559, 1.000000000000000000),
 ( 1.000000000000000000, 0.7155933398974227977, 1.000000000000000000),
 ( 1.000000000000000000, 0.7166513996729255709, 1.000000000000000000),
 ( 1.000000000000000000, 0.7189195979667037939, 1.000000000000000000),
 ( 1.000000000000000000, 0.7201312545562511547, 1.000000000000000000),
 ( 1.000000000000000000, 0.7214151048184016535, 1.000000000000000000) ) ) 
 REPRESENTATION_ITEM ( '' )  SURFACE ( )  );
#7990=CARTESIAN_POINT ( 'NONE',  ( -1.181342415325333350, 0.3435647566446739520, 0.03937007874015747977 ) ) ;
#8000=DIRECTION ( 'NONE',  ( -0.000000000000000000, -2.212657494868377674E-16, 1.000000000000000000 ) ) ;
#8001=EDGE_LOOP ( 'NONE', ( #8572, #13050, #7255, #12523 ) ) ;
#8009=DIRECTION ( 'NONE',  ( -0.000000000000000000, -0.000000000000000000, -1.000000000000000000 ) ) ;
#8015=DIRECTION ( 'NONE',  ( 0.000000000000000000, 0.000000000000000000, 1.000000000000000000 ) ) ;
#8018=ORIENTED_EDGE ( 'NONE', *, *, #8292, .T. ) ;
#8019=VERTEX_POINT ( 'NONE', #4969 ) ;
#8026=CARTESIAN_POINT ( 'NONE',  ( -1.962370792254545027, -2.889990620475674898, 0.1128190176297459296 ) ) ;
#8027=PRODUCT ( 'Finger', 'Finger', '', ( #4250 ) ) ;
#8030=CARTESIAN_POINT ( 'NONE',  ( -1.398125690441303526, -0.003404927804347094439, 0.05905511811023622659 ) ) ;
#8034=ORIENTED_EDGE ( 'NONE', *, *, #3179, .T. ) ;
#8044=CARTESIAN_POINT ( 'NONE',  ( -1.951077307720631149, -2.792367362670038045, -0.1761343083128099618 ) ) ;
#8048=CARTESIAN_POINT ( 'NONE',  ( -1.332606523864378945, 0.1355266887446167634, 0.05905511811023622659 ) ) ;
#8057=CARTESIAN_POINT ( 'NONE',  ( -1.925122157694118652, -2.949207805218784006, 0.01171943552855665704 ) ) ;
#8061=VERTEX_POINT ( 'NONE', #8659 ) ;
#8065=CARTESIAN_POINT ( 'NONE',  ( -0.02374036903667606571, 0.1505616924844531690, 0.03732860159234808323 ) ) ;
#8070=ORIENTED_EDGE ( 'NONE', *, *, #3717, .T. ) ;
#8073=ORIENTED_EDGE ( 'NONE', *, *, #317, .T. ) ;
#8076=CARTESIAN_POINT ( 'NONE',  ( -1.964126537190518107, -2.749515453455440905, 0.1756903148397124803 ) ) ;
#8093=ORIENTED_EDGE ( 'NONE', *, *, #5438, .T. ) ;
#8095=APPLICATION_CONTEXT ( 'automotive_design' ) ;
#8103=ORIENTED_EDGE ( 'NONE', *, *, #2047, .F. ) ;
#8107=CARTESIAN_POINT ( 'NONE',  ( -1.950291921842994158, -2.794930396112696336, -0.1760874378794451134 ) ) ;
#8112=CARTESIAN_POINT ( 'NONE',  ( -1.409467368996963010, -0.007141430561139886987, 0.06138464873084744505 ) ) ;
#8114=AXIS2_PLACEMENT_3D ( 'NONE', #12413, #2534, #349 ) ;
#8117=CIRCLE ( 'NONE', #360, 0.2303149606299203511 ) ;
#8125=ORIENTED_EDGE ( 'NONE', *, *, #5843, .F. ) ;
#8129=DIRECTION ( 'NONE',  ( 0.5984233124757303290, 0.8011800915434521553, -0.000000000000000000 ) ) ;
#8131=FACE_OUTER_BOUND ( 'NONE', #13068, .T. ) ;
#8147=TOROIDAL_SURFACE ( 'NONE', #10895, 3.149606299212599048, 0.01968503937007873988 ) ;
#8152=DIRECTION ( 'NONE',  ( -0.9387676358159492418, 0.3445509047216873677, 0.000000000000000000 ) ) ;
#8156=ORIENTED_EDGE ( 'NONE', *, *, #3969, .T. ) ;
#8163=DIRECTION ( 'NONE',  ( 1.000000000000000000, 0.000000000000000000, 0.000000000000000000 ) ) ;
#8169=ORIENTED_EDGE ( 'NONE', *, *, #1508, .T. ) ;
#8170=CIRCLE ( 'NONE', #2404, 2.214566929133857887 ) ;
#8175=CARTESIAN_POINT ( 'NONE',  ( -0.002557446713253753914, 0.1765481709910071695, -0.0002437469044493141156 ) ) ;
#8178=DIRECTION ( 'NONE',  ( -1.000000000000000000, 0.000000000000000000, 0.000000000000000000 ) ) ;
#8180=CARTESIAN_POINT ( 'NONE',  ( -1.568343923620152847, 0.1178486908565804514, 0.05905511811023622659 ) ) ;
#8182=CARTESIAN_POINT ( 'NONE',  ( -1.234181327013985197, 0.1355266887446167634, 0.05905511811023622659 ) ) ;
#8200=CARTESIAN_POINT ( 'NONE',  ( -1.922875500960418149, -2.878807188367765058, 0.1420686080738781387 ) ) ;
#8201=VECTOR ( 'NONE', #15381, 39.37007874015748143 ) ;
#8216=DIRECTION ( 'NONE',  ( -0.8144815189573204606, 0.5801894994542525774, -0.000000000000000000 ) ) ;
#8218=CARTESIAN_POINT ( 'NONE',  ( -0.02525249394761181279, 0.1725264476027946747, 0.03885236003517052172 ) ) ;
#8219=ADVANCED_FACE ( 'NONE', ( #11236 ), #9385, .T. ) ;
#8225=DIRECTION ( 'NONE',  ( 0.000000000000000000, -0.000000000000000000, -1.000000000000000000 ) ) ;
#8229=ORIENTED_EDGE ( 'NONE', *, *, #404, .F. ) ;
#8232=EDGE_CURVE ( 'NONE', #7004, #2439, #5337, .T. ) ;
#8233=CARTESIAN_POINT ( 'NONE',  ( -1.925888590729081473, -2.947122644516800172, 0.02949560467575229258 ) ) ;
#8236=CARTESIAN_POINT ( 'NONE',  ( -1.923270046725593430, -2.877647921889221028, 0.1430015488209055441 ) ) ;
#8242=VERTEX_POINT ( 'NONE', #7776 ) ;
#8254=CARTESIAN_POINT ( 'NONE',  ( -1.190198933766853706, 0.3259758027579612860, 0.05905511811023622659 ) ) ;
#8256=CARTESIAN_POINT ( 'NONE',  ( -1.180847381051866707, 0.3433074774306728028, 0.05905511811023622659 ) ) ;
#8259=DIRECTION ( 'NONE',  ( -1.000000000000000000, 0.000000000000000000, 0.000000000000000000 ) ) ;
#8266=CARTESIAN_POINT ( 'NONE',  ( -1.906686051247057145, -2.925149623272649713, -0.09038834661822293948 ) ) ;
#8268=EDGE_CURVE ( 'NONE', #14788, #14790, #12140, .T. ) ;
#8272=EDGE_CURVE ( 'NONE', #12093, #4326, #15240, .T. ) ;
#8273=LINE ( 'NONE', #919, #5823 ) ;
#8275=ORIENTED_EDGE ( 'NONE', *, *, #12396, .F. ) ;
#8282=CARTESIAN_POINT ( 'NONE',  ( -0.01782267696647955174, -0.1622289191103822303, -0.03095755538600572856 ) ) ;
#8283=DIRECTION ( 'NONE',  ( 0.5984233124757279976, 0.8011800915434538206, 0.000000000000000000 ) ) ;
#8292=EDGE_CURVE ( 'NONE', #12093, #13620, #14136, .T. ) ;
#8293=ORIENTED_EDGE ( 'NONE', *, *, #5473, .F. ) ;
#8295=CARTESIAN_POINT ( 'NONE',  ( -1.938865708396552590, -2.947839766983606946, 0.02498451593668036402 ) ) ;
#8300=CARTESIAN_POINT ( 'NONE',  ( -1.912441115949275794, -2.839038486429707575, 0.1647378018180373216 ) ) ;
#8302=CARTESIAN_POINT ( 'NONE',  ( -1.991669579775100729, -2.812944829929203916, -0.1541819158628824904 ) ) ;
#8315=LINE ( 'NONE', #5796, #8201 ) ;
#8318=CARTESIAN_POINT ( 'NONE',  ( -1.607606114292111643, 0.09732815221480063672, -0.07874015748031495954 ) ) ;
#8323=VERTEX_POINT ( 'NONE', #4562 ) ;
#8330=AXIS2_PLACEMENT_3D ( 'NONE', #13691, #8991, #4040 ) ;
#8334=AXIS2_PLACEMENT_3D ( 'NONE', #14423, #13238, #11028 ) ;
#8337=CARTESIAN_POINT ( 'NONE',  ( -1.395867684562290378, -0.02540710596904927759, 0.04030457392454530469 ) ) ;
#8338=CARTESIAN_POINT ( 'NONE',  ( -1.961854477779698014, -2.757150671784349694, 0.1766817721349826786 ) ) ;
#8339=DIRECTION ( 'NONE',  ( 0.000000000000000000, 2.212657494868377674E-16, -1.000000000000000000 ) ) ;
#8344=AXIS2_PLACEMENT_3D ( 'NONE', #10272, #12779, #10341 ) ;
#8364=ORIENTED_EDGE ( 'NONE', *, *, #13314, .T. ) ;
#8365=TOROIDAL_SURFACE ( 'NONE', #5097, 0.2303149606299203511, 0.01968503937007873988 ) ;
#8368=EDGE_CURVE ( 'NONE', #11513, #10081, #144, .T. ) ;
#8371=AXIS2_PLACEMENT_3D ( 'NONE', #1190, #9411, #14185 ) ;
#8372=CARTESIAN_POINT ( 'NONE',  ( -1.985311755390524624, -2.772329397582317778, 0.1771653543307079026 ) ) ;
#8373=CARTESIAN_POINT ( 'NONE',  ( -1.900068616880432160, -2.943488425837897271, 0.04725664440068118310 ) ) ;
#8374=EDGE_CURVE ( 'NONE', #6704, #5049, #4651, .T. ) ;
#8375=CARTESIAN_POINT ( 'NONE',  ( -1.607606113623927691, 0.09732815316532632266, 0.07192616626583318851 ) ) ;
#8376=CARTESIAN_POINT ( 'NONE',  ( -1.930187871534237765, -2.935355666847295986, -0.06964585819737736938 ) ) ;
#8378=CARTESIAN_POINT ( 'NONE',  ( -0.03213667549430108267, -0.1820030000337380938, -0.02170016096604327968 ) ) ;
#8379=DIRECTION ( 'NONE',  ( -0.000000000000000000, 0.000000000000000000, 1.000000000000000000 ) ) ;
#8383=CARTESIAN_POINT ( 'NONE',  ( -1.942131557808294717, -2.755773022703220665, 0.1769289245135293731 ) ) ;
#8386=CARTESIAN_POINT ( 'NONE',  ( -1.945338968710944361, -2.932170493076832862, -0.04030640840855362339 ) ) ;
#8399=APPLICATION_CONTEXT ( 'automotive_design' ) ;
#8405=EDGE_LOOP ( 'NONE', ( #969, #10565, #1917, #7163 ) ) ;
#8410=AXIS2_PLACEMENT_3D ( 'NONE', #467, #5212, #12349 ) ;
#8412=AXIS2_PLACEMENT_3D ( 'NONE', #5606, #1010, #11659 ) ;
#8414=VECTOR ( 'NONE', #8015, 39.37007874015748143 ) ;
#8416=ORIENTED_EDGE ( 'NONE', *, *, #8232, .F. ) ;
#8419=DIRECTION ( 'NONE',  ( 0.000000000000000000, -0.000000000000000000, 1.000000000000000000 ) ) ;
#8447=EDGE_CURVE ( 'NONE', #1873, #15252, #8926, .T. ) ;
#8453=EDGE_CURVE ( 'NONE', #8061, #11513, #4128, .T. ) ;
#8459=CARTESIAN_POINT ( 'NONE',  ( -1.595687817112648954, 0.1142625427334059557, 0.07194693897042922504 ) ) ;
#8463=FACE_OUTER_BOUND ( 'NONE', #13818, .T. ) ;
#8465=AXIS2_PLACEMENT_3D ( 'NONE', #9971, #8781, #6418 ) ;
#8466=CARTESIAN_POINT ( 'NONE',  ( -1.934032282416884740, -2.845555853951683201, 0.1617933121749894620 ) ) ;
#8470=CIRCLE ( 'NONE', #5194, 0.05905511811023627516 ) ;
#8471=CARTESIAN_POINT ( 'NONE',  ( -0.01783696211247718169, 0.1513009196653194166, -0.03097470637416573774 ) ) ;
#8478=CARTESIAN_POINT ( 'NONE',  ( -1.395776408008654990, -0.02488039011573578430, 0.06612399333097303267 ) ) ;
#8479=PLANE ( 'NONE',  #12143 ) ;
#8485=CARTESIAN_POINT ( 'NONE',  ( -1.593720380427063876, 0.1169877005562839495, -0.06604764719695267738 ) ) ;
#8487=CARTESIAN_POINT ( 'NONE',  ( -0.03549374849269339854, -0.1824859222442999918, 0.04671604978335693048 ) ) ;
#8495=EDGE_CURVE ( 'NONE', #12240, #5035, #1139, .T. ) ;
#8496=DIRECTION ( 'NONE',  ( 0.000000000000000000, -0.000000000000000000, -1.000000000000000000 ) ) ;
#8500=DIRECTION ( 'NONE',  ( 1.000000000000000000, -0.000000000000000000, -0.000000000000000000 ) ) ;
#8505=EDGE_LOOP ( 'NONE', ( #8364, #2628, #5874, #3449 ) ) ;
#8509=CARTESIAN_POINT ( 'NONE',  ( -1.293236445124221312, 0.1355266887446167634, -0.03937007874015747977 ) ) ;
#8523=CARTESIAN_POINT ( 'NONE',  ( -1.584743043511021909, 0.1295304748375773751, -0.05905511811023622659 ) ) ;
#8525=DIRECTION ( 'NONE',  ( -0.000000000000000000, -0.000000000000000000, -1.000000000000000000 ) ) ;
#8527=CARTESIAN_POINT ( 'NONE',  ( -2.054794062199362781, -2.568933014740236498, 0.1522411129244188310 ) ) ;
#8528=FACE_OUTER_BOUND ( 'NONE', #6279, .T. ) ;
#8529=CARTESIAN_POINT ( 'NONE',  ( -1.926804229133072699, -2.867234193721032831, 0.1501075262831944590 ) ) ;
#8530=EDGE_LOOP ( 'NONE', ( #5991, #14864, #14568, #11377 ) ) ;
#8531=CARTESIAN_POINT ( 'NONE',  ( -1.955247660674698906, -2.907829365248872033, -0.09169626363195912400 ) ) ;
#8533=ORIENTED_EDGE ( 'NONE', *, *, #11823, .F. ) ;
#8534=EDGE_LOOP ( 'NONE', ( #10147, #6741 ) ) ;
#8538=DIRECTION ( 'NONE',  ( -0.000000000000000000, -0.000000000000000000, -1.000000000000000000 ) ) ;
#8541=CARTESIAN_POINT ( 'NONE',  ( -1.602377441323804996, 0.1047452084010624673, -0.05343540472197173818 ) ) ;
#8542=DIRECTION ( 'NONE',  ( -0.5801894994542525774, -0.8144815189573204606, 0.000000000000000000 ) ) ;
#8543=DIRECTION ( 'NONE',  ( -1.349229370204184172E-15, -1.000000000000000000, 0.000000000000000000 ) ) ;
#8546=CARTESIAN_POINT ( 'NONE',  ( -1.596293587998522945, 0.1133155780025432574, -0.04477369844328129428 ) ) ;
#8557=CARTESIAN_POINT ( 'NONE',  ( -2.755905511811024056, -2.772329397582842248, 0.000000000000000000 ) ) ;
#8559=DIRECTION ( 'NONE',  ( 0.7402970580929170152, 0.6722799013647308142, 0.000000000000000000 ) ) ;
#8560=CARTESIAN_POINT ( 'NONE',  ( -1.100415514366356762, -0.04998955061627542718, 0.05905511811023622659 ) ) ;
#8565=DIRECTION ( 'NONE',  ( -0.000000000000000000, -0.000000000000000000, -1.000000000000000000 ) ) ;
#8566=DIRECTION ( 'NONE',  ( 0.000000000000000000, 1.000000000000000000, -4.880644499660747568E-12 ) ) ;
#8569=CARTESIAN_POINT ( 'NONE',  ( -1.417802900492933782, -0.04287136159519133044, 0.07874015748031495954 ) ) ;
#8572=ORIENTED_EDGE ( 'NONE', *, *, #2599, .T. ) ;
#8579=EDGE_CURVE ( 'NONE', #14086, #4146, #9149, .T. ) ;
#8587=CARTESIAN_POINT ( 'NONE',  ( -1.926743884294085829, -2.799928598775826671, -0.1541059977087025634 ) ) ;
#8607=CARTESIAN_POINT ( 'NONE',  ( -2.176576600058865107, -2.015093358878988106, 0.09005837916847796165 ) ) ;
#8608=DIRECTION ( 'NONE',  ( 1.000000000000000000, 0.000000000000000000, 0.000000000000000000 ) ) ;
#8609=CARTESIAN_POINT ( 'NONE',  ( -1.906026250053923565, -2.926978850311991120, 0.08666856585884122333 ) ) ;
#8611=CARTESIAN_POINT ( 'NONE',  ( -1.943752432982631007, -2.936018085428647062, -0.02335751294002252551 ) ) ;
#8612=CARTESIAN_POINT ( 'NONE',  ( -1.584115185264708625, 0.1296286773226380806, 0.03937007874015747977 ) ) ;
#8619=CARTESIAN_POINT ( 'NONE',  ( -1.431036756819011213, -0.02829858486107876200, -0.08366141732283460808 ) ) ;
#8625=DIRECTION ( 'NONE',  ( -0.000000000000000000, 0.000000000000000000, 1.000000000000000000 ) ) ;
#8629=CARTESIAN_POINT ( 'NONE',  ( -0.04497577134311978031, -0.1837750859334940368, -0.03094209595079721806 ) ) ;
#8633=DIRECTION ( 'NONE',  ( 0.000000000000000000, -0.000000000000000000, 1.000000000000000000 ) ) ;
#8634=CARTESIAN_POINT ( 'NONE',  ( -1.182292271279389295, 0.3416831649379189484, -0.04963307157686430715 ) ) ;
#8635=CARTESIAN_POINT ( 'NONE',  ( -0.008240795940610745954, -0.1611877539686307204, 0.01644599795625022523 ) ) ;
#8637=AXIS2_PLACEMENT_3D ( 'NONE', #13644, #13729, #12476 ) ;
#8649=CARTESIAN_POINT ( 'NONE',  ( -0.3441669734936866343, 2.010494531933507467, -0.03937007874015747977 ) ) ;
#8654=LINE ( 'NONE', #15261, #15375 ) ;
#8659=CARTESIAN_POINT ( 'NONE',  ( -1.580080891953811628, 0.1020406297922293037, -0.08366141732283462196 ) ) ;
#8670=CARTESIAN_POINT ( 'NONE',  ( -1.941063491063433677, -2.942568514135356583, 0.04947710996518819848 ) ) ;
#8677=CARTESIAN_POINT ( 'NONE',  ( -1.895365998581063360, -2.883386225592859287, 0.1045859054727397014 ) ) ;
#8685=ORIENTED_EDGE ( 'NONE', *, *, #9165, .T. ) ;
#8692=CIRCLE ( 'NONE', #1683, 0.01968503937007872948 ) ;
#8695=CARTESIAN_POINT ( 'NONE',  ( -1.964126537190518107, -2.752050336136263819, 0.1561691687464110412 ) ) ;
#8697=CARTESIAN_POINT ( 'NONE',  ( -2.119211488178836866, -2.391206066311296841, 0.1145569965097087001 ) ) ;
#8698=CARTESIAN_POINT ( 'NONE',  ( -0.1771653543307086243, -0.02638708502139245488, -0.05905511811023622659 ) ) ;
#8699=CARTESIAN_POINT ( 'NONE',  ( -1.871152938270946642, -2.943146576430611727, -0.04758650140680115159 ) ) ;
#8701=CARTESIAN_POINT ( 'NONE',  ( -2.099929645848620297, -2.385360057865189454, -0.1341722008959704004 ) ) ;
#8705=VECTOR ( 'NONE', #13733, 39.37007874015748143 ) ;
#8709=CARTESIAN_POINT ( 'NONE',  ( -2.184126211765464287, -1.725292181286280480, 0.1968503937007874127 ) ) ;
#8714=CARTESIAN_POINT ( 'NONE',  ( -0.04489327544264908737, -0.1650454269528150719, -0.05194604157257243227 ) ) ;
#8720=DIRECTION ( 'NONE',  ( 0.000000000000000000, 2.212657494868377674E-16, 1.000000000000000000 ) ) ;
#8723=EDGE_LOOP ( 'NONE', ( #4958, #2024, #8103, #10105 ) ) ;
#8724=ORIENTED_EDGE ( 'NONE', *, *, #9165, .F. ) ;
#8726=DIRECTION ( 'NONE',  ( 1.000000000000000000, -0.000000000000000000, -0.000000000000000000 ) ) ;
#8728=CARTESIAN_POINT ( 'NONE',  ( -0.08151194962748890827, 0.1637246173173402264, -0.03937007874015747977 ) ) ;
#8730=CARTESIAN_POINT ( 'NONE',  ( -1.408713103043102821, -0.006839756437906783539, 0.06104195403929376512 ) ) ;
#8737=EDGE_LOOP ( 'NONE', ( #6199, #8125, #4637, #11824, #6587 ) ) ;
#8744=CARTESIAN_POINT ( 'NONE',  ( -1.949387861892222018, -2.922373346087915547, 0.09505135847318786635 ) ) ;
#8748=PLANE ( 'NONE',  #2090 ) ;
#8749=CARTESIAN_POINT ( 'NONE',  ( -1.452763252956529083, -0.05091287232363064796, -0.08366141732283456645 ) ) ;
#8751=CARTESIAN_POINT ( 'NONE',  ( -1.881730119666213508, -2.917306682172244869, 0.03996051238533837591 ) ) ;
#8760=CARTESIAN_POINT ( 'NONE',  ( -1.391815368240343576, -0.02267036402578939333, -0.03937007906611866836 ) ) ;
#8765=EDGE_CURVE ( 'NONE', #4146, #9812, #9483, .T. ) ;
#8767=CARTESIAN_POINT ( 'NONE',  ( -1.185322244938940894, 0.3350014259199165512, 0.05695314934226588383 ) ) ;
#8768=CARTESIAN_POINT ( 'NONE',  ( -1.887765756933061478, -2.902443322690533734, 0.07703872521121671313 ) ) ;
#8772=CARTESIAN_POINT ( 'NONE',  ( -1.572630165645712008, 0.1123721976951364415, 0.05999513677286145291 ) ) ;
#8777=ORIENTED_EDGE ( 'NONE', *, *, #3035, .F. ) ;
#8778=DIRECTION ( 'NONE',  ( 1.000000000000000000, 0.000000000000000000, 0.000000000000000000 ) ) ;
#8779=DIRECTION ( 'NONE',  ( -0.8144815189573204606, 0.5801894994542525774, -1.283760644411384396E-16 ) ) ;
#8781=DIRECTION ( 'NONE',  ( 0.000000000000000000, -0.000000000000000000, -1.000000000000000000 ) ) ;
#8782=CARTESIAN_POINT ( 'NONE',  ( -0.002345674784311424250, -0.1605320876855827750, 0.0006089964461715403551 ) ) ;
#8783=ORIENTED_EDGE ( 'NONE', *, *, #7114, .T. ) ;
#8787=CARTESIAN_POINT ( 'NONE',  ( -0.01656597074380655038, -0.1797544903306448061, 0.02941166498823430051 ) ) ;
#8788=EDGE_CURVE ( 'NONE', #11758, #11513, #6886, .T. ) ;
#8794=CARTESIAN_POINT ( 'NONE',  ( -1.417802900492933560, -0.04287136159519124717, -0.08366141732283458032 ) ) ;
#8795=CARTESIAN_POINT ( 'NONE',  ( -2.042760673955246187, -2.379061152454923889, 0.1351464036074991604 ) ) ;
#8796=FACE_OUTER_BOUND ( 'NONE', #5262, .T. ) ;
#8809=CARTESIAN_POINT ( 'NONE',  ( -1.945324558181595664, -2.932205473225905301, -0.04017210842460155334 ) ) ;
#8815=CARTESIAN_POINT ( 'NONE',  ( -1.938093919480919469, -2.767579153824591742, -0.1578472193797151868 ) ) ;
#8822=ORIENTED_EDGE ( 'NONE', *, *, #4003, .F. ) ;
#8831=CIRCLE ( 'NONE', #333, 1.865354330708661745 ) ;
#8840=CARTESIAN_POINT ( 'NONE',  ( -1.899963887369776172, -2.943774530195527372, 0.04512397944535982697 ) ) ;
#8842=CARTESIAN_POINT ( 'NONE',  ( -2.054794062201786176, -2.568933014739907872, -0.1522411129243764483 ) ) ;
#8848=EDGE_LOOP ( 'NONE', ( #7717, #8070, #9360, #264 ) ) ;
#8849=AXIS2_PLACEMENT_3D ( 'NONE', #13581, #12508, #12272 ) ;
#8858=VECTOR ( 'NONE', #14075, 39.37007874015748143 ) ;
#8863=CARTESIAN_POINT ( 'NONE',  ( -2.100501784635051550, -1.630597114118274238, 0.1033464566929129663 ) ) ;
#8869=CARTESIAN_POINT ( 'NONE',  ( -1.172017912842092668, 0.3609012623030120603, 0.05905511811023622659 ) ) ;
#8884=CARTESIAN_POINT ( 'NONE',  ( -2.030417246223212402, -2.521630590619702961, 0.1490281301122292346 ) ) ;
#8896=AXIS2_PLACEMENT_3D ( 'NONE', #10406, #15262, #11503 ) ;
#8901=TOROIDAL_SURFACE ( 'NONE', #13652, 0.2165354330708662012, 0.01968503937007873988 ) ;
#8906=CARTESIAN_POINT ( 'NONE',  ( -1.945459748359985142, -2.745801194614594820, -0.1561691687464109024 ) ) ;
#8909=CARTESIAN_POINT ( 'NONE',  ( -1.988219667330677565, -2.822309060621705168, -0.1701858252292633988 ) ) ;
#8912=CARTESIAN_POINT ( 'NONE',  ( -1.898314360964700853, -2.875886787523748822, -0.1125291835257540562 ) ) ;
#8914=CARTESIAN_POINT ( 'NONE',  ( -1.964126537190516331, -2.749515453455443570, -0.1756903148397133685 ) ) ;
#8916=CIRCLE ( 'NONE', #8410, 0.2106299212598415904 ) ;
#8924=CARTESIAN_POINT ( 'NONE',  ( -1.417127096045877499, -0.01082856000845578912, -0.06859240798594633259 ) ) ;
#8925=EDGE_CURVE ( 'NONE', #10393, #2999, #1164, .T. ) ;
#8926=B_SPLINE_CURVE_WITH_KNOTS ( 'NONE', 3,
 ( #3168, #7945, #8634, #108, #3782, #12172 ),
 .UNSPECIFIED., .F., .F.,
 ( 4, 2, 4 ),
 ( 4.336808689942017736E-19, 0.0003906509022999027445, 0.0007813018045998050554 ),
 .UNSPECIFIED. ) ;
#8936=CARTESIAN_POINT ( 'NONE',  ( -1.869327508327784271, -2.947498318410580964, -0.02746507530585597448 ) ) ;
#8942=EDGE_LOOP ( 'NONE', ( #8999, #2271, #385, #1466 ) ) ;
#8945=VECTOR ( 'NONE', #316, 39.37007874015748143 ) ;
#8949=CARTESIAN_POINT ( 'NONE',  ( -1.580080891953811628, 0.1020406297922293454, 0.07874015748031495954 ) ) ;
#8954=CARTESIAN_POINT ( 'NONE',  ( -1.452763252956527751, -0.05091287232363168880, 0.08366141732283458032 ) ) ;
#8955=ORIENTED_EDGE ( 'NONE', *, *, #14036, .F. ) ;
#8960=CARTESIAN_POINT ( 'NONE',  ( -0.01755170026722350021, -0.1621998028774611911, 0.03064271692327978289 ) ) ;
#8967=CARTESIAN_POINT ( 'NONE',  ( -2.090051324975654268, -1.858423098537180129, 0.08664193191037310171 ) ) ;
#8970=CARTESIAN_POINT ( 'NONE',  ( -2.092336816894301954, -2.008044473685774545, 0.1095437400971965014 ) ) ;
#8986=CARTESIAN_POINT ( 'NONE',  ( -1.977060708627759400, -2.798357293484028396, 0.1753504056559904711 ) ) ;
#8988=CARTESIAN_POINT ( 'NONE',  ( -1.961618730074871753, -2.845436301845790439, -0.1618467189898775138 ) ) ;
#8990=CARTESIAN_POINT ( 'NONE',  ( -0.3441669734936866343, 2.010494531933507467, 0.03937007874015747977 ) ) ;
#8991=DIRECTION ( 'NONE',  ( 0.8144815189573204606, -0.5801894994542525774, -1.283760644411384396E-16 ) ) ;
#8994=EDGE_CURVE ( 'NONE', #14646, #10393, #8916, .T. ) ;
#8995=EDGE_LOOP ( 'NONE', ( #1545, #7842, #3445 ) ) ;
#8999=ORIENTED_EDGE ( 'NONE', *, *, #171, .F. ) ;
#9000=CARTESIAN_POINT ( 'NONE',  ( -2.090051324975654268, -1.783311776966560736, 0.08466247786334288317 ) ) ;
#9008=CARTESIAN_POINT ( 'NONE',  ( -1.181342415303537230, 0.3435647566330583547, 0.04453711288980924388 ) ) ;
#9009=CARTESIAN_POINT ( 'NONE',  ( -1.945364619566915643, -2.810512954809210928, -0.1731107110282803507 ) ) ;
#9012=CARTESIAN_POINT ( 'NONE',  ( -1.584115185264708403, 0.1296286773226380251, 0.03937007874015747977 ) ) ;
#9014=ORIENTED_EDGE ( 'NONE', *, *, #14489, .T. ) ;
#9017=FACE_OUTER_BOUND ( 'NONE', #12787, .T. ) ;
#9021=DIRECTION ( 'NONE',  ( 0.5801894994542512451, 0.8144815189573213488, -2.341876692568692102E-14 ) ) ;
#9025=CARTESIAN_POINT ( 'NONE',  ( -1.419615703680148000, -0.01226548409420233354, -0.08366141732283458032 ) ) ;
#9030=ORIENTED_EDGE ( 'NONE', *, *, #10765, .T. ) ;
#9037=DIRECTION ( 'NONE',  ( 0.000000000000000000, -0.000000000000000000, 1.000000000000000000 ) ) ;
#9049=ORIENTED_EDGE ( 'NONE', *, *, #8272, .T. ) ;
#9050=ORIENTED_EDGE ( 'NONE', *, *, #12567, .T. ) ;
#9051=ADVANCED_FACE ( 'NONE', ( #2958 ), #2867, .T. ) ;
#9052=DIRECTION ( 'NONE',  ( -0.5801894994542512451, -0.8144815189573213488, 0.000000000000000000 ) ) ;
#9053=CARTESIAN_POINT ( 'NONE',  ( -1.992382107315058049, -2.749515453455440905, 0.1756903148397118974 ) ) ;
#9055=CARTESIAN_POINT ( 'NONE',  ( -1.959346498473351739, -2.897603755323506558, -0.1049048269901905472 ) ) ;
#9058=FACE_OUTER_BOUND ( 'NONE', #904, .T. ) ;
#9064=AXIS2_PLACEMENT_3D ( 'NONE', #10456, #15236, #1996 ) ;
#9068=ADVANCED_FACE ( 'NONE', ( #15174 ), #7476, .T. ) ;
#9074=CARTESIAN_POINT ( 'NONE',  ( -1.924914443801520880, -2.804978272008806339, -0.1525920034357165223 ) ) ;
#9078=( BOUNDED_SURFACE ( )  B_SPLINE_SURFACE ( 3, 2, ( 
 ( #4643, #9435, #10748 ),
 ( #14207, #4784, #5882 ),
 ( #14347, #13184, #2448 ),
 ( #3704, #6024, #15462 ),
 ( #98, #4724, #13253 ),
 ( #4864, #8478, #9508 ),
 ( #14276, #3541, #8112 ),
 ( #8337, #2243, #4582 ),
 ( #14235, #10470, #13994 ),
 ( #13046, #12899, #8030 ) ),
 .UNSPECIFIED., .F., .F., .T. ) 
 B_SPLINE_SURFACE_WITH_KNOTS ( ( 4, 2, 2, 2, 4 ),
 ( 3, 3 ),
 ( -4.336808689942017736E-19, 0.0004011410879367268431, 0.0008022821758734541200, 0.001203423263810181505, 0.001604564351746908674 ),
 ( 0.000000000000000000, 1.000000000000000000 ),
 .UNSPECIFIED. ) 
 GEOMETRIC_REPRESENTATION_ITEM ( )  RATIONAL_B_SPLINE_SURFACE ( (
 ( 1.000000000000000000, 0.6273322353868007184, 1.000000000000000000),
 ( 1.000000000000000000, 0.6273746451327694151, 1.000000000000000000),
 ( 1.000000000000000000, 0.6276600930324378602, 1.000000000000000000),
 ( 1.000000000000000000, 0.6305495266240448426, 1.000000000000000000),
 ( 1.000000000000000000, 0.6332412771137517771, 1.000000000000000000),
 ( 1.000000000000000000, 0.6440211513203998317, 1.000000000000000000),
 ( 1.000000000000000000, 0.6523247361999675586, 1.000000000000000000),
 ( 1.000000000000000000, 0.6753292279000220333, 1.000000000000000000),
 ( 1.000000000000000000, 0.6902147318493536687, 1.000000000000000000),
 ( 1.000000000000000000, 0.7071067811865465735, 1.000000000000000000) ) ) 
 REPRESENTATION_ITEM ( '' )  SURFACE ( )  );
#9082=CIRCLE ( 'NONE', #13831, 0.01968503937007883009 ) ;
#9088=DIRECTION ( 'NONE',  ( 0.5801894994542535766, 0.8144815189573197944, 0.000000000000000000 ) ) ;
#9098=CIRCLE ( 'NONE', #10846, 0.01968503937007873988 ) ;
#9100=VECTOR ( 'NONE', #1807, 39.37007874015748854 ) ;
#9116=CARTESIAN_POINT ( 'NONE',  ( -0.06425120930260368179, -0.1863186860285575841, 0.03845354371037630614 ) ) ;
#9122=CYLINDRICAL_SURFACE ( 'NONE', #12185, 2.214566929133857887 ) ;
#9126=AXIS2_PLACEMENT_3D ( 'NONE', #1883, #7911, #2026 ) ;
#9131=AXIS2_PLACEMENT_3D ( 'NONE', #1432, #2676, #5161 ) ;
#9143=EDGE_CURVE ( 'NONE', #13968, #14556, #11666, .T. ) ;
#9145=CARTESIAN_POINT ( 'NONE',  ( -1.946192867917151181, -2.743611295743891620, -0.1749236412511689931 ) ) ;
#9149=CIRCLE ( 'NONE', #5625, 3.169291338582677753 ) ;
#9152=CARTESIAN_POINT ( 'NONE',  ( -1.592432191550702480, 0.1184937169715563343, -0.04125010960116162056 ) ) ;
#9159=CARTESIAN_POINT ( 'NONE',  ( -1.964126537190516997, -2.749515453455444014, -0.1756903148397123970 ) ) ;
#9160=CIRCLE ( 'NONE', #7639, 0.2303149606299203511 ) ;
#9165=EDGE_CURVE ( 'NONE', #7239, #7930, #14666, .T. ) ;
#9173=DIRECTION ( 'NONE',  ( -0.000000000000000000, 0.000000000000000000, 1.000000000000000000 ) ) ;
#9177=ORIENTED_EDGE ( 'NONE', *, *, #1283, .F. ) ;
#9182=B_SPLINE_CURVE_WITH_KNOTS ( 'NONE', 3,
 ( #13490, #12394, #1572, #557, #5481, #1895, #6331, #11453 ),
 .UNSPECIFIED., .F., .F.,
 ( 4, 2, 2, 4 ),
 ( 0.005704847486038692669, 0.01714141318827901161, 0.02285969603939917022, 0.02857797889051934964 ),
 .UNSPECIFIED. ) ;
#9185=AXIS2_PLACEMENT_3D ( 'NONE', #87, #10663, #4846 ) ;
#9191=CIRCLE ( 'NONE', #9949, 3.149606299212599048 ) ;
#9196=CIRCLE ( 'NONE', #12200, 0.01968503937007875723 ) ;
#9197=CARTESIAN_POINT ( 'NONE',  ( -0.02018259705034725071, -0.1802452534892125813, 1.049219007154695292E-17 ) ) ;
#9199=DIRECTION ( 'NONE',  ( 0.000000000000000000, 2.212657494868377674E-16, 1.000000000000000000 ) ) ;
#9200=AXIS2_PLACEMENT_3D ( 'NONE', #492, #1970, #9088 ) ;
#9201=CARTESIAN_POINT ( 'NONE',  ( -1.580080891953810962, 0.1020406297922289152, 0.07529375917875073820 ) ) ;
#9214=LINE ( 'NONE', #3180, #7097 ) ;
#9218=CARTESIAN_POINT ( 'NONE',  ( -1.574484809660005480, 0.1100025355994808662, -0.06175692796176408816 ) ) ;
#9219=DIRECTION ( 'NONE',  ( -0.000000000000000000, -0.000000000000000000, 1.000000000000000000 ) ) ;
#9224=B_SPLINE_CURVE_WITH_KNOTS ( 'NONE', 3,
 ( #1410, #10795, #78, #2560, #9639, #6167 ),
 .UNSPECIFIED., .F., .F.,
 ( 4, 2, 4 ),
 ( 0.000000000000000000, 0.01440388436194928005, 0.02880776872389856011 ),
 .UNSPECIFIED. ) ;
#9230=ORIENTED_EDGE ( 'NONE', *, *, #11755, .F. ) ;
#9232=CARTESIAN_POINT ( 'NONE',  ( -1.568343923620152847, 0.1178486908565804514, 0.05905511811023622659 ) ) ;
#9234=CARTESIAN_POINT ( 'NONE',  ( -0.008695292838828817469, 0.1754324108223994649, 0.01747077667448701521 ) ) ;
#9236=CARTESIAN_POINT ( 'NONE',  ( -0.008240795940610761566, -0.1611877539686306926, -0.01644599795625024952 ) ) ;
#9238=CARTESIAN_POINT ( 'NONE',  ( -1.949180757224311611, -2.798430349193752775, -0.1753397919474670996 ) ) ;
#9248=CARTESIAN_POINT ( 'NONE',  ( -1.927187694266953466, -2.943580729745926661, 0.04691452208654782463 ) ) ;
#9249=DIRECTION ( 'NONE',  ( 1.000000000000000000, 0.000000000000000000, 0.000000000000000000 ) ) ;
#9250=CARTESIAN_POINT ( 'NONE',  ( -2.090051324975654268, -1.858423098536573503, -0.08664193191035729491 ) ) ;
#9253=DIRECTION ( 'NONE',  ( -0.000000000000000000, -0.000000000000000000, -1.000000000000000000 ) ) ;
#9260=ORIENTED_EDGE ( 'NONE', *, *, #11338, .F. ) ;
#9265=CARTESIAN_POINT ( 'NONE',  ( -0.002500327830562678200, 0.1532658568795227105, 0.000000000000000000 ) ) ;
#9275=DIRECTION ( 'NONE',  ( 1.000000000000000000, -0.000000000000000000, -0.000000000000000000 ) ) ;
#9279=ORIENTED_EDGE ( 'NONE', *, *, #1071, .T. ) ;
#9281=ORIENTED_EDGE ( 'NONE', *, *, #14895, .F. ) ;
#9284=CARTESIAN_POINT ( 'NONE',  ( -1.115439883890946726, -0.06270839865334709717, -0.03937007874015747977 ) ) ;
#9286=CARTESIAN_POINT ( 'NONE',  ( -1.898327483181569963, -2.948264329531598893, 0.02398964596264746910 ) ) ;
#9289=CARTESIAN_POINT ( 'NONE',  ( -1.100415514366371195, -0.04998955061625851709, 0.03937007874015747977 ) ) ;
#9295=EDGE_LOOP ( 'NONE', ( #10806, #5870, #1980, #3234 ) ) ;
#9296=VERTEX_POINT ( 'NONE', #6277 ) ;
#9297=DIRECTION ( 'NONE',  ( -0.000000000000000000, -0.000000000000000000, -1.000000000000000000 ) ) ;
#9298=LINE ( 'NONE', #14072, #14888 ) ;
#9318=CARTESIAN_POINT ( 'NONE',  ( -1.925470963062591023, -2.948261428410166918, -0.02401791239041710727 ) ) ;
#9321=CARTESIAN_POINT ( 'NONE',  ( -1.190198933766848155, 0.3259758027579586215, -0.05905511811023622659 ) ) ;
#9323=ORIENTED_EDGE ( 'NONE', *, *, #9610, .F. ) ;
#9334=ORIENTED_EDGE ( 'NONE', *, *, #4999, .T. ) ;
#9356=DIRECTION ( 'NONE',  ( 0.000000000000000000, -1.000000000000000000, 2.212657494868377674E-16 ) ) ;
#9359=AXIS2_PLACEMENT_3D ( 'NONE', #802, #8009, #3397 ) ;
#9360=ORIENTED_EDGE ( 'NONE', *, *, #13331, .F. ) ;
#9363=CIRCLE ( 'NONE', #13594, 0.01968503937007872948 ) ;
#9367=CARTESIAN_POINT ( 'NONE',  ( -1.961853848035927994, -2.757152788027944279, -0.1766820469359192958 ) ) ;
#9380=ORIENTED_EDGE ( 'NONE', *, *, #12567, .F. ) ;
#9385=TOROIDAL_SURFACE ( 'NONE', #10142, 0.05905511811023621271, 0.01968503937007873988 ) ;
#9387=FACE_OUTER_BOUND ( 'NONE', #15468, .T. ) ;
#9389=CARTESIAN_POINT ( 'NONE',  ( -0.002322522588111503115, 0.1532890258252367910, -0.0007019553870510035357 ) ) ;
#9390=CARTESIAN_POINT ( 'NONE',  ( -0.004688298860636734219, -0.1607931678657649743, -0.008473975361459462965 ) ) ;
#9403=EDGE_CURVE ( 'NONE', #2172, #9995, #7663, .T. ) ;
#9405=ADVANCED_FACE ( 'NONE', ( #5193 ), #9122, .T. ) ;
#9411=DIRECTION ( 'NONE',  ( -0.000000000000000000, -0.000000000000000000, -1.000000000000000000 ) ) ;
#9417=CARTESIAN_POINT ( 'NONE',  ( -1.387704745771440207, -0.02010536753476152225, 0.03937007874015747977 ) ) ;
#9425=EDGE_LOOP ( 'NONE', ( #15451, #1763, #1403 ) ) ;
#9432=CARTESIAN_POINT ( 'NONE',  ( -1.992382107315057160, -2.749515453455444014, -0.1756903148397123138 ) ) ;
#9435=CARTESIAN_POINT ( 'NONE',  ( -1.399712685227380016, -0.02644324263748132689, 0.07874015748031497341 ) ) ;
#9440=VERTEX_POINT ( 'NONE', #6681 ) ;
#9442=CARTESIAN_POINT ( 'NONE',  ( -1.580080891953811628, 0.1020406297922293454, 0.07874015748031495954 ) ) ;
#9445=AXIS2_PLACEMENT_3D ( 'NONE', #15063, #15145, #11616 ) ;
#9456=DIRECTION ( 'NONE',  ( 1.000000000000000000, 0.000000000000000000, 0.000000000000000000 ) ) ;
#9457=CARTESIAN_POINT ( 'NONE',  ( -1.943208788703627787, -2.817317615915758466, -0.1717371570881610909 ) ) ;
#9463=CIRCLE ( 'NONE', #11450, 0.05905511811023620578 ) ;
#9475=CARTESIAN_POINT ( 'NONE',  ( -2.182693454834259139, -1.630005269948474389, -0.08366141732283423338 ) ) ;
#9483=LINE ( 'NONE', #3673, #10152 ) ;
#9486=ORIENTED_EDGE ( 'NONE', *, *, #12675, .T. ) ;
#9487=( GEOMETRIC_REPRESENTATION_CONTEXT ( 3 ) GLOBAL_UNCERTAINTY_ASSIGNED_CONTEXT ( ( #12071 ) ) GLOBAL_UNIT_ASSIGNED_CONTEXT ( ( #14065, #1151, #13042 ) ) REPRESENTATION_CONTEXT ( 'NONE', 'WORKASPACE' ) );
#9494=CARTESIAN_POINT ( 'NONE',  ( -1.960454989549089699, -2.761853628972389174, 0.1772924660290619847 ) ) ;
#9496=CARTESIAN_POINT ( 'NONE',  ( -1.959418227522675249, -2.897423706371843100, -0.1051064557059967070 ) ) ;
#9508=CARTESIAN_POINT ( 'NONE',  ( -1.411829724187707580, -0.008176884669458164834, 0.06280128582456272202 ) ) ;
#9522=ORIENTED_EDGE ( 'NONE', *, *, #3073, .T. ) ;
#9525=DIRECTION ( 'NONE',  ( 0.000000000000000000, 0.000000000000000000, -1.000000000000000000 ) ) ;
#9533=CARTESIAN_POINT ( 'NONE',  ( -1.511943070284283097, 0.2262540267724839904, 0.03937007874015747977 ) ) ;
#9535=DIRECTION ( 'NONE',  ( -0.000000000000000000, 0.000000000000000000, 1.000000000000000000 ) ) ;
#9542=DIRECTION ( 'NONE',  ( 0.000000000000000000, -0.000000000000000000, -1.000000000000000000 ) ) ;
#9544=CARTESIAN_POINT ( 'NONE',  ( 0.9851651268172137987, -1.725292181286280480, 0.1968503937007874127 ) ) ;
#9556=CARTESIAN_POINT ( 'NONE',  ( -1.596214514713377719, 0.1135332889814021501, 0.07874015748031495954 ) ) ;
#9557=CARTESIAN_POINT ( 'NONE',  ( -1.949533059518675726, -2.921996214527964764, -0.09505434699680524735 ) ) ;
#9561=CARTESIAN_POINT ( 'NONE',  ( -1.964126537190517441, -2.749515453455440905, 0.1756903148397118697 ) ) ;
#9563=CARTESIAN_POINT ( 'NONE',  ( -2.007201644623049841, -2.769458770238572676, 0.1575875454750225446 ) ) ;
#9572=DIRECTION ( 'NONE',  ( -1.000000000000000000, 0.000000000000000000, 0.000000000000000000 ) ) ;
#9575=CARTESIAN_POINT ( 'NONE',  ( -1.607606113623940791, 0.09732815316530769867, -0.07192616626586137429 ) ) ;
#9579=DIRECTION ( 'NONE',  ( 0.000000000000000000, -1.000000000000000000, 2.212657494868377674E-16 ) ) ;
#9583=ORIENTED_EDGE ( 'NONE', *, *, #5549, .F. ) ;
#9588=EDGE_CURVE ( 'NONE', #4902, #8242, #1182, .T. ) ;
#9589=CIRCLE ( 'NONE', #11585, 0.01968503937007868437 ) ;
#9590=SPHERICAL_SURFACE ( 'NONE', #4593, 0.01968503937007873988 ) ;
#9598=DIRECTION ( 'NONE',  ( 7.230275848357267942E-16, -5.150430092931769150E-16, -1.000000000000000000 ) ) ;
#9606=VERTEX_POINT ( 'NONE', #3548 ) ;
#9610=EDGE_CURVE ( 'NONE', #3678, #12240, #688, .T. ) ;
#9614=DIRECTION ( 'NONE',  ( 0.9995479251422038081, -0.03006568382583900759, 0.000000000000000000 ) ) ;
#9623=CIRCLE ( 'NONE', #10626, 0.01968503937007875723 ) ;
#9624=FACE_OUTER_BOUND ( 'NONE', #12679, .T. ) ;
#9628=CARTESIAN_POINT ( 'NONE',  ( -2.183651372152203507, -1.661851685721183136, -0.08366141732283423338 ) ) ;
#9631=VERTEX_POINT ( 'NONE', #6260 ) ;
#9635=AXIS2_PLACEMENT_3D ( 'NONE', #9888, #7519, #2811 ) ;
#9637=AXIS2_PLACEMENT_3D ( 'NONE', #13254, #5010, #3928 ) ;
#9639=CARTESIAN_POINT ( 'NONE',  ( -2.054789683517502574, -2.568945684013812070, 0.1522427580697409966 ) ) ;
#9640=CARTESIAN_POINT ( 'NONE',  ( -1.579560462702055190, 0.1027931347612739549, 0.07190453453444432819 ) ) ;
#9646=VECTOR ( 'NONE', #2751, 39.37007874015748143 ) ;
#9649=CARTESIAN_POINT ( 'NONE',  ( -1.943431940181322481, -2.816572830930641036, 0.1716618975443832407 ) ) ;
#9652=CARTESIAN_POINT ( 'NONE',  ( -1.980093622780896956, -2.844111206679635906, 0.1439326711935206005 ) ) ;
#9654=CARTESIAN_POINT ( 'NONE',  ( -0.04509495097506254629, 0.1479884890110657880, -0.05203401519686126631 ) ) ;
#9661=AXIS2_PLACEMENT_3D ( 'NONE', #882, #4554, #14042 ) ;
#9670=CARTESIAN_POINT ( 'NONE',  ( -1.599731447215878788, 0.1084887237743279165, -0.04822519498669181059 ) ) ;
#9671=DIRECTION ( 'NONE',  ( 1.000000000000000000, 0.000000000000000000, 0.000000000000000000 ) ) ;
#9674=CARTESIAN_POINT ( 'NONE',  ( -0.06972667172716363881, -0.1870117487642863896, 0.03937007824553747509 ) ) ;
#9682=CYLINDRICAL_SURFACE ( 'NONE', #10646, 0.1771653543307079026 ) ;
#9688=CARTESIAN_POINT ( 'NONE',  ( -0.07545607570875816072, 0.1645859079935992897, 0.03937007874015746589 ) ) ;
#9692=CARTESIAN_POINT ( 'NONE',  ( -1.580259682937577903, 0.1018956540318208953, -0.04477369844328074611 ) ) ;
#9698=TOROIDAL_SURFACE ( 'NONE', #13192, 2.194881889763779181, 0.01968503937007873988 ) ;
#9708=FACE_OUTER_BOUND ( 'NONE', #1409, .T. ) ;
#9713=ADVANCED_FACE ( 'NONE', ( #37 ), #269, .F. ) ;
#9717=B_SPLINE_CURVE_WITH_KNOTS ( 'NONE', 3,
 ( #12023, #14358, #6033, #3937, #6195, #9817, #6259, #8635, #13263, #13327 ),
 .UNSPECIFIED., .F., .F.,
 ( 4, 2, 2, 2, 4 ),
 ( 0.000000000000000000, 0.0006575499428678712377, 0.001315099885735742475, 0.001972649828603614038, 0.002630199771471484517 ),
 .UNSPECIFIED. ) ;
#9728=CARTESIAN_POINT ( 'NONE',  ( -1.979213154580101275, -2.704552134622930204, 0.1698516854049418046 ) ) ;
#9729=ORIENTED_EDGE ( 'NONE', *, *, #4801, .F. ) ;
#9730=CARTESIAN_POINT ( 'NONE',  ( -1.959343309635757757, -2.897611896471060433, 0.1048995451756935399 ) ) ;
#9731=ADVANCED_FACE ( 'NONE', ( #4082 ), #15053, .F. ) ;
#9739=ORIENTED_EDGE ( 'NONE', *, *, #5801, .F. ) ;
#9740=CYLINDRICAL_SURFACE ( 'NONE', #5862, 0.01968503937007875723 ) ;
#9749=CARTESIAN_POINT ( 'NONE',  ( -1.596214514379631577, 0.1135332894430610556, -0.07535569387266634334 ) ) ;
#9751=CARTESIAN_POINT ( 'NONE',  ( -0.03452177266044149928, -0.1823242888858135624, 0.02287309002717315826 ) ) ;
#9754=MANIFOLD_SOLID_BREP ( 'Fillet5', #12378 ) ;
#9770=ORIENTED_EDGE ( 'NONE', *, *, #13651, .F. ) ;
#9776=DIRECTION ( 'NONE',  ( 1.000000000000000000, 0.000000000000000000, 0.000000000000000000 ) ) ;
#9785=VERTEX_POINT ( 'NONE', #11372 ) ;
#9786=VERTEX_POINT ( 'NONE', #1579 ) ;
#9794=CARTESIAN_POINT ( 'NONE',  ( -1.888395665188653094, -2.901081385897817277, -0.1225630396599474148 ) ) ;
#9796=CARTESIAN_POINT ( 'NONE',  ( -1.943333224563443595, -2.937028733817375947, 0.01142278406163464016 ) ) ;
#9804=ADVANCED_FACE ( 'NONE', ( #2040 ), #10694, .T. ) ;
#9806=EDGE_CURVE ( 'NONE', #2439, #9943, #9191, .T. ) ;
#9812=VERTEX_POINT ( 'NONE', #15132 ) ;
#9815=CARTESIAN_POINT ( 'NONE',  ( -1.591501945092674841, 0.08600752902535276079, -0.08366141732283462196 ) ) ;
#9817=CARTESIAN_POINT ( 'NONE',  ( -0.02371960882139430987, -0.1628608293428424891, 0.03730919803856837247 ) ) ;
#9820=VERTEX_POINT ( 'NONE', #11528 ) ;
#9824=CARTESIAN_POINT ( 'NONE',  ( -2.061751060645342637, -2.382911221804981494, 0.1354770691259033766 ) ) ;
#9841=CARTESIAN_POINT ( 'NONE',  ( -1.945283543323844455, -2.932305031303924281, 0.03979015993530637257 ) ) ;
#9844=CARTESIAN_POINT ( 'NONE',  ( -1.574484809660005480, 0.1100025355994808662, -0.06175692796176408816 ) ) ;
#9845=DIRECTION ( 'NONE',  ( 1.000000000000000000, 0.000000000000000000, 0.000000000000000000 ) ) ;
#9850=DIRECTION ( 'NONE',  ( -0.8011800915434517112, 0.5984233124757307731, 0.000000000000000000 ) ) ;
#9852=CIRCLE ( 'NONE', #10345, 0.01968503937007873988 ) ;
#9853=ORIENTED_EDGE ( 'NONE', *, *, #1012, .T. ) ;
#9857=VERTEX_POINT ( 'NONE', #12854 ) ;
#9861=CARTESIAN_POINT ( 'NONE',  ( -1.403185310738388036, -0.03069143131531506044, -0.04402505006082085837 ) ) ;
#9870=CARTESIAN_POINT ( 'NONE',  ( -1.879680948933423856, -2.922298401170338344, 0.01183035193844450030 ) ) ;
#9884=B_SPLINE_CURVE_WITH_KNOTS ( 'NONE', 3,
 ( #10927, #218, #13125, #14304, #5988, #7601, #3564, #6139, #12481, #8569 ),
 .UNSPECIFIED., .F., .F.,
 ( 4, 2, 2, 2, 4 ),
 ( 0.000000000000000000, 0.0003853806145889340524, 0.0007707612291778681048, 0.001156141843766802157, 0.001541522458355736210 ),
 .UNSPECIFIED. ) ;
#9888=CARTESIAN_POINT ( 'NONE',  ( -0.2362204724409448231, -0.02638708502139245488, -0.03937007874015747977 ) ) ;
#9889=DIRECTION ( 'NONE',  ( 0.8144815189573203495, -0.5801894994542524664, 0.000000000000000000 ) ) ;
#9892=CARTESIAN_POINT ( 'NONE',  ( -0.01656597074380673426, -0.1797544903306477204, -0.02941166498823429704 ) ) ;
#9897=FACE_OUTER_BOUND ( 'NONE', #1134, .T. ) ;
#9901=EDGE_CURVE ( 'NONE', #9995, #10028, #5504, .T. ) ;
#9915=CARTESIAN_POINT ( 'NONE',  ( -1.985311755390326782, -2.772329397582949717, -0.1771653543307079026 ) ) ;
#9924=ORIENTED_EDGE ( 'NONE', *, *, #8374, .T. ) ;
#9927=AXIS2_PLACEMENT_3D ( 'NONE', #11238, #7628, #4101 ) ;
#9928=EDGE_CURVE ( 'NONE', #7929, #2402, #4215, .T. ) ;
#9931=CARTESIAN_POINT ( 'NONE',  ( -0.002500327830563101039, -0.1605493263772690415, 0.000000000000000000 ) ) ;
#9932=CARTESIAN_POINT ( 'NONE',  ( -1.939282332474665305, -2.946842880316514979, 0.03118749810191574420 ) ) ;
#9934=CARTESIAN_POINT ( 'NONE',  ( -1.580259682937507515, 0.1018956540318726595, -0.04477369844321319597 ) ) ;
#9937=CARTESIAN_POINT ( 'NONE',  ( -1.509677571405407148, 0.2301488344313167012, 0.03937007874015747977 ) ) ;
#9938=AXIS2_PLACEMENT_3D ( 'NONE', #11864, #1137, #4732 ) ;
#9940=CARTESIAN_POINT ( 'NONE',  ( -1.880307312777807827, -2.920775457401061814, -0.02280129370432555300 ) ) ;
#9943=VERTEX_POINT ( 'NONE', #766 ) ;
#9949=AXIS2_PLACEMENT_3D ( 'NONE', #11694, #8000, #11773 ) ;
#9957=CARTESIAN_POINT ( 'NONE',  ( -1.185589860597406675, 0.3351407497376039935, 0.05695314934232943715 ) ) ;
#9958=CARTESIAN_POINT ( 'NONE',  ( -1.871969607273682001, -2.941194614679324637, -0.05413282885976344189 ) ) ;
#9959=VERTEX_POINT ( 'NONE', #12528 ) ;
#9960=CARTESIAN_POINT ( 'NONE',  ( -2.073793831555620137, -2.576344762739053884, -0.1326668340855626793 ) ) ;
#9961=CARTESIAN_POINT ( 'NONE',  ( -1.496171808639726875, 0.2144740403064262779, -0.03937007874015747977 ) ) ;
#9964=ORIENTED_EDGE ( 'NONE', *, *, #8925, .F. ) ;
#9966=EDGE_LOOP ( 'NONE', ( #4550, #11054, #2491, #10608 ) ) ;
#9967=CIRCLE ( 'NONE', #8465, 0.01968503937007875723 ) ;
#9968=CARTESIAN_POINT ( 'NONE',  ( -0.3441669734936866343, 2.010494531933507467, 0.05905511811023622659 ) ) ;
#9971=CARTESIAN_POINT ( 'NONE',  ( -1.527714331928839098, 0.2380340132385416752, -0.03937007874015747977 ) ) ;
#9972=CARTESIAN_POINT ( 'NONE',  ( -0.004184981454871861475, -0.1778800751599175500, -0.007038468095567116702 ) ) ;
#9980=VERTEX_POINT ( 'NONE', #7664 ) ;
#9985=CARTESIAN_POINT ( 'NONE',  ( -0.06997329305369037744, 0.1451708428228665193, -0.05905511811023622659 ) ) ;
#9987=CARTESIAN_POINT ( 'NONE',  ( -1.400886410084237976, -0.004134161352976360726, 0.05905511811021026125 ) ) ;
#9990=CARTESIAN_POINT ( 'NONE',  ( -1.596030944582063960, 0.1136756404979307328, 0.04477369844320258641 ) ) ;
#9991=DIRECTION ( 'NONE',  ( -0.000000000000000000, 0.000000000000000000, 1.000000000000000000 ) ) ;
#9995=VERTEX_POINT ( 'NONE', #6627 ) ;
#9996=VERTEX_POINT ( 'NONE', #1720 ) ;
#9998=CARTESIAN_POINT ( 'NONE',  ( -1.959271706435208760, -2.897791574176610485, 0.1046970101888178434 ) ) ;
#10005=CARTESIAN_POINT ( 'NONE',  ( -0.002500327830563101039, -0.1605493263772690415, 0.000000000000000000 ) ) ;
#10007=DIRECTION ( 'NONE',  ( -0.000000000000000000, -0.000000000000000000, -1.000000000000000000 ) ) ;
#10011=ORIENTED_EDGE ( 'NONE', *, *, #5234, .F. ) ;
#10015=CARTESIAN_POINT ( 'NONE',  ( -1.401202394148545194, -0.004217627448835788682, -0.05905511811023622659 ) ) ;
#10017=CARTESIAN_POINT ( 'NONE',  ( -2.184126211765464287, -1.725292181286298021, 0.08417626406393743932 ) ) ;
#10018=FACE_OUTER_BOUND ( 'NONE', #6738, .T. ) ;
#10021=CARTESIAN_POINT ( 'NONE',  ( -1.902950105202808606, -2.935536217473399212, -0.06922576094222421261 ) ) ;
#10025=EDGE_CURVE ( 'NONE', #579, #9996, #6419, .T. ) ;
#10026=CARTESIAN_POINT ( 'NONE',  ( -1.415146647999188767, -0.009757455497112661746, -0.06578125416968487460 ) ) ;
#10028=VERTEX_POINT ( 'NONE', #10017 ) ;
#10031=VERTEX_POINT ( 'NONE', #12992 ) ;
#10032=DIRECTION ( 'NONE',  ( 1.000000000000000000, 0.000000000000000000, 0.000000000000000000 ) ) ;
#10036=CARTESIAN_POINT ( 'NONE',  ( -1.596030944582063960, 0.1136756404979308160, 0.05905511811023622659 ) ) ;
#10055=B_SPLINE_CURVE_WITH_KNOTS ( 'NONE', 3,
 ( #2535, #9688, #14375, #2615, #1455, #4891, #13347, #6132 ),
 .UNSPECIFIED., .F., .F.,
 ( 4, 2, 2, 4 ),
 ( 0.000000000000000000, 0.0004593534821998672391, 0.0009187069643997344782, 0.001837413928799469390 ),
 .UNSPECIFIED. ) ;
#10061=ADVANCED_FACE ( 'NONE', ( #8131 ), #2178, .T. ) ;
#10065=CARTESIAN_POINT ( 'NONE',  ( -1.951481176069858270, -2.917150509235289846, -0.07712466264118481019 ) ) ;
#10067=CARTESIAN_POINT ( 'NONE',  ( -1.990389617432203551, -2.816408247477061089, -0.1718103083736243208 ) ) ;
#10068=DIRECTION ( 'NONE',  ( -0.000000000000000000, -2.212657494868377674E-16, -1.000000000000000000 ) ) ;
#10070=CARTESIAN_POINT ( 'NONE',  ( -1.879797169039889582, -2.922016187845676960, -0.01134394994210854990 ) ) ;
#10072=CARTESIAN_POINT ( 'NONE',  ( -2.084730511138506159, -1.679593886630597277, -0.08366141732295870326 ) ) ;
#10081=VERTEX_POINT ( 'NONE', #9475 ) ;
#10082=CARTESIAN_POINT ( 'NONE',  ( -1.417043596213071632, -0.04217320660662462334, -0.06809929043877624433 ) ) ;
#10093=DIRECTION ( 'NONE',  ( 1.000000000000000000, 0.000000000000000000, 0.000000000000000000 ) ) ;
#10094=CARTESIAN_POINT ( 'NONE',  ( -1.180847381073178770, 0.3433074774414748287, 0.04453711288976135857 ) ) ;
#10095=CARTESIAN_POINT ( 'NONE',  ( -1.903002266451024216, -2.935391651063040008, 0.06956102793678921314 ) ) ;
#10097=FACE_OUTER_BOUND ( 'NONE', #12198, .T. ) ;
#10098=ORIENTED_EDGE ( 'NONE', *, *, #14036, .T. ) ;
#10102=ADVANCED_FACE ( 'NONE', ( #4519 ), #11898, .T. ) ;
#10105=ORIENTED_EDGE ( 'NONE', *, *, #7498, .F. ) ;
#10108=EDGE_CURVE ( 'NONE', #579, #13379, #9463, .T. ) ;
#10111=CARTESIAN_POINT ( 'NONE',  ( -1.527714331928839098, 0.2380340132385416752, 0.03937007874015747977 ) ) ;
#10123=CARTESIAN_POINT ( 'NONE',  ( -1.417802900492933560, -0.04287136159519130962, -0.06853082236355059753 ) ) ;
#10134=CARTESIAN_POINT ( 'NONE',  ( -1.574484809660414042, 0.1100025355989073528, 0.06175692796217682051 ) ) ;
#10135=SHAPE_DEFINITION_REPRESENTATION ( #5766, #12105 ) ;
#10136=DIRECTION ( 'NONE',  ( 0.000000000000000000, 0.000000000000000000, -1.000000000000000000 ) ) ;
#10142=AXIS2_PLACEMENT_3D ( 'NONE', #5259, #9991, #13750 ) ;
#10147=ORIENTED_EDGE ( 'NONE', *, *, #2735, .T. ) ;
#10152=VECTOR ( 'NONE', #3586, 39.37007874015748143 ) ;
#10154=CARTESIAN_POINT ( 'NONE',  ( -1.994705189605018303, -2.804563710229789564, 0.1744288432568320280 ) ) ;
#10156=AXIS2_PLACEMENT_3D ( 'NONE', #9289, #11801, #14151 ) ;
#10164=AXIS2_PLACEMENT_3D ( 'NONE', #10305, #6699, #13920 ) ;
#10166=EDGE_CURVE ( 'NONE', #880, #1514, #2942, .T. ) ;
#10168=ORIENTED_EDGE ( 'NONE', *, *, #7027, .T. ) ;
#10170=EDGE_LOOP ( 'NONE', ( #11753, #9281, #13999, #6091 ) ) ;
#10181=EDGE_CURVE ( 'NONE', #3768, #4146, #4688, .T. ) ;
#10186=( BOUNDED_SURFACE ( )  B_SPLINE_SURFACE ( 3, 2, ( 
 ( #13303, #10963, #12294 ),
 ( #1554, #6307, #11103 ),
 ( #9957, #7570, #8767 ),
 ( #2016, #5382, #14881 ),
 ( #9008, #5292, #10094 ),
 ( #13617, #4141, #5463 ) ),
 .UNSPECIFIED., .F., .F., .T. ) 
 B_SPLINE_SURFACE_WITH_KNOTS ( ( 4, 2, 4 ),
 ( 3, 3 ),
 ( -3.623019766863768071E-05, 0.0007449614524472654561, 0.001526153102563168606 ),
 ( 0.000000000000000000, 1.000000000000000000 ),
 .UNSPECIFIED. ) 
 GEOMETRIC_REPRESENTATION_ITEM ( )  RATIONAL_B_SPLINE_SURFACE ( (
 ( 1.000000000000000000, 1.000000000000000000, 1.000000000000000000),
 ( 1.000000000000000000, 1.000000656565393609, 1.000000000000000000),
 ( 1.000000000000000000, 0.9999739034943005977, 1.000000000000000000),
 ( 1.000000000000000000, 0.9999216474068165494, 1.000000000000000000),
 ( 1.000000000000000000, 0.9998986130898321889, 1.000000000000000000),
 ( 1.000000000000000000, 0.9998995914418479236, 1.000000000000000000) ) ) 
 REPRESENTATION_ITEM ( '' )  SURFACE ( )  );
#10192=AXIS2_PLACEMENT_3D ( 'NONE', #7753, #8152, #13165 ) ;
#10197=AXIS2_PLACEMENT_3D ( 'NONE', #14196, #12720, #8163 ) ;
#10210=ORIENTED_EDGE ( 'NONE', *, *, #10665, .F. ) ;
#10222=CARTESIAN_POINT ( 'NONE',  ( -2.068647409231313183, -2.591269129772357349, -0.1345927733208679422 ) ) ;
#10226=ORIENTED_EDGE ( 'NONE', *, *, #15345, .F. ) ;
#10230=EDGE_CURVE ( 'NONE', #13695, #2668, #217, .T. ) ;
#10234=CARTESIAN_POINT ( 'NONE',  ( -1.996856552776540505, -2.798603954469058852, 0.1754249698848522609 ) ) ;
#10236=CARTESIAN_POINT ( 'NONE',  ( -1.971194147208129355, -2.816470572534745198, -0.1716880295712622795 ) ) ;
#10240=CARTESIAN_POINT ( 'NONE',  ( -2.046873694507677754, -2.382074652208439058, -0.1339202096237949169 ) ) ;
#10250=CARTESIAN_POINT ( 'NONE',  ( -1.293236445124221312, 0.1355266887446167634, 0.03937007874015747977 ) ) ;
#10252=CARTESIAN_POINT ( 'NONE',  ( -1.926777348550824165, -2.867314143461890730, -0.1500590184085016932 ) ) ;
#10257=ORIENTED_EDGE ( 'NONE', *, *, #10687, .F. ) ;
#10265=CYLINDRICAL_SURFACE ( 'NONE', #9200, 0.01968503937007875723 ) ;
#10272=CARTESIAN_POINT ( 'NONE',  ( -1.063205505495480097, 0.7941372572243097228, 0.03937007874015747977 ) ) ;
#10273=EDGE_LOOP ( 'NONE', ( #5896, #12441, #13016, #207 ) ) ;
#10297=CARTESIAN_POINT ( 'NONE',  ( -1.973162713238899135, -2.810427108646321503, 0.1731293751518992452 ) ) ;
#10305=CARTESIAN_POINT ( 'NONE',  ( -1.431036756819011213, -0.02829858486107876200, 0.1968503937007874127 ) ) ;
#10311=DIRECTION ( 'NONE',  ( 1.000000000000000000, 0.000000000000000000, 0.000000000000000000 ) ) ;
#10314=CARTESIAN_POINT ( 'NONE',  ( -1.276200637803905691, -0.1988000726501942539, -0.03937007874015747977 ) ) ;
#10316=DIRECTION ( 'NONE',  ( -1.000000000000000000, 0.000000000000000000, -9.020562075079388813E-13 ) ) ;
#10320=CARTESIAN_POINT ( 'NONE',  ( -1.592395536721566751, 0.1185427911281785041, 0.04121422034918794525 ) ) ;
#10324=ORIENTED_EDGE ( 'NONE', *, *, #9143, .T. ) ;
#10329=AXIS2_PLACEMENT_3D ( 'NONE', #7015, #3731, #1373 ) ;
#10331=FACE_OUTER_BOUND ( 'NONE', #2800, .T. ) ;
#10336=LINE ( 'NONE', #15126, #9100 ) ;
#10341=DIRECTION ( 'NONE',  ( -0.8011800915434506010, 0.5984233124757325495, 0.000000000000000000 ) ) ;
#10345=AXIS2_PLACEMENT_3D ( 'NONE', #6212, #5189, #8566 ) ;
#10351=CARTESIAN_POINT ( 'NONE',  ( -0.02641567992992046449, 0.1724028871747071145, 1.853431881210122409E-17 ) ) ;
#10360=DIRECTION ( 'NONE',  ( -0.000000000000000000, -0.000000000000000000, -1.000000000000000000 ) ) ;
#10366=CARTESIAN_POINT ( 'NONE',  ( -1.879669382776355979, -2.922326502959081029, -0.005509842852737917643 ) ) ;
#10376=CIRCLE ( 'NONE', #3627, 0.03937007874015751446 ) ;
#10379=FACE_OUTER_BOUND ( 'NONE', #5322, .T. ) ;
#10385=EDGE_CURVE ( 'NONE', #15252, #9785, #2893, .T. ) ;
#10391=DIRECTION ( 'NONE',  ( 0.8144815189573203495, -0.5801894994542524664, -1.283760644411384396E-16 ) ) ;
#10392=CARTESIAN_POINT ( 'NONE',  ( -2.100501784635051550, -1.630597114118274460, -0.1033464566929128137 ) ) ;
#10393=VERTEX_POINT ( 'NONE', #7228 ) ;
#10395=ORIENTED_EDGE ( 'NONE', *, *, #3179, .F. ) ;
#10403=CARTESIAN_POINT ( 'NONE',  ( -1.586197524890927024, 0.1268408028905886054, -0.05897664633272541035 ) ) ;
#10405=CARTESIAN_POINT ( 'NONE',  ( -0.08151194962748890827, 0.1637246173173402264, -0.03937007874015747977 ) ) ;
#10406=CARTESIAN_POINT ( 'NONE',  ( -0.3441669734936866343, 2.010494531933507467, 0.03937007874015747977 ) ) ;
#10413=DIRECTION ( 'NONE',  ( 1.224646799147353207E-16, 1.000000000000000000, 0.000000000000000000 ) ) ;
#10422=EDGE_CURVE ( 'NONE', #11956, #10983, #2202, .T. ) ;
#10425=CARTESIAN_POINT ( 'NONE',  ( -1.970947046482191656, -2.817268671564700178, 0.1717492298712584298 ) ) ;
#10438=ORIENTED_EDGE ( 'NONE', *, *, #14895, .T. ) ;
#10456=CARTESIAN_POINT ( 'NONE',  ( -0.2362204724409448231, -0.02638708502139245488, 0.03937007874015747977 ) ) ;
#10462=CARTESIAN_POINT ( 'NONE',  ( -2.755905511811024056, -2.772329397582842248, 0.000000000000000000 ) ) ;
#10470=CARTESIAN_POINT ( 'NONE',  ( -1.389958893394353412, -0.02151193858058574049, 0.06001963939216824889 ) ) ;
#10474=ORIENTED_EDGE ( 'NONE', *, *, #4265, .F. ) ;
#10478=VERTEX_POINT ( 'NONE', #5585 ) ;
#10481=DIRECTION ( 'NONE',  ( 0.000000000000000000, 0.000000000000000000, 1.000000000000000000 ) ) ;
#10482=CARTESIAN_POINT ( 'NONE',  ( -0.02636306718619302325, 0.1724112960300248354, 0.0009221601458071186511 ) ) ;
#10497=CARTESIAN_POINT ( 'NONE',  ( -1.931857757055364777, -2.930757773757384665, 0.08017971412056627833 ) ) ;
#10500=FACE_OUTER_BOUND ( 'NONE', #8995, .T. ) ;
#10505=CARTESIAN_POINT ( 'NONE',  ( -0.07874015748031501505, 0.1442356988431297560, 0.05905511811023622659 ) ) ;
#10515=CARTESIAN_POINT ( 'NONE',  ( -0.005352459137615327503, 0.1648200595001707847, 1.247430111210527045E-16 ) ) ;
#10519=CARTESIAN_POINT ( 'NONE',  ( -1.100415514366371639, -0.04998955061625907220, 0.03937007874015747977 ) ) ;
#10520=CARTESIAN_POINT ( 'NONE',  ( -0.07022707542947256854, -0.1870727099175781838, 0.03937007874015747283 ) ) ;
#10522=CARTESIAN_POINT ( 'NONE',  ( -1.969722513608740178, -2.871257544293922770, -0.1475413299907661346 ) ) ;
#10535=CARTESIAN_POINT ( 'NONE',  ( -2.080881322745466999, -1.632190302820504479, 0.08366141732283424726 ) ) ;
#10537=CARTESIAN_POINT ( 'NONE',  ( -1.897981793197825340, -2.949207328992450083, -0.01172296963439428338 ) ) ;
#10542=LINE ( 'NONE', #15170, #4358 ) ;
#10546=ORIENTED_EDGE ( 'NONE', *, *, #7027, .F. ) ;
#10548=ORIENTED_EDGE ( 'NONE', *, *, #4247, .T. ) ;
#10550=ADVANCED_FACE ( 'NONE', ( #192 ), #1504, .T. ) ;
#10552=CARTESIAN_POINT ( 'NONE',  ( -0.01753362615437764269, 0.1513390073937369296, 0.03062283071528665995 ) ) ;
#10553=FACE_OUTER_BOUND ( 'NONE', #4044, .T. ) ;
#10556=ORIENTED_EDGE ( 'NONE', *, *, #9901, .T. ) ;
#10557=DIRECTION ( 'NONE',  ( -0.000000000000000000, -0.000000000000000000, -1.000000000000000000 ) ) ;
#10565=ORIENTED_EDGE ( 'NONE', *, *, #10765, .F. ) ;
#10568=CARTESIAN_POINT ( 'NONE',  ( -1.938704201247565928, -2.911695145306065324, -0.1100133229241002375 ) ) ;
#10571=CARTESIAN_POINT ( 'NONE',  ( -1.938022636209871363, -2.767800838503367888, 0.1776221991034347969 ) ) ;
#10581=ORIENTED_EDGE ( 'NONE', *, *, #1370, .F. ) ;
#10584=AXIS2_PLACEMENT_3D ( 'NONE', #6135, #9598, #7173 ) ;
#10591=CARTESIAN_POINT ( 'NONE',  ( -1.599593005878032992, 0.1086758623451425237, -0.04860704773263154616 ) ) ;
#10592=CARTESIAN_POINT ( 'NONE',  ( -2.755905511811024056, -2.772329397582842248, -0.1771653543307079026 ) ) ;
#10593=FACE_OUTER_BOUND ( 'NONE', #5767, .T. ) ;
#10594=VECTOR ( 'NONE', #9297, 39.37007874015748143 ) ;
#10596=DIRECTION ( 'NONE',  ( -1.000000000000000000, 0.000000000000000000, 0.000000000000000000 ) ) ;
#10605=CIRCLE ( 'NONE', #10843, 1.885039370078740451 ) ;
#10608=ORIENTED_EDGE ( 'NONE', *, *, #11755, .T. ) ;
#10614=CARTESIAN_POINT ( 'NONE',  ( -1.950289002586781173, -2.794939870759669098, 0.1760869912453440211 ) ) ;
#10616=CARTESIAN_POINT ( 'NONE',  ( -1.957251767100264495, -2.772329397581817734, -0.1771653543307079026 ) ) ;
#10623=DIRECTION ( 'NONE',  ( 1.000000000000000000, 0.000000000000000000, 0.000000000000000000 ) ) ;
#10626=AXIS2_PLACEMENT_3D ( 'NONE', #3307, #11614, #4785 ) ;
#10633=AXIS2_PLACEMENT_3D ( 'NONE', #1439, #14583, #12022 ) ;
#10635=CARTESIAN_POINT ( 'NONE',  ( -1.107198012490790306, -0.06846922848666045502, 0.05905511811023622659 ) ) ;
#10638=DIRECTION ( 'NONE',  ( -0.000000000000000000, 0.000000000000000000, 1.000000000000000000 ) ) ;
#10642=ADVANCED_FACE ( 'NONE', ( #5011 ), #4008, .T. ) ;
#10646=AXIS2_PLACEMENT_3D ( 'NONE', #8557, #8726, #6205 ) ;
#10661=CARTESIAN_POINT ( 'NONE',  ( -1.929649418975808439, -2.791725965709412449, 0.1763356003537114580 ) ) ;
#10663=DIRECTION ( 'NONE',  ( -0.3150766955165275607, 0.9411644975924603473, 0.1222131924708513701 ) ) ;
#10664=B_SPLINE_CURVE_WITH_KNOTS ( 'NONE', 3,
 ( #4829, #9628, #14406, #6068 ),
 .UNSPECIFIED., .F., .F.,
 ( 4, 4 ),
 ( 0.000000000000000000, 0.002383301291214095802 ),
 .UNSPECIFIED. ) ;
#10665=EDGE_CURVE ( 'NONE', #6873, #10081, #3714, .T. ) ;
#10667=CARTESIAN_POINT ( 'NONE',  ( -1.293236445124221312, 0.1355266887446167634, 0.03937007874015747977 ) ) ;
#10669=ORIENTED_EDGE ( 'NONE', *, *, #2711, .F. ) ;
#10673=DIMENSIONAL_EXPONENTS ( 1.000000000000000000, 0.000000000000000000, 0.000000000000000000, 0.000000000000000000, 0.000000000000000000, 0.000000000000000000, 0.000000000000000000 ) ;
#10675=VECTOR ( 'NONE', #1918, 39.37007874015748143 ) ;
#10680=CARTESIAN_POINT ( 'NONE',  ( -1.598024100230236444, 0.1108858885491604135, -0.04651107584905353476 ) ) ;
#10682=DIRECTION ( 'NONE',  ( 1.000000000000000000, 0.000000000000000000, -9.159339953157533381E-13 ) ) ;
#10685=ORIENTED_EDGE ( 'NONE', *, *, #1076, .T. ) ;
#10687=EDGE_CURVE ( 'NONE', #7239, #2402, #9967, .T. ) ;
#10692=ORIENTED_EDGE ( 'NONE', *, *, #12770, .F. ) ;
#10694=TOROIDAL_SURFACE ( 'NONE', #10197, 0.05905511811023614333, 0.01968503937007873988 ) ;
#10710=ORIENTED_EDGE ( 'NONE', *, *, #1760, .F. ) ;
#10712=VERTEX_POINT ( 'NONE', #12708 ) ;
#10721=CARTESIAN_POINT ( 'NONE',  ( -1.452763252956527751, -0.05091287232363173737, 0.1033464566929133133 ) ) ;
#10723=DIRECTION ( 'NONE',  ( -0.8180917953313905366, 0.5750876580239416835, 0.000000000000000000 ) ) ;
#10730=CARTESIAN_POINT ( 'NONE',  ( -1.932153213347265197, -2.929935046723639580, -0.08117000303833375729 ) ) ;
#10735=CARTESIAN_POINT ( 'NONE',  ( -2.018747272517074531, -2.567808539723777983, 0.1539156967279681487 ) ) ;
#10737=CARTESIAN_POINT ( 'NONE',  ( -1.953932514027914014, -2.911092722762949059, -0.08698641157505102028 ) ) ;
#10744=ORIENTED_EDGE ( 'NONE', *, *, #7114, .F. ) ;
#10748=CARTESIAN_POINT ( 'NONE',  ( -1.419615703680148000, -0.01226548409420234569, 0.07874015748031495954 ) ) ;
#10750=CARTESIAN_POINT ( 'NONE',  ( -0.3441669734936866343, 2.010494531933507467, 0.05905511811023622659 ) ) ;
#10752=ORIENTED_EDGE ( 'NONE', *, *, #10385, .T. ) ;
#10753=CARTESIAN_POINT ( 'NONE',  ( -1.580080891953811628, 0.1020406297922293176, -0.07874015748031495954 ) ) ;
#10756=CARTESIAN_POINT ( 'NONE',  ( -0.06145017734370220031, -0.1666692956086705812, 0.05763041683086380512 ) ) ;
#10762=VERTEX_POINT ( 'NONE', #9250 ) ;
#10765=EDGE_CURVE ( 'NONE', #1514, #12673, #225, .T. ) ;
#10767=CARTESIAN_POINT ( 'NONE',  ( -1.897873245346056947, -2.949503897763099403, -0.005687192277569496669 ) ) ;
#10770=DIRECTION ( 'NONE',  ( 1.000000000000000000, 0.000000000000000000, 0.000000000000000000 ) ) ;
#10781=CARTESIAN_POINT ( 'NONE',  ( -2.100501784635051550, -1.630597114118274238, -0.1033464566929129386 ) ) ;
#10782=CARTESIAN_POINT ( 'NONE',  ( -1.945459748359986252, -2.745801194614591711, 0.1561691687464105693 ) ) ;
#10785=DIRECTION ( 'NONE',  ( -0.6461174802841006537, 0.7632379718484431086, -1.126465149071359074E-12 ) ) ;
#10787=CARTESIAN_POINT ( 'NONE',  ( -1.398125690441303526, -0.003404927804347070153, 0.05905511811023622659 ) ) ;
#10795=CARTESIAN_POINT ( 'NONE',  ( -2.168820329264121050, -1.823085014281403016, 0.1033464566929129386 ) ) ;
#10798=CARTESIAN_POINT ( 'NONE',  ( -1.253866366384063902, 0.1355266887446167634, -0.03937007874015747977 ) ) ;
#10801=CARTESIAN_POINT ( 'NONE',  ( -1.930616173493556520, -2.788983622150487118, 0.1558567757490539607 ) ) ;
#10806=ORIENTED_EDGE ( 'NONE', *, *, #8453, .T. ) ;
#10816=CARTESIAN_POINT ( 'NONE',  ( -1.606548329185371937, 0.09883514492710566979, -0.06506891156476989069 ) ) ;
#10825=ORIENTED_EDGE ( 'NONE', *, *, #9588, .F. ) ;
#10841=CARTESIAN_POINT ( 'NONE',  ( -1.964126537190518107, -2.749515453455440905, 0.1756903148397124803 ) ) ;
#10843=AXIS2_PLACEMENT_3D ( 'NONE', #13138, #9542, #5994 ) ;
#10846=AXIS2_PLACEMENT_3D ( 'NONE', #2038, #6737, #11526 ) ;
#10848=ORIENTED_EDGE ( 'NONE', *, *, #3697, .T. ) ;
#10849=ORIENTED_EDGE ( 'NONE', *, *, #2420, .F. ) ;
#10859=DIRECTION ( 'NONE',  ( -0.7666137478421605200, 0.6421085279136201640, 0.000000000000000000 ) ) ;
#10877=DIRECTION ( 'NONE',  ( 0.000000000000000000, -0.000000000000000000, -1.000000000000000000 ) ) ;
#10878=CARTESIAN_POINT ( 'NONE',  ( -1.602629991056265801, 0.1043896402809140617, 0.05327537141218099959 ) ) ;
#10885=CARTESIAN_POINT ( 'NONE',  ( -1.904888967627721863, -2.858900249894324119, 0.1271124878405535397 ) ) ;
#10887=CARTESIAN_POINT ( 'NONE',  ( -1.951376757933277917, -2.917415184539839945, 0.07729597236840124452 ) ) ;
#10895=AXIS2_PLACEMENT_3D ( 'NONE', #13519, #13290, #12129 ) ;
#10898=B_SPLINE_CURVE_WITH_KNOTS ( 'NONE', 3,
 ( #8906, #1768, #13823, #3256, #754, #7870 ),
 .UNSPECIFIED., .F., .F.,
 ( 4, 2, 4 ),
 ( 1.390486644391990834E-17, 0.01145241905537470843, 0.02290483811074940299 ),
 .UNSPECIFIED. ) ;
#10905=CARTESIAN_POINT ( 'NONE',  ( -0.08151194962748890827, 0.1637246173173402264, -0.03937007874015747977 ) ) ;
#10911=CARTESIAN_POINT ( 'NONE',  ( -0.07635964791965738074, -0.1878198040935885327, 0.03937007874015747977 ) ) ;
#10917=CARTESIAN_POINT ( 'NONE',  ( -1.588328939002294549, 0.1239872266390840139, -0.03937007874015752834 ) ) ;
#10919=DIRECTION ( 'NONE',  ( -0.000000000000000000, 0.000000000000000000, 1.000000000000000000 ) ) ;
#10921=CARTESIAN_POINT ( 'NONE',  ( -1.415143637612825467, -0.009756740514708567291, 0.06578375869326227865 ) ) ;
#10927=CARTESIAN_POINT ( 'NONE',  ( -1.387704745771440207, -0.02010536753476152225, 0.03937007874015747977 ) ) ;
#10932=EDGE_LOOP ( 'NONE', ( #10825, #7358, #1142, #12807 ) ) ;
#10934=EDGE_CURVE ( 'NONE', #924, #12712, #2430, .T. ) ;
#10936=AXIS2_PLACEMENT_3D ( 'NONE', #11707, #4558, #8178 ) ;
#10942=CARTESIAN_POINT ( 'NONE',  ( -1.100415514366371195, -0.04998955061625851709, -0.03937007874015747977 ) ) ;
#10943=DIRECTION ( 'NONE',  ( 1.000000000000000000, 0.000000000000000000, 0.000000000000000000 ) ) ;
#10945=DIRECTION ( 'NONE',  ( 1.000000000000000000, 0.000000000000000000, 0.000000000000000000 ) ) ;
#10951=AXIS2_PLACEMENT_3D ( 'NONE', #9934, #14626, #292 ) ;
#10959=ADVANCED_FACE ( 'NONE', ( #12232, #3993, #5063 ), #5226, .T. ) ;
#10963=CARTESIAN_POINT ( 'NONE',  ( -1.190198933766852152, 0.3259758027579607309, 0.05905511811023622659 ) ) ;
#10965=CARTESIAN_POINT ( 'NONE',  ( -1.913690542245347626, -2.905358729579917476, -0.1176961216033449859 ) ) ;
#10966=EDGE_LOOP ( 'NONE', ( #12873, #7158, #8073, #12753 ) ) ;
#10967=CARTESIAN_POINT ( 'NONE',  ( -1.947386292800456387, -2.927198029129052692, 0.05659550234681299391 ) ) ;
#10982=CARTESIAN_POINT ( 'NONE',  ( -0.05270315828015969400, 0.1680450278838720168, -0.03205052537796104772 ) ) ;
#10983=VERTEX_POINT ( 'NONE', #13393 ) ;
#10984=CARTESIAN_POINT ( 'NONE',  ( -1.398495881576244493, -0.02731002314121875815, -0.08366141732283458032 ) ) ;
#10986=FACE_OUTER_BOUND ( 'NONE', #9425, .T. ) ;
#10990=ORIENTED_EDGE ( 'NONE', *, *, #8495, .F. ) ;
#10993=VERTEX_POINT ( 'NONE', #8698 ) ;
#11007=EDGE_LOOP ( 'NONE', ( #3412, #13464, #12903, #11936 ) ) ;
#11008=CARTESIAN_POINT ( 'NONE',  ( -2.065879816533417124, -2.386386741922390531, -0.1342549684437943924 ) ) ;
#11009=CARTESIAN_POINT ( 'NONE',  ( -1.941126393898428226, -2.942417223422608252, -0.04999253742952749352 ) ) ;
#11010=CARTESIAN_POINT ( 'NONE',  ( -2.163017314575554462, -1.630597114118274238, 0.08366141732283423338 ) ) ;
#11016=DIRECTION ( 'NONE',  ( 1.000000000000000000, 0.000000000000000000, 0.000000000000000000 ) ) ;
#11025=FACE_OUTER_BOUND ( 'NONE', #11007, .T. ) ;
#11026=DIRECTION ( 'NONE',  ( -0.000000000000000000, -2.212657494868377674E-16, -1.000000000000000000 ) ) ;
#11028=DIRECTION ( 'NONE',  ( 1.000000000000000000, 0.000000000000000000, 0.000000000000000000 ) ) ;
#11030=CARTESIAN_POINT ( 'NONE',  ( -1.898519999023877469, -2.947734826116759965, -0.02574579424190774277 ) ) ;
#11034=DIRECTION ( 'NONE',  ( 1.000000000000000000, 0.000000000000000000, 8.673617379884028570E-16 ) ) ;
#11043=CARTESIAN_POINT ( 'NONE',  ( -0.007978440472143270498, -0.1611588996411620900, -0.01594766689393424530 ) ) ;
#11050=ADVANCED_FACE ( 'NONE', ( #8528 ), #10186, .F. ) ;
#11054=ORIENTED_EDGE ( 'NONE', *, *, #13960, .T. ) ;
#11068=ORIENTED_EDGE ( 'NONE', *, *, #14675, .F. ) ;
#11069=ORIENTED_EDGE ( 'NONE', *, *, #1370, .T. ) ;
#11077=CARTESIAN_POINT ( 'NONE',  ( -1.951331694435471498, -2.917526071354513029, 0.07709592686080572743 ) ) ;
#11084=CARTESIAN_POINT ( 'NONE',  ( -1.882371321102604078, -2.915739816777954463, 0.04555328826220117477 ) ) ;
#11093=AXIS2_PLACEMENT_3D ( 'NONE', #4742, #210, #13342 ) ;
#11094=CARTESIAN_POINT ( 'NONE',  ( -1.411972059858401574, -0.03772986244363892711, -0.05403728031753547711 ) ) ;
#11102=CARTESIAN_POINT ( 'NONE',  ( -2.010991777528384983, -2.758467574604075434, 0.1561691687464110412 ) ) ;
#11103=CARTESIAN_POINT ( 'NONE',  ( -1.187740243782755556, 0.3305209984255413902, 0.05905511811023626823 ) ) ;
#11104=CARTESIAN_POINT ( 'NONE',  ( -1.881708026547704860, -2.917360643372564066, -0.03975124946893780070 ) ) ;
#11106=CARTESIAN_POINT ( 'NONE',  ( -2.168819294506413087, -1.823050691322769090, -0.1033464566929129108 ) ) ;
#11114=AXIS2_PLACEMENT_3D ( 'NONE', #3526, #6010, #13 ) ;
#11119=EDGE_CURVE ( 'NONE', #1797, #9786, #13935, .T. ) ;
#11121=VECTOR ( 'NONE', #13814, 39.37007874015748854 ) ;
#11128=CARTESIAN_POINT ( 'NONE',  ( -0.02281238468002976319, -0.1806356120156163148, -0.007039490205851098130 ) ) ;
#11131=SPHERICAL_SURFACE ( 'NONE', #4334, 0.01968503937007873988 ) ;
#11133=LINE ( 'NONE', #13796, #8705 ) ;
#11137=AXIS2_PLACEMENT_3D ( 'NONE', #10462, #14293, #9525 ) ;
#11149=CARTESIAN_POINT ( 'NONE',  ( -1.403610094870331393, -0.004984718095728941228, 0.05942212872828700476 ) ) ;
#11160=ORIENTED_EDGE ( 'NONE', *, *, #10665, .T. ) ;
#11166=CARTESIAN_POINT ( 'NONE',  ( -1.938752474876189069, -2.948113922056589065, -0.02541044617147641266 ) ) ;
#11169=CARTESIAN_POINT ( 'NONE',  ( -1.180847381051866485, 0.3433074774306730803, -0.03937007874015747977 ) ) ;
#11170=CARTESIAN_POINT ( 'NONE',  ( -1.995574481745110651, -2.802154287413662459, -0.1558670771739966432 ) ) ;
#11174=CARTESIAN_POINT ( 'NONE',  ( -0.3441669734936866343, 2.010494531933507467, -0.05905511811023622659 ) ) ;
#11189=DIRECTION ( 'NONE',  ( 0.000000000000000000, -1.000000000000000000, 0.000000000000000000 ) ) ;
#11196=CARTESIAN_POINT ( 'NONE',  ( -1.875101537351226311, -2.933668943012675001, 0.07363248663697015417 ) ) ;
#11202=CARTESIAN_POINT ( 'NONE',  ( -1.416791279958480976, -0.01064335357298143957, -0.06799382560225487870 ) ) ;
#11206=ORIENTED_EDGE ( 'NONE', *, *, #13102, .T. ) ;
#11209=LINE ( 'NONE', #7121, #6109 ) ;
#11229=B_SPLINE_CURVE_WITH_KNOTS ( 'NONE', 3,
 ( #5500, #3008, #6588, #13813, #10222, #14835 ),
 .UNSPECIFIED., .F., .F.,
 ( 4, 2, 4 ),
 ( 0.002383301291214095802, 0.01571728647480164637, 0.02905127165838919390 ),
 .UNSPECIFIED. ) ;
#11230=CARTESIAN_POINT ( 'NONE',  ( -1.960442862720704005, -2.701045185997201781, 0.1503165316663955531 ) ) ;
#11234=ADVANCED_FACE ( 'NONE', ( #3514 ), #11901, .T. ) ;
#11236=FACE_OUTER_BOUND ( 'NONE', #2328, .T. ) ;
#11238=CARTESIAN_POINT ( 'NONE',  ( -1.992382107315058271, -2.752050336136262931, 0.1561691687464115408 ) ) ;
#11245=CARTESIAN_POINT ( 'NONE',  ( -1.927778962255358053, -2.941963733592956487, -0.05151121078832996553 ) ) ;
#11248=CARTESIAN_POINT ( 'NONE',  ( -1.984789438093313541, -2.774065754419840601, -0.1775759736344397766 ) ) ;
#11252=CARTESIAN_POINT ( 'NONE',  ( -1.884728029847772879, -2.909954979002622011, 0.06162763431411907855 ) ) ;
#11261=CARTESIAN_POINT ( 'NONE',  ( -1.389961391698828708, -0.02151349750585865306, -0.06002070848877767706 ) ) ;
#11265=CARTESIAN_POINT ( 'NONE',  ( -2.111626822439223172, -2.421545435136619684, 0.1175637245596499597 ) ) ;
#11270=CARTESIAN_POINT ( 'NONE',  ( -1.908239321022362489, -2.920800340391614291, -0.09749645815890824185 ) ) ;
#11272=CARTESIAN_POINT ( 'NONE',  ( -2.163017314575554462, -1.630597114118274238, -0.1033464566929129386 ) ) ;
#11279=CYLINDRICAL_SURFACE ( 'NONE', #5833, 0.01968503937007875723 ) ;
#11282=CARTESIAN_POINT ( 'NONE',  ( -0.06997480235680504645, -0.1674783595965826377, -0.05905511811023622659 ) ) ;
#11289=ORIENTED_EDGE ( 'NONE', *, *, #13764, .F. ) ;
#11293=CARTESIAN_POINT ( 'NONE',  ( -0.07500546397816693078, 0.1646499958011362896, -0.03937007824588655003 ) ) ;
#11301=DIRECTION ( 'NONE',  ( -1.000000000000000000, 0.000000000000000000, 0.000000000000000000 ) ) ;
#11309=CARTESIAN_POINT ( 'NONE',  ( -1.954244229570128111, -2.867204336101874418, 0.1501281538326428022 ) ) ;
#11313=CARTESIAN_POINT ( 'NONE',  ( -2.010991777528384095, -2.758467574604078543, -0.1561691687464109024 ) ) ;
#11316=CARTESIAN_POINT ( 'NONE',  ( -1.883711820814927274, -2.912463908419459901, -0.05618017532687354099 ) ) ;
#11318=CARTESIAN_POINT ( 'NONE',  ( -2.090218168050184122, -1.822025907981831727, -0.08562854774378582390 ) ) ;
#11338=EDGE_CURVE ( 'NONE', #10031, #13899, #8831, .T. ) ;
#11341=CARTESIAN_POINT ( 'NONE',  ( -1.945459748359985142, -2.745801194614594376, -0.1561691687464109302 ) ) ;
#11345=CARTESIAN_POINT ( 'NONE',  ( -1.596030944582063960, 0.1136756404979307328, 0.04477369844320258641 ) ) ;
#11355=EDGE_CURVE ( 'NONE', #14453, #12673, #7821, .T. ) ;
#11363=CIRCLE ( 'NONE', #14383, 0.2303149606299203511 ) ;
#11367=CARTESIAN_POINT ( 'NONE',  ( -0.02015118043373552090, -0.1802412052441877965, 0.0009776059035733464502 ) ) ;
#11369=DIRECTION ( 'NONE',  ( 1.000000000000000000, -1.813574543066661640E-15, 0.000000000000000000 ) ) ;
#11372=CARTESIAN_POINT ( 'NONE',  ( -1.180847381051866485, 0.3433074774306730803, -0.03937007874015747977 ) ) ;
#11373=EDGE_LOOP ( 'NONE', ( #14308, #13027, #6261, #10011, #9380, #11675 ) ) ;
#11377=ORIENTED_EDGE ( 'NONE', *, *, #6942, .F. ) ;
#11382=CARTESIAN_POINT ( 'NONE',  ( -2.042401582839019181, -2.380935903742845028, 0.1158648208881124103 ) ) ;
#11383=DIRECTION ( 'NONE',  ( -0.000000000000000000, -0.000000000000000000, -1.000000000000000000 ) ) ;
#11388=CARTESIAN_POINT ( 'NONE',  ( -1.078976767140036319, 0.8059172436903675463, -0.03937007874015747977 ) ) ;
#11391=AXIS2_PLACEMENT_3D ( 'NONE', #6800, #3289, #9021 ) ;
#11392=AXIS2_PLACEMENT_3D ( 'NONE', #14320, #940, #10723 ) ;
#11400=AXIS2_PLACEMENT_3D ( 'NONE', #8990, #4270, #4120 ) ;
#11402=VECTOR ( 'NONE', #14258, 39.37007874015748143 ) ;
#11404=CARTESIAN_POINT ( 'NONE',  ( -1.997525977910308947, -2.796737313284686000, 0.1565702274318891973 ) ) ;
#11405=AXIS2_PLACEMENT_3D ( 'NONE', #10942, #10785, #11900 ) ;
#11407=CARTESIAN_POINT ( 'NONE',  ( -1.994705048877226661, -2.804564119885714302, -0.1744288896405255807 ) ) ;
#11415=ORIENTED_EDGE ( 'NONE', *, *, #9928, .T. ) ;
#11431=CARTESIAN_POINT ( 'NONE',  ( -1.915562887302063144, -2.830608845893845871, -0.1438018468321328736 ) ) ;
#11433=CARTESIAN_POINT ( 'NONE',  ( -0.3441669734936866343, 2.010494531933507467, -0.03937007874015747977 ) ) ;
#11440=AXIS2_PLACEMENT_3D ( 'NONE', #3807, #7188, #13451 ) ;
#11441=EDGE_CURVE ( 'NONE', #2439, #4146, #9082, .T. ) ;
#11450=AXIS2_PLACEMENT_3D ( 'NONE', #14400, #2484, #9776 ) ;
#11453=CARTESIAN_POINT ( 'NONE',  ( -1.945459748359986252, -2.745801194614591711, 0.1561691687464105693 ) ) ;
#11456=CARTESIAN_POINT ( 'NONE',  ( -1.387704745771440207, -0.02010536753476144939, -0.03937007874015747977 ) ) ;
#11457=CARTESIAN_POINT ( 'NONE',  ( -1.190198933766853706, 0.3259758027579612860, 0.05905511811023622659 ) ) ;
#11462=EDGE_CURVE ( 'NONE', #4326, #9812, #7075, .T. ) ;
#11463=ORIENTED_EDGE ( 'NONE', *, *, #128, .T. ) ;
#11481=AXIS2_PLACEMENT_3D ( 'NONE', #12576, #4264, #5441 ) ;
#11488=CARTESIAN_POINT ( 'NONE',  ( -1.961602614639095687, -2.845484579323528163, 0.1618271791655376268 ) ) ;
#11493=CARTESIAN_POINT ( 'NONE',  ( -2.100301733797227399, -2.106182698134460907, -0.1158666453195839885 ) ) ;
#11495=VERTEX_POINT ( 'NONE', #9937 ) ;
#11497=ORIENTED_EDGE ( 'NONE', *, *, #634, .T. ) ;
#11503=DIRECTION ( 'NONE',  ( 1.000000000000000000, 0.000000000000000000, 0.000000000000000000 ) ) ;
#11505=CARTESIAN_POINT ( 'NONE',  ( -1.908371742851994624, -2.849778903878224412, -0.1333857941085078158 ) ) ;
#11513=VERTEX_POINT ( 'NONE', #6464 ) ;
#11522=DIRECTION ( 'NONE',  ( 0.000000000000000000, 0.000000000000000000, -1.000000000000000000 ) ) ;
#11526=DIRECTION ( 'NONE',  ( -2.775557561562891351E-14, 0.5840537863392681883, 0.8117149589990099168 ) ) ;
#11527=EDGE_LOOP ( 'NONE', ( #11581, #2213, #4423, #13002 ) ) ;
#11528=CARTESIAN_POINT ( 'NONE',  ( -1.607606114292111199, 0.09732815221480045631, -0.07874015748031495954 ) ) ;
#11533=CARTESIAN_POINT ( 'NONE',  ( -1.417802900492933782, -0.04287136159519135126, 0.1968503937007874127 ) ) ;
#11536=CARTESIAN_POINT ( 'NONE',  ( -0.02479723250354459035, 0.1726834024554402824, 0.005447726382808077729 ) ) ;
#11537=DIRECTION ( 'NONE',  ( 0.000000000000000000, 1.000000000000000000, 2.212657494868377674E-16 ) ) ;
#11544=DIRECTION ( 'NONE',  ( 0.8011800915435203230, -0.5984233124756390687, 0.000000000000000000 ) ) ;
#11546=ORIENTED_EDGE ( 'NONE', *, *, #14977, .F. ) ;
#11550=ORIENTED_EDGE ( 'NONE', *, *, #3657, .F. ) ;
#11561=CARTESIAN_POINT ( 'NONE',  ( -2.104378079979697169, -1.678226622365109222, -0.1033464566929128137 ) ) ;
#11563=EDGE_CURVE ( 'NONE', #14453, #880, #1833, .T. ) ;
#11567=B_SPLINE_CURVE_WITH_KNOTS ( 'NONE', 3,
 ( #7313, #13650, #8338, #10841 ),
 .UNSPECIFIED., .F., .F.,
 ( 4, 4 ),
 ( 0.01503324949781038346, 0.01563576546786441673 ),
 .UNSPECIFIED. ) ;
#11568=CARTESIAN_POINT ( 'NONE',  ( -1.570493619109623262, 0.1151020441257367272, -0.05905511811023622659 ) ) ;
#11574=CARTESIAN_POINT ( 'NONE',  ( -1.919254730030994338, -2.820607295135873382, -0.1479486526684962999 ) ) ;
#11575=ORIENTED_EDGE ( 'NONE', *, *, #4247, .F. ) ;
#11580=ORIENTED_EDGE ( 'NONE', *, *, #14685, .T. ) ;
#11581=ORIENTED_EDGE ( 'NONE', *, *, #10934, .F. ) ;
#11584=DIRECTION ( 'NONE',  ( 0.000000000000000000, 0.000000000000000000, 1.000000000000000000 ) ) ;
#11585=AXIS2_PLACEMENT_3D ( 'NONE', #15082, #4272, #5516 ) ;
#11588=CARTESIAN_POINT ( 'NONE',  ( -1.947132143286702144, -2.887778429919098500, 0.1348783224627881361 ) ) ;
#11591=CARTESIAN_POINT ( 'NONE',  ( -1.496171808639726653, 0.2144740403064262224, 0.05905511811023622659 ) ) ;
#11600=EDGE_CURVE ( 'NONE', #3964, #15344, #15081, .T. ) ;
#11601=AXIS2_PLACEMENT_3D ( 'NONE', #15051, #6570, #11369 ) ;
#11603=AXIS2_PLACEMENT_3D ( 'NONE', #1509, #6257, #871 ) ;
#11609=CYLINDRICAL_SURFACE ( 'NONE', #9661, 0.03937007874015747977 ) ;
#11614=DIRECTION ( 'NONE',  ( -0.9926610512904576744, -0.1209298856814283729, -0.000000000000000000 ) ) ;
#11616=DIRECTION ( 'NONE',  ( 1.000000000000000000, -1.783360582779902981E-15, 0.000000000000000000 ) ) ;
#11645=CARTESIAN_POINT ( 'NONE',  ( -1.190198933766853706, 0.3259758027579612860, 0.05905511811023622659 ) ) ;
#11648=CARTESIAN_POINT ( 'NONE',  ( -0.07874015748031543138, -0.1682792322177920907, 0.05905511811023622659 ) ) ;
#11659=DIRECTION ( 'NONE',  ( 0.000000000000000000, 0.000000000000000000, -1.000000000000000000 ) ) ;
#11666=CIRCLE ( 'NONE', #5397, 2.814960629921260171 ) ;
#11667=CARTESIAN_POINT ( 'NONE',  ( -1.916688711786504351, -2.827624850986260263, -0.1689233196601243048 ) ) ;
#11675=ORIENTED_EDGE ( 'NONE', *, *, #271, .F. ) ;
#11677=EDGE_LOOP ( 'NONE', ( #2396, #15070, #5826, #9030, #3749 ) ) ;
#11683=CARTESIAN_POINT ( 'NONE',  ( -1.956909830981848453, -2.859374696368682578, -0.1547382899828209646 ) ) ;
#11684=CIRCLE ( 'NONE', #4922, 0.01968503937007875723 ) ;
#11693=ORIENTED_EDGE ( 'NONE', *, *, #5556, .T. ) ;
#11694=CARTESIAN_POINT ( 'NONE',  ( 0.9851651268172137987, -1.725292181286280480, 0.1033464566929129524 ) ) ;
#11704=CARTESIAN_POINT ( 'NONE',  ( -0.01753362615437414548, 0.1513390073936909108, -0.03062283071528134476 ) ) ;
#11707=CARTESIAN_POINT ( 'NONE',  ( -1.591501945092674841, 0.08600752902535303834, 0.1968503937007874127 ) ) ;
#11712=CARTESIAN_POINT ( 'NONE',  ( -1.965820533970300543, -2.881262407559504801, -0.1403303144071717523 ) ) ;
#11722=ORIENTED_EDGE ( 'NONE', *, *, #3722, .F. ) ;
#11733=ADVANCED_FACE ( 'NONE', ( #594, #14782, #14945 ), #8748, .F. ) ;
#11739=ADVANCED_FACE ( 'NONE', ( #461 ), #7380, .T. ) ;
#11746=CARTESIAN_POINT ( 'NONE',  ( -1.568343923620152180, 0.1178486908565802016, -0.05905511811023622659 ) ) ;
#11747=CARTESIAN_POINT ( 'NONE',  ( -1.276200637803905691, -0.1988000726501942539, 0.03937007874015747977 ) ) ;
#11749=CARTESIAN_POINT ( 'NONE',  ( -0.06144837730694100580, 0.1461156186057984141, 0.05762996311186435044 ) ) ;
#11753=ORIENTED_EDGE ( 'NONE', *, *, #4650, .T. ) ;
#11755=EDGE_CURVE ( 'NONE', #4395, #10762, #10898, .T. ) ;
#11758=VERTEX_POINT ( 'NONE', #13683 ) ;
#11759=ORIENTED_EDGE ( 'NONE', *, *, #1698, .T. ) ;
#11764=DIRECTION ( 'NONE',  ( 0.8144815189573203495, -0.5801894994542524664, 1.283760644411384150E-16 ) ) ;
#11767=CARTESIAN_POINT ( 'NONE',  ( -1.185456167499539193, 0.3350708678521160944, -0.05695194461256634227 ) ) ;
#11771=CARTESIAN_POINT ( 'NONE',  ( -1.607347250558628149, 0.09769655912556320099, 0.07190431746647057976 ) ) ;
#11773=DIRECTION ( 'NONE',  ( 0.000000000000000000, 1.000000000000000000, 2.222614453595283597E-16 ) ) ;
#11785=CARTESIAN_POINT ( 'NONE',  ( -0.03213667549430108267, -0.1820030000337380105, 0.02170016096604327621 ) ) ;
#11787=DIRECTION ( 'NONE',  ( -0.8483823383050520528, -0.5293839892290402860, -0.000000000000000000 ) ) ;
#11788=CARTESIAN_POINT ( 'NONE',  ( -1.293236445124221312, 0.1355266887446167634, -0.05905511811023622659 ) ) ;
#11792=ORIENTED_EDGE ( 'NONE', *, *, #3883, .F. ) ;
#11793=VERTEX_POINT ( 'NONE', #817 ) ;
#11801=DIRECTION ( 'NONE',  ( -0.000000000000000000, -0.000000000000000000, -1.000000000000000000 ) ) ;
#11804=DIRECTION ( 'NONE',  ( -0.000000000000000000, 0.000000000000000000, 1.000000000000000000 ) ) ;
#11807=ORIENTED_EDGE ( 'NONE', *, *, #5096, .F. ) ;
#11821=CIRCLE ( 'NONE', #9064, 0.03937007874015747977 ) ;
#11822=EDGE_LOOP ( 'NONE', ( #8416, #12609, #4171, #15309 ) ) ;
#11823=EDGE_CURVE ( 'NONE', #8019, #10712, #13151, .T. ) ;
#11824=ORIENTED_EDGE ( 'NONE', *, *, #13960, .F. ) ;
#11832=CARTESIAN_POINT ( 'NONE',  ( -2.077823265817535514, -2.289991437693742249, 0.1278967700780702654 ) ) ;
#11837=CARTESIAN_POINT ( 'NONE',  ( -1.607606114292110977, 0.09732815221480028978, 0.07528365722483934541 ) ) ;
#11864=CARTESIAN_POINT ( 'NONE',  ( -0.07874015748031543138, -0.1682792322177920907, 0.03937007874015747977 ) ) ;
#11867=AXIS2_PLACEMENT_3D ( 'NONE', #5523, #8216, #5828 ) ;
#11868=ORIENTED_EDGE ( 'NONE', *, *, #5360, .F. ) ;
#11875=DIRECTION ( 'NONE',  ( 1.000000000000000000, 0.000000000000000000, 0.000000000000000000 ) ) ;
#11876=CARTESIAN_POINT ( 'NONE',  ( -1.919773973138744205, -2.887845448549585470, -0.1348206780894404822 ) ) ;
#11885=DIRECTION ( 'NONE',  ( -0.000000000000000000, 0.000000000000000000, 1.000000000000000000 ) ) ;
#11898=CYLINDRICAL_SURFACE ( 'NONE', #7686, 3.169291338582677753 ) ;
#11900=DIRECTION ( 'NONE',  ( 0.7632379718484426645, 0.6461174802841010978, 0.000000000000000000 ) ) ;
#11901=SPHERICAL_SURFACE ( 'NONE', #7565, 0.01968503937007873988 ) ;
#11916=DIRECTION ( 'NONE',  ( 0.5984233124757279976, 0.8011800915434538206, 0.000000000000000000 ) ) ;
#11918=CARTESIAN_POINT ( 'NONE',  ( -1.926054244504965984, -2.946671621383704309, 0.03215668881446384630 ) ) ;
#11923=CARTESIAN_POINT ( 'NONE',  ( -1.941333777923719639, -2.904294378039212976, 0.1187681980620380745 ) ) ;
#11926=CARTESIAN_POINT ( 'NONE',  ( -1.932500704111168366, -2.783628473676827753, 0.1565635629552918073 ) ) ;
#11929=CARTESIAN_POINT ( 'NONE',  ( -2.007203421661559961, -2.769453616915882321, -0.1575868804561089964 ) ) ;
#11935=ORIENTED_EDGE ( 'NONE', *, *, #13651, .T. ) ;
#11936=ORIENTED_EDGE ( 'NONE', *, *, #5167, .F. ) ;
#11943=DIRECTION ( 'NONE',  ( -0.3445509047204711184, -0.9387676358163955515, 0.000000000000000000 ) ) ;
#11945=CARTESIAN_POINT ( 'NONE',  ( -0.06956272065387625325, 0.1654544434110864770, -0.03844121289758908183 ) ) ;
#11956=VERTEX_POINT ( 'NONE', #8560 ) ;
#11960=ADVANCED_FACE ( 'NONE', ( #8796 ), #14875, .T. ) ;
#11972=B_SPLINE_CURVE_WITH_KNOTS ( 'NONE', 3,
 ( #6175, #11929, #4709, #3606, #8302, #7277, #12236, #3827, #13077, #2664, #9496, #8531, #10737, #14335, #5001, #7128, #1195, #5948, #8386, #8611, #2343, #13170, #9796, #1261, #18, #3690, #10967, #10887, #178, #9730, #6088, #13397, #7436, #9652, #7213, #4778, #14266, #5864, #9563, #2434 ),
 .UNSPECIFIED., .F., .F.,
 ( 4, 2, 2, 2, 2, 2, 2, 2, 2, 2, 2, 2, 2, 2, 2, 2, 2, 2, 2, 4 ),
 ( 0.000000000000000000, 0.0008795077490859314886, 0.001759015498171862977, 0.002638523247257794357, 0.003518030996343725954, 0.004397538745429656684, 0.004837292619972635710, 0.005277046494515613868, 0.005716800369058592027, 0.006156554243601570185, 0.007036061992687516094, 0.007475815867230489915, 0.007915569741773462870, 0.008795077490859405309, 0.009674585239945351217, 0.01055409298903129539, 0.01143360073811723783, 0.01231310848720318200, 0.01319261623628912618, 0.01407212398537507209 ),
 .UNSPECIFIED. ) ;
#11982=CARTESIAN_POINT ( 'NONE',  ( -2.107032882782853722, -1.725908548393271458, -0.1037381152052583161 ) ) ;
#11986=DIRECTION ( 'NONE',  ( -0.000000000000000000, -0.000000000000000000, -1.000000000000000000 ) ) ;
#11989=ORIENTED_EDGE ( 'NONE', *, *, #15276, .T. ) ;
#12007=CARTESIAN_POINT ( 'NONE',  ( -0.07874015748031520934, 1.062385330869439640E-16, 0.01968503937007873988 ) ) ;
#12011=ORIENTED_EDGE ( 'NONE', *, *, #14417, .F. ) ;
#12021=FACE_OUTER_BOUND ( 'NONE', #8848, .T. ) ;
#12022=DIRECTION ( 'NONE',  ( 1.000000000000000000, 0.000000000000000000, 0.000000000000000000 ) ) ;
#12023=CARTESIAN_POINT ( 'NONE',  ( -0.07874015748031543138, -0.1682792322177920907, 0.05905511811023622659 ) ) ;
#12027=ORIENTED_EDGE ( 'NONE', *, *, #2960, .T. ) ;
#12028=EDGE_CURVE ( 'NONE', #1797, #9820, #6095, .T. ) ;
#12031=ADVANCED_FACE ( 'NONE', ( #4313 ), #14631, .T. ) ;
#12032=DIRECTION ( 'NONE',  ( -0.000000000000000000, 0.000000000000000000, 1.000000000000000000 ) ) ;
#12033=CARTESIAN_POINT ( 'NONE',  ( -1.914091141911949734, -2.904218397859934075, 0.1188472834034596526 ) ) ;
#12036=CARTESIAN_POINT ( 'NONE',  ( -2.184126211765464287, -1.693613514254873165, 0.08383392658276944687 ) ) ;
#12046=CARTESIAN_POINT ( 'NONE',  ( -0.2755905511811023167, -0.02638708502139245488, -0.03937007874015747977 ) ) ;
#12060=CARTESIAN_POINT ( 'NONE',  ( -1.293236445124221312, 0.1355266887446167634, -0.03937007874015747977 ) ) ;
#12062=CARTESIAN_POINT ( 'NONE',  ( -1.452763252956529083, -0.05091287232363069654, -0.1033464566929133133 ) ) ;
#12063=CARTESIAN_POINT ( 'NONE',  ( -2.011807227224586825, -2.756102811318747126, 0.1765457041329571430 ) ) ;
#12065=CARTESIAN_POINT ( 'NONE',  ( -1.915575942926155406, -2.830573451792969486, 0.1438162775209220201 ) ) ;
#12068=CARTESIAN_POINT ( 'NONE',  ( -0.008251140381529230641, 0.1525182358981297670, -0.01646613645217641364 ) ) ;
#12071=UNCERTAINTY_MEASURE_WITH_UNIT (LENGTH_MEASURE( 1.000000000000000082E-05 ), #14065, 'distance_accuracy_value', 'NONE');
#12076=FACE_OUTER_BOUND ( 'NONE', #4304, .T. ) ;
#12078=CARTESIAN_POINT ( 'NONE',  ( -1.180847381051866485, 0.3433074774306730803, 0.03937007874015747977 ) ) ;
#12089=ORIENTED_EDGE ( 'NONE', *, *, #5058, .T. ) ;
#12093=VERTEX_POINT ( 'NONE', #10134 ) ;
#12100=CIRCLE ( 'NONE', #1335, 0.2362204724409449619 ) ;
#12102=CARTESIAN_POINT ( 'NONE',  ( -1.398125690441303526, -0.003404927804347070153, 0.05905511811023622659 ) ) ;
#12103=CARTESIAN_POINT ( 'NONE',  ( -2.090051324975654268, -1.858423098537180129, 0.1968503937007874127 ) ) ;
#12105=SHAPE_REPRESENTATION ( 'Finger', ( #11481 ), #9487 ) ;
#12118=VERTEX_POINT ( 'NONE', #15144 ) ;
#12122=DIRECTION ( 'NONE',  ( -1.000000000000000000, 0.000000000000000000, 0.000000000000000000 ) ) ;
#12127=DIRECTION ( 'NONE',  ( 0.6421085279136217183, 0.7666137478421592988, -1.662328581735447640E-15 ) ) ;
#12129=DIRECTION ( 'NONE',  ( 0.000000000000000000, -1.000000000000000000, 2.212657494868377674E-16 ) ) ;
#12134=EDGE_LOOP ( 'NONE', ( #7435, #15104, #4985, #8093 ) ) ;
#12136=ADVANCED_FACE ( 'NONE', ( #1817 ), #507, .F. ) ;
#12140=CIRCLE ( 'NONE', #5858, 0.05905511811023627516 ) ;
#12142=ORIENTED_EDGE ( 'NONE', *, *, #13797, .F. ) ;
#12143=AXIS2_PLACEMENT_3D ( 'NONE', #14512, #8542, #9889 ) ;
#12147=CARTESIAN_POINT ( 'NONE',  ( -1.551763806551527347, 0.1400464552716836897, 0.05905511811023622659 ) ) ;
#12148=CARTESIAN_POINT ( 'NONE',  ( -2.182693454834260027, -1.630005269948474167, 0.1033464566929130080 ) ) ;
#12152=CARTESIAN_POINT ( 'NONE',  ( -1.941813874431828957, -2.756691771901667476, 0.1575933035815317296 ) ) ;
#12172=CARTESIAN_POINT ( 'NONE',  ( -1.190198933766853706, 0.3259758027579612860, -0.05905511811023622659 ) ) ;
#12180=ORIENTED_EDGE ( 'NONE', *, *, #10181, .T. ) ;
#12184=DIRECTION ( 'NONE',  ( 0.5750876580239430158, 0.8180917953313895374, 0.000000000000000000 ) ) ;
#12185=AXIS2_PLACEMENT_3D ( 'NONE', #12652, #7857, #11301 ) ;
#12186=EDGE_CURVE ( 'NONE', #9296, #749, #9623, .T. ) ;
#12198=EDGE_LOOP ( 'NONE', ( #14952, #15311, #13402, #4693 ) ) ;
#12200=AXIS2_PLACEMENT_3D ( 'NONE', #14013, #10413, #4457 ) ;
#12203=CIRCLE ( 'NONE', #2191, 0.03937007874015751446 ) ;
#12205=CARTESIAN_POINT ( 'NONE',  ( -2.100298540928004165, -2.106218814929184724, -0.1158686206437609667 ) ) ;
#12206=CARTESIAN_POINT ( 'NONE',  ( -1.943704794560271676, -2.936197138332786061, -0.06765823053126623909 ) ) ;
#12214=CARTESIAN_POINT ( 'NONE',  ( -0.02641567992992046449, 0.1724028871747071145, 1.853431881210122409E-17 ) ) ;
#12215=CARTESIAN_POINT ( 'NONE',  ( -0.002500327830563135300, -0.1654030484222656916, 8.530201525337163767E-32 ) ) ;
#12217=DIRECTION ( 'NONE',  ( -0.000000000000000000, -2.212657494868377674E-16, 1.000000000000000000 ) ) ;
#12224=AXIS2_PLACEMENT_3D ( 'NONE', #10667, #6736, #4711 ) ;
#12225=EDGE_CURVE ( 'NONE', #631, #8019, #14045, .T. ) ;
#12226=CARTESIAN_POINT ( 'NONE',  ( -1.419105553176674306, -0.01195146698575283613, -0.07341972397144938545 ) ) ;
#12227=DIRECTION ( 'NONE',  ( 1.000000000000000000, 0.000000000000000000, 0.000000000000000000 ) ) ;
#12232=FACE_BOUND ( 'NONE', #1022, .T. ) ;
#12233=AXIS2_PLACEMENT_3D ( 'NONE', #723, #1803, #643 ) ;
#12234=CARTESIAN_POINT ( 'NONE',  ( -1.868651797801601733, -2.949104743336227408, -0.01367295599960066839 ) ) ;
#12236=CARTESIAN_POINT ( 'NONE',  ( -1.980110816268535689, -2.844065425694749738, -0.1439511263496600080 ) ) ;
#12237=DIRECTION ( 'NONE',  ( -6.571729149350554040E-16, -5.967930543588097370E-16, 1.000000000000000000 ) ) ;
#12238=VECTOR ( 'NONE', #291, 39.37007874015748143 ) ;
#12240=VERTEX_POINT ( 'NONE', #3542 ) ;
#12242=ORIENTED_EDGE ( 'NONE', *, *, #3893, .T. ) ;
#12246=DIRECTION ( 'NONE',  ( 0.000000000000000000, -0.000000000000000000, -1.000000000000000000 ) ) ;
#12251=DIRECTION ( 'NONE',  ( 1.349229370204184172E-15, 1.000000000000000000, -0.000000000000000000 ) ) ;
#12260=CARTESIAN_POINT ( 'NONE',  ( -1.946192867917153180, -2.743611295743889400, 0.1749236412511678829 ) ) ;
#12269=EDGE_LOOP ( 'NONE', ( #4354, #14491, #3738, #9964 ) ) ;
#12272=DIRECTION ( 'NONE',  ( 1.000000000000000000, 0.000000000000000000, 0.000000000000000000 ) ) ;
#12273=CARTESIAN_POINT ( 'NONE',  ( -1.933092583737872516, -2.927344828647098662, 0.08673291769302551857 ) ) ;
#12276=CARTESIAN_POINT ( 'NONE',  ( -1.992382107315057160, -2.749515453455444014, -0.1756903148397123415 ) ) ;
#12279=CARTESIAN_POINT ( 'NONE',  ( -1.945459748359986252, -2.745801194614591711, 0.1561691687464105693 ) ) ;
#12281=DIRECTION ( 'NONE',  ( 0.000000000000000000, 1.000000000000000000, 2.198945251238206020E-16 ) ) ;
#12283=ORIENTED_EDGE ( 'NONE', *, *, #3657, .T. ) ;
#12294=CARTESIAN_POINT ( 'NONE',  ( -1.190198933766852152, 0.3259758027579607864, 0.05905511811023622659 ) ) ;
#12295=CARTESIAN_POINT ( 'NONE',  ( -1.880204665810354392, -2.921028484878219977, 0.02323882831853205100 ) ) ;
#12296=ORIENTED_EDGE ( 'NONE', *, *, #9403, .F. ) ;
#12299=CARTESIAN_POINT ( 'NONE',  ( -1.419615703680148000, -0.01226548409420238732, -0.07587027276709679136 ) ) ;
#12304=ADVANCED_FACE ( 'NONE', ( #1567 ), #14369, .T. ) ;
#12306=B_SPLINE_CURVE_WITH_KNOTS ( 'NONE', 3,
 ( #13876, #10123, #5314, #13649, #14909, #12717, #7834, #11456 ),
 .UNSPECIFIED., .F., .F.,
 ( 4, 2, 2, 4 ),
 ( 0.000000000000000000, 0.0007747600241158876608, 0.001162140036173831600, 0.001549520048231775322 ),
 .UNSPECIFIED. ) ;
#12310=DIRECTION ( 'NONE',  ( -0.5984233124757303290, -0.8011800915434521553, 0.000000000000000000 ) ) ;
#12311=DIRECTION ( 'NONE',  ( -0.6421085279136220514, -0.7666137478421591878, -1.662328581735448824E-15 ) ) ;
#12315=CARTESIAN_POINT ( 'NONE',  ( -0.05916619364927751951, -0.1856756262235988719, 0.05712045715993030459 ) ) ;
#12318=ORIENTED_EDGE ( 'NONE', *, *, #7923, .T. ) ;
#12319=ADVANCED_FACE ( 'NONE', ( #12076 ), #14441, .F. ) ;
#12324=CARTESIAN_POINT ( 'NONE',  ( -0.07874015748031501505, 0.1442356988431299225, -0.05905511811023622659 ) ) ;
#12331=ORIENTED_EDGE ( 'NONE', *, *, #4194, .T. ) ;
#12340=CARTESIAN_POINT ( 'NONE',  ( -1.948352921524023396, -2.924828074509654208, 0.06159255423288990949 ) ) ;
#12342=CARTESIAN_POINT ( 'NONE',  ( -2.003334911435759480, -2.780488847103764982, -0.1775198577236423436 ) ) ;
#12349=DIRECTION ( 'NONE',  ( 2.593979029498040879E-15, 1.000000000000000000, 2.431855340154413200E-16 ) ) ;
#12357=CARTESIAN_POINT ( 'NONE',  ( -1.419615703680148000, -0.01226548409420240640, -0.07874015748031495954 ) ) ;
#12358=ADVANCED_FACE ( 'NONE', ( #3774 ), #8479, .F. ) ;
#12365=EDGE_CURVE ( 'NONE', #9820, #11513, #6221, .T. ) ;
#12369=DIRECTION ( 'NONE',  ( -0.000000000000000000, 0.000000000000000000, 1.000000000000000000 ) ) ;
#12370=CARTESIAN_POINT ( 'NONE',  ( -1.900614262648875785, -2.941986504649573675, 0.05143564777245772379 ) ) ;
#12376=AXIS2_PLACEMENT_3D ( 'NONE', #6213, #13437, #4895 ) ;
#12377=CARTESIAN_POINT ( 'NONE',  ( -1.419615703680148000, -0.01226548409420231273, -0.07874015748031495954 ) ) ;
#12378=CLOSED_SHELL ( 'NONE', ( #12304, #4477, #2221, #8219, #1036, #4828, #508, #670, #5363, #12577, #7144, #3575, #12358, #10102, #7697, #14732, #9731, #4721, #1900, #9713, #9405, #1780, #14157, #12319, #12136, #7393, #10959, #11733, #15200, #10642, #7221, #6970, #1963, #3501, #14324, #12031, #12471, #7613, #9051, #5871, #7855, #9068, #4809, #13003, #14861, #1465, #1842, #5702, #13658, #4432, #14515, #7481, #5900, #12966, #13045, #472, #1092, #1897, #732, #6793, #2133, #11739, #14311, #6218, #2695, #5918, #13864, #57, #3879, #1982, #3020, #7445, #330, #6246, #2833, #10061, #11234, #7680, #6937, #11960, #10550, #6030, #6037, #5838, #3839, #11050, #6079, #3613, #9804, #13438 ) ) ;
#12392=CARTESIAN_POINT ( 'NONE',  ( -0.07874015748031543138, -0.1682792322177920907, -0.05905511811023622659 ) ) ;
#12394=CARTESIAN_POINT ( 'NONE',  ( -2.090051324975654268, -2.008999527832921572, 0.09061016354475488754 ) ) ;
#12395=EDGE_CURVE ( 'NONE', #10993, #10478, #7879, .T. ) ;
#12396=EDGE_CURVE ( 'NONE', #11793, #12712, #10376, .T. ) ;
#12397=DIRECTION ( 'NONE',  ( 0.000000000000000000, 1.000000000000000000, 2.208809394877300528E-16 ) ) ;
#12399=CARTESIAN_POINT ( 'NONE',  ( -1.580080891953811628, 0.1020406297922293593, 0.08366141732283462196 ) ) ;
#12410=CARTESIAN_POINT ( 'NONE',  ( -2.096278492746562971, -1.821809766472917369, 0.08366141731681048244 ) ) ;
#12413=CARTESIAN_POINT ( 'NONE',  ( -0.3441669734936866343, 2.010494531933507467, -0.03937007874015747977 ) ) ;
#12432=CARTESIAN_POINT ( 'NONE',  ( -1.925142990015122679, -2.949151230150205194, 0.01280935300854439338 ) ) ;
#12434=DIRECTION ( 'NONE',  ( -0.000000000000000000, 0.000000000000000000, 1.000000000000000000 ) ) ;
#12436=FACE_OUTER_BOUND ( 'NONE', #7560, .T. ) ;
#12441=ORIENTED_EDGE ( 'NONE', *, *, #15054, .T. ) ;
#12460=CARTESIAN_POINT ( 'NONE',  ( -1.905882447707811345, -2.927389732709596792, -0.08665040272426297041 ) ) ;
#12465=CARTESIAN_POINT ( 'NONE',  ( -1.293236445124221312, 0.1355266887446167634, 0.05905511811023622659 ) ) ;
#12471=ADVANCED_FACE ( 'NONE', ( #10331 ), #12544, .T. ) ;
#12473=FACE_OUTER_BOUND ( 'NONE', #8505, .T. ) ;
#12476=DIRECTION ( 'NONE',  ( -1.000000000000000000, 0.000000000000000000, 0.000000000000000000 ) ) ;
#12478=CYLINDRICAL_SURFACE ( 'NONE', #5825, 0.01968503937007875723 ) ;
#12481=CARTESIAN_POINT ( 'NONE',  ( -1.417802900492933782, -0.04287136159519127493, 0.07363999040138466401 ) ) ;
#12482=LENGTH_MEASURE_WITH_UNIT ( LENGTH_MEASURE( 0.02539999999999999897 ), #2920 );
#12487=ORIENTED_EDGE ( 'NONE', *, *, #4452, .F. ) ;
#12491=CARTESIAN_POINT ( 'NONE',  ( -2.077827123841874624, -2.289966559474202690, 0.1278948828575666996 ) ) ;
#12503=EDGE_LOOP ( 'NONE', ( #6664, #10669, #7814, #6231 ) ) ;
#12508=DIRECTION ( 'NONE',  ( 0.000000000000000000, -0.000000000000000000, -1.000000000000000000 ) ) ;
#12509=CARTESIAN_POINT ( 'NONE',  ( -1.971195541939750218, -2.816466357294567846, 0.1716894902957993574 ) ) ;
#12512=CARTESIAN_POINT ( 'NONE',  ( -1.989671392673562522, -2.818355208888676966, -0.1526115818275636249 ) ) ;
#12514=FACE_OUTER_BOUND ( 'NONE', #13600, .T. ) ;
#12518=ORIENTED_EDGE ( 'NONE', *, *, #14794, .F. ) ;
#12523=ORIENTED_EDGE ( 'NONE', *, *, #1068, .F. ) ;
#12524=CARTESIAN_POINT ( 'NONE',  ( -1.398125690441303304, -0.003404927804347051071, -0.05905511811023622659 ) ) ;
#12525=DIRECTION ( 'NONE',  ( 0.000000000000000000, 1.000000000000000000, 2.212657494868377674E-16 ) ) ;
#12526=LINE ( 'NONE', #14961, #3152 ) ;
#12528=CARTESIAN_POINT ( 'NONE',  ( -0.07874015748031501505, 0.1442356988431297560, 0.05905511811023622659 ) ) ;
#12530=EDGE_CURVE ( 'NONE', #14935, #1514, #14386, .T. ) ;
#12535=DIRECTION ( 'NONE',  ( 0.000000000000000000, 1.000000000000000000, 2.212657494868377674E-16 ) ) ;
#12542=DIRECTION ( 'NONE',  ( 1.000000000000000000, 0.000000000000000000, 0.000000000000000000 ) ) ;
#12544=SPHERICAL_SURFACE ( 'NONE', #4869, 0.01968503937007873988 ) ;
#12560=CARTESIAN_POINT ( 'NONE',  ( -0.002500327830562892005, -0.005471572485237196845, 0.000000000000000000 ) ) ;
#12561=EDGE_CURVE ( 'NONE', #11758, #1514, #11209, .T. ) ;
#12567=EDGE_CURVE ( 'NONE', #6534, #631, #5999, .T. ) ;
#12570=ORIENTED_EDGE ( 'NONE', *, *, #3524, .F. ) ;
#12576=CARTESIAN_POINT ( 'NONE',  ( 0.000000000000000000, 0.000000000000000000, 0.000000000000000000 ) ) ;
#12577=ADVANCED_FACE ( 'NONE', ( #13007 ), #14096, .T. ) ;
#12579=CARTESIAN_POINT ( 'NONE',  ( -1.980036129185591687, -2.844263444572586952, -0.1438637502453037620 ) ) ;
#12580=CARTESIAN_POINT ( 'NONE',  ( -0.2755905511811023167, -0.02638708502139245488, 0.05905511811023622659 ) ) ;
#12583=CARTESIAN_POINT ( 'NONE',  ( -2.090430742248608809, -1.869089515625215192, -0.1064913232527224946 ) ) ;
#12589=TOROIDAL_SURFACE ( 'NONE', #6070, 0.05905511811023621271, 0.01968503937007873988 ) ;
#12591=EDGE_LOOP ( 'NONE', ( #8156, #6163, #11935, #11546 ) ) ;
#12594=CARTESIAN_POINT ( 'NONE',  ( -1.596293587998444341, 0.1133155780026528781, 0.04477369844320258641 ) ) ;
#12595=AXIS2_PLACEMENT_3D ( 'NONE', #14071, #1078, #3340 ) ;
#12604=CARTESIAN_POINT ( 'NONE',  ( -1.912425819538432936, -2.839079622322270513, -0.1647229803796586289 ) ) ;
#12605=ORIENTED_EDGE ( 'NONE', *, *, #7400, .T. ) ;
#12609=ORIENTED_EDGE ( 'NONE', *, *, #5801, .T. ) ;
#12612=CIRCLE ( 'NONE', #11093, 0.01968503937007873988 ) ;
#12622=CARTESIAN_POINT ( 'NONE',  ( -1.182291936363664364, 0.3416838286736338937, -0.04963174987406846622 ) ) ;
#12626=CIRCLE ( 'NONE', #5848, 0.01968503937007880233 ) ;
#12629=CARTESIAN_POINT ( 'NONE',  ( -0.2755905511811023167, -0.02638708502139245488, 0.03937007874015747977 ) ) ;
#12641=CARTESIAN_POINT ( 'NONE',  ( -0.02525249394760406899, 0.1725264476027483229, -0.03885236003516508857 ) ) ;
#12645=CARTESIAN_POINT ( 'NONE',  ( -1.570515516786431975, 0.1150740656596127842, 0.05905511811023623353 ) ) ;
#12650=AXIS2_PLACEMENT_3D ( 'NONE', #8954, #12311, #2911 ) ;
#12652=CARTESIAN_POINT ( 'NONE',  ( -0.3441669734936866343, 2.010494531933507467, 0.05905511811023622659 ) ) ;
#12653=TOROIDAL_SURFACE ( 'NONE', #7130, 0.2303149606299203511, 0.01968503937007873988 ) ;
#12654=ORIENTED_EDGE ( 'NONE', *, *, #14396, .F. ) ;
#12661=VECTOR ( 'NONE', #3754, 39.37007874015748143 ) ;
#12662=EDGE_CURVE ( 'NONE', #3768, #2439, #7116, .T. ) ;
#12664=CARTESIAN_POINT ( 'NONE',  ( -1.965791048816216913, -2.881337861409273504, 0.1402741378984690979 ) ) ;
#12667=CARTESIAN_POINT ( 'NONE',  ( -1.950690859776006425, -2.877529656554294046, -0.1430888780872220378 ) ) ;
#12671=CARTESIAN_POINT ( 'NONE',  ( -2.080790309745595756, -2.104291597191282115, -0.1157681807899624687 ) ) ;
#12673=VERTEX_POINT ( 'NONE', #12062 ) ;
#12674=ORIENTED_EDGE ( 'NONE', *, *, #12530, .T. ) ;
#12675=EDGE_CURVE ( 'NONE', #749, #9606, #5243, .T. ) ;
#12679=EDGE_LOOP ( 'NONE', ( #9522, #10257, #8685, #11807 ) ) ;
#12683=CARTESIAN_POINT ( 'NONE',  ( -2.068647409231312295, -2.591269129772357349, 0.1345927733208676091 ) ) ;
#12690=DIRECTION ( 'NONE',  ( -0.5293839892290541638, 0.8483823383050430600, 0.000000000000000000 ) ) ;
#12702=EDGE_CURVE ( 'NONE', #15414, #925, #5373, .T. ) ;
#12708=CARTESIAN_POINT ( 'NONE',  ( -1.957251767099916107, -2.772329397582958599, 0.1771653543307079026 ) ) ;
#12710=B_SPLINE_CURVE_WITH_KNOTS ( 'NONE', 3,
 ( #10005, #12215, #14785, #4039, #1706, #13590 ),
 .UNSPECIFIED., .F., .F.,
 ( 4, 2, 4 ),
 ( 0.000000000000000000, 0.0003645138504237786640, 0.0007290277008475573280 ),
 .UNSPECIFIED. ) ;
#12712=VERTEX_POINT ( 'NONE', #10798 ) ;
#12717=CARTESIAN_POINT ( 'NONE',  ( -1.396183715708124051, -0.02562187435717607278, -0.04038159613861123237 ) ) ;
#12718=CARTESIAN_POINT ( 'NONE',  ( -1.187897378299091367, 0.3305578035811536641, 0.05905511811023621271 ) ) ;
#12720=DIRECTION ( 'NONE',  ( -0.000000000000000000, 0.000000000000000000, 1.000000000000000000 ) ) ;
#12735=CARTESIAN_POINT ( 'NONE',  ( 0.9851651268172137987, -1.725292181286280480, -0.08366141732283417787 ) ) ;
#12738=AXIS2_PLACEMENT_3D ( 'NONE', #11010, #7486, #9614 ) ;
#12743=DIRECTION ( 'NONE',  ( -1.349229370204184172E-15, -1.000000000000000000, 0.000000000000000000 ) ) ;
#12746=CARTESIAN_POINT ( 'NONE',  ( -1.276200637803905691, -0.1988000726501942539, -0.08366141732283455257 ) ) ;
#12749=CARTESIAN_POINT ( 'NONE',  ( -2.087452354246647879, -2.011709019740274940, -0.09152848164307673950 ) ) ;
#12753=ORIENTED_EDGE ( 'NONE', *, *, #3199, .F. ) ;
#12761=EDGE_CURVE ( 'NONE', #6873, #11758, #14154, .T. ) ;
#12770=EDGE_CURVE ( 'NONE', #5808, #6948, #2565, .T. ) ;
#12771=CARTESIAN_POINT ( 'NONE',  ( -1.100415514366356762, -0.04998955061627542718, -0.05905511811023622659 ) ) ;
#12772=CARTESIAN_POINT ( 'NONE',  ( -1.938628142022554401, -2.911908481707071950, 0.1097354202932025180 ) ) ;
#12779=DIRECTION ( 'NONE',  ( 0.5984233124757303290, 0.8011800915434521553, 0.000000000000000000 ) ) ;
#12787=EDGE_LOOP ( 'NONE', ( #8275, #14018, #1286, #6618 ) ) ;
#12798=FACE_OUTER_BOUND ( 'NONE', #6295, .T. ) ;
#12807=ORIENTED_EDGE ( 'NONE', *, *, #15077, .F. ) ;
#12813=CARTESIAN_POINT ( 'NONE',  ( -0.2362204724409448231, -0.02638708502139245488, 0.03937007874015747977 ) ) ;
#12826=CARTESIAN_POINT ( 'NONE',  ( -1.943436547385579249, -2.816558498006583644, -0.1716660038806392119 ) ) ;
#12828=DIRECTION ( 'NONE',  ( 1.000000000000000000, 0.000000000000000000, 0.000000000000000000 ) ) ;
#12830=ORIENTED_EDGE ( 'NONE', *, *, #3852, .F. ) ;
#12838=TOROIDAL_SURFACE ( 'NONE', #6067, 0.05905511811023621271, 0.01968503937007873988 ) ;
#12842=CARTESIAN_POINT ( 'NONE',  ( -1.927226688427879475, -2.943474258813137290, -0.04731147916820623023 ) ) ;
#12845=ORIENTED_EDGE ( 'NONE', *, *, #12225, .T. ) ;
#12846=CARTESIAN_POINT ( 'NONE',  ( -2.100501784635051550, -1.630597114118274238, -0.1033464566929129386 ) ) ;
#12848=CIRCLE ( 'NONE', #13586, 0.2362204724409449619 ) ;
#12851=DIRECTION ( 'NONE',  ( -0.000000000000000000, 0.000000000000000000, 1.000000000000000000 ) ) ;
#12854=CARTESIAN_POINT ( 'NONE',  ( -1.596293587998444563, 0.1133155780026525727, 0.04477369844320282927 ) ) ;
#12858=B_SPLINE_CURVE_WITH_KNOTS ( 'NONE', 3,
 ( #13478, #5154, #2743, #10026, #11202, #7513, #12299, #12377 ),
 .UNSPECIFIED., .F., .F.,
 ( 4, 2, 2, 4 ),
 ( 0.000000000000000000, 0.0004305386933195752574, 0.0006458080399793631301, 0.0008610773866391509485 ),
 .UNSPECIFIED. ) ;
#12863=CIRCLE ( 'NONE', #6089, 0.03937007874015751446 ) ;
#12864=AXIS2_PLACEMENT_3D ( 'NONE', #15244, #7953, #6841 ) ;
#12871=DIRECTION ( 'NONE',  ( -0.000000000000000000, -0.000000000000000000, -1.000000000000000000 ) ) ;
#12873=ORIENTED_EDGE ( 'NONE', *, *, #15077, .T. ) ;
#12878=ORIENTED_EDGE ( 'NONE', *, *, #8765, .T. ) ;
#12892=CARTESIAN_POINT ( 'NONE',  ( -1.932762117030202953, -2.849396711222250023, -0.1599284002103965874 ) ) ;
#12894=AXIS2_PLACEMENT_3D ( 'NONE', #4791, #13100, #9671 ) ;
#12899=CARTESIAN_POINT ( 'NONE',  ( -1.387704745771440429, -0.02010536753476148755, 0.05905511811023627516 ) ) ;
#12901=DIRECTION ( 'NONE',  ( -1.000000000000000000, 0.000000000000000000, 0.000000000000000000 ) ) ;
#12903=ORIENTED_EDGE ( 'NONE', *, *, #3723, .T. ) ;
#12904=ORIENTED_EDGE ( 'NONE', *, *, #10422, .F. ) ;
#12913=CARTESIAN_POINT ( 'NONE',  ( -0.06867854503139053657, 0.1655849054964026734, 0.03830121270948940587 ) ) ;
#12917=DIRECTION ( 'NONE',  ( 1.000000000000000000, 0.000000000000000000, 0.000000000000000000 ) ) ;
#12933=CARTESIAN_POINT ( 'NONE',  ( -1.187809996374852739, 0.3305575196848991038, -0.05905511802097350438 ) ) ;
#12939=CARTESIAN_POINT ( 'NONE',  ( -1.603592887480403295, 0.1030246510253539083, 0.05618170010999483377 ) ) ;
#12959=CARTESIAN_POINT ( 'NONE',  ( -1.580259682938329524, 0.1018956540307723729, 0.04477369844403742555 ) ) ;
#12961=EDGE_CURVE ( 'NONE', #7280, #9296, #15370, .T. ) ;
#12966=ADVANCED_FACE ( 'NONE', ( #768 ), #15100, .T. ) ;
#12970=ORIENTED_EDGE ( 'NONE', *, *, #2745, .T. ) ;
#12974=CARTESIAN_POINT ( 'NONE',  ( -1.901381477150592358, -2.939880072212064377, 0.05875302977771206664 ) ) ;
#12983=FACE_OUTER_BOUND ( 'NONE', #763, .T. ) ;
#12992=CARTESIAN_POINT ( 'NONE',  ( -1.180847381051866485, 0.3433074774306730803, 0.03937007874015747977 ) ) ;
#12993=CARTESIAN_POINT ( 'NONE',  ( -0.04507696108106434146, -0.1650637432014245287, -0.05202626060216886811 ) ) ;
#12997=DIRECTION ( 'NONE',  ( 1.000000000000000000, 0.000000000000000000, 0.000000000000000000 ) ) ;
#12999=ORIENTED_EDGE ( 'NONE', *, *, #1310, .T. ) ;
#13002=ORIENTED_EDGE ( 'NONE', *, *, #12396, .T. ) ;
#13003=ADVANCED_FACE ( 'NONE', ( #10553 ), #5119, .T. ) ;
#13007=FACE_OUTER_BOUND ( 'NONE', #7, .T. ) ;
#13010=CARTESIAN_POINT ( 'NONE',  ( -1.916695816424315746, -2.827605297880910751, 0.1689279957868018711 ) ) ;
#13011=ORIENTED_EDGE ( 'NONE', *, *, #7798, .T. ) ;
#13015=CARTESIAN_POINT ( 'NONE',  ( -1.606327126723951615, 0.09914643767337930069, 0.06529511858635557442 ) ) ;
#13016=ORIENTED_EDGE ( 'NONE', *, *, #2731, .F. ) ;
#13021=CARTESIAN_POINT ( 'NONE',  ( -0.02063990244551198311, 0.1734013470568572801, -3.760128896581743291E-13 ) ) ;
#13027=ORIENTED_EDGE ( 'NONE', *, *, #14198, .F. ) ;
#13041=CARTESIAN_POINT ( 'NONE',  ( -1.900032110109137307, -2.943588721549657006, -0.04688266410269418399 ) ) ;
#13042=( NAMED_UNIT ( * ) SI_UNIT ( $, .STERADIAN. ) SOLID_ANGLE_UNIT ( ) );
#13044=CARTESIAN_POINT ( 'NONE',  ( -1.580080891953811850, 0.1020406297922293037, -0.07529375917861416689 ) ) ;
#13045=ADVANCED_FACE ( 'NONE', ( #7028 ), #12653, .T. ) ;
#13046=CARTESIAN_POINT ( 'NONE',  ( -1.387704745771440429, -0.02010536753476150837, 0.03937007874015747977 ) ) ;
#13047=CARTESIAN_POINT ( 'NONE',  ( -2.080881322745466999, -1.632190302820504479, -0.08366141732283423338 ) ) ;
#13050=ORIENTED_EDGE ( 'NONE', *, *, #13512, .F. ) ;
#13054=B_SPLINE_CURVE_WITH_KNOTS ( 'NONE', 3,
 ( #4578, #9367, #1063, #10616 ),
 .UNSPECIFIED., .F., .F.,
 ( 4, 4 ),
 ( 0.000000000000000000, 0.0006024839870383029905 ),
 .UNSPECIFIED. ) ;
#13058=CARTESIAN_POINT ( 'NONE',  ( -1.572611271869832184, 0.1123963381039306264, -0.05997718891474942970 ) ) ;
#13068=EDGE_LOOP ( 'NONE', ( #14825, #14551, #5927, #15112 ) ) ;
#13069=DIRECTION ( 'NONE',  ( -0.000000000000000000, 0.000000000000000000, 1.000000000000000000 ) ) ;
#13070=CARTESIAN_POINT ( 'NONE',  ( -1.944249365573698540, -2.934812813689591682, 0.02858372338952079941 ) ) ;
#13071=CARTESIAN_POINT ( 'NONE',  ( -2.755905511811024056, -2.772329397582842248, 0.000000000000000000 ) ) ;
#13072=CARTESIAN_POINT ( 'NONE',  ( -1.950280692371897384, -2.878718452480370615, -0.1421344132345661593 ) ) ;
#13075=CARTESIAN_POINT ( 'NONE',  ( -2.116009644208461271, -1.821148055095885399, 0.1033464566929130357 ) ) ;
#13076=ORIENTED_EDGE ( 'NONE', *, *, #12395, .F. ) ;
#13077=CARTESIAN_POINT ( 'NONE',  ( -1.969122886354301327, -2.872755761241831518, -0.1273454318878232960 ) ) ;
#13093=DIRECTION ( 'NONE',  ( -0.9387676358163957735, 0.3445509047204710629, 1.288839711614000126E-12 ) ) ;
#13097=CARTESIAN_POINT ( 'NONE',  ( -1.576192857444074225, 0.1076040293810619497, -0.06348264010178604477 ) ) ;
#13098=AXIS2_PLACEMENT_3D ( 'NONE', #8869, #13278, #13877 ) ;
#13100=DIRECTION ( 'NONE',  ( 0.000000000000000000, -0.000000000000000000, -1.000000000000000000 ) ) ;
#13102=EDGE_CURVE ( 'NONE', #10393, #14453, #3669, .T. ) ;
#13116=CARTESIAN_POINT ( 'NONE',  ( -1.911437664849721108, -2.911761458588945750, 0.1099279165421168103 ) ) ;
#13118=CARTESIAN_POINT ( 'NONE',  ( -2.182693454834259139, -1.630005269948474389, 0.08366141732283424726 ) ) ;
#13125=CARTESIAN_POINT ( 'NONE',  ( -1.396233373141806400, -0.02565714533840434894, 0.04040313278352580806 ) ) ;
#13126=DIRECTION ( 'NONE',  ( 0.9162674345903514261, -0.4005670834070318986, 0.000000000000000000 ) ) ;
#13138=CARTESIAN_POINT ( 'NONE',  ( -0.3441669734936866343, 2.010494531933507467, 0.05905511811023622659 ) ) ;
#13140=CARTESIAN_POINT ( 'NONE',  ( -1.591501945092674841, 0.08600752902535294120, 0.08366141732283462196 ) ) ;
#13151=B_SPLINE_CURVE_WITH_KNOTS ( 'NONE', 3,
 ( #5813, #2470, #8107, #9457, #1293, #12892, #1060, #14372, #11876, #3496, #2302, #8266, #7242, #4667, #13041, #4800, #6933, #10537, #10767, #993, #9286, #8373, #12974, #3645, #5741, #13116, #12033, #15316, #8200, #14230, #7078, #1150, #4576, #10614, #5905, #2164 ),
 .UNSPECIFIED., .F., .F.,
 ( 4, 2, 2, 2, 2, 2, 2, 2, 2, 2, 2, 2, 2, 2, 2, 2, 2, 4 ),
 ( 0.0006024839870383029905, 0.001504406831461554354, 0.002406329675884806042, 0.003308252520308057297, 0.004210175364731308552, 0.005112098209154560674, 0.006014021053577811061, 0.006915943898001062316, 0.007366905320212691413, 0.007817866742424321377, 0.008719789586847579571, 0.009621712431270836030, 0.01052363527569409422, 0.01142555812011735242, 0.01232748096454061061, 0.01322940380896386707, 0.01413132665338712526, 0.01503324949781038346 ),
 .UNSPECIFIED. ) ;
#13154=ORIENTED_EDGE ( 'NONE', *, *, #11563, .T. ) ;
#13161=CARTESIAN_POINT ( 'NONE',  ( -1.925012530255905130, -2.949505661444294269, 0.006211189736853072255 ) ) ;
#13164=CARTESIAN_POINT ( 'NONE',  ( -0.02433043306709228512, -0.1808586691373950950, -0.01162756877077187820 ) ) ;
#13165=DIRECTION ( 'NONE',  ( -0.3445509047216855913, -0.9387676358159497969, 0.000000000000000000 ) ) ;
#13168=CARTESIAN_POINT ( 'NONE',  ( -1.925363067542684936, -2.803745874285077821, 0.1746042784463377462 ) ) ;
#13170=CARTESIAN_POINT ( 'NONE',  ( -1.943201052682586027, -2.937347917504331996, 0.005536254343342756137 ) ) ;
#13174=EDGE_CURVE ( 'NONE', #4567, #532, #6137, .T. ) ;
#13178=PRODUCT_DEFINITION_CONTEXT ( 'detailed design', #8095, 'design' ) ;
#13183=EDGE_CURVE ( 'NONE', #4234, #14001, #3773, .T. ) ;
#13184=CARTESIAN_POINT ( 'NONE',  ( -1.399422649241788497, -0.02634252632334466854, 0.07488899955401198683 ) ) ;
#13190=CARTESIAN_POINT ( 'NONE',  ( -1.580080891959645850, 0.1020406297963854930, -0.07533316186190673613 ) ) ;
#13192=AXIS2_PLACEMENT_3D ( 'NONE', #11433, #6637, #12828 ) ;
#13216=ORIENTED_EDGE ( 'NONE', *, *, #14198, .T. ) ;
#13224=CARTESIAN_POINT ( 'NONE',  ( -0.3441669734936866343, 2.010494531933507467, 0.03937007874015747977 ) ) ;
#13232=VERTEX_POINT ( 'NONE', #11645 ) ;
#13237=CARTESIAN_POINT ( 'NONE',  ( 0.9851651268172137987, -1.725292181286280480, -0.1033464566929129524 ) ) ;
#13238=DIRECTION ( 'NONE',  ( -0.000000000000000000, 0.000000000000000000, 1.000000000000000000 ) ) ;
#13240=CARTESIAN_POINT ( 'NONE',  ( -2.100501784635051550, -1.630597114118274238, 0.1033464566929129663 ) ) ;
#13244=CARTESIAN_POINT ( 'NONE',  ( -1.574484809660440021, 0.1100025355989264070, 0.06175692796217654990 ) ) ;
#13253=CARTESIAN_POINT ( 'NONE',  ( -1.415645031250719388, -0.01001692594509011672, 0.06639602688116504059 ) ) ;
#13254=CARTESIAN_POINT ( 'NONE',  ( -1.078976767140036319, 0.8059172436903675463, 0.05905511811023622659 ) ) ;
#13259=CARTESIAN_POINT ( 'NONE',  ( -1.592259916642329465, 0.1190110821473790575, -0.06350111023902997587 ) ) ;
#13263=CARTESIAN_POINT ( 'NONE',  ( -0.004688298860636740291, -0.1607931678657651686, 0.008473975361459438679 ) ) ;
#13269=DIRECTION ( 'NONE',  ( 1.000000000000000000, 0.000000000000000000, 0.000000000000000000 ) ) ;
#13278=DIRECTION ( 'NONE',  ( -0.000000000000000000, -0.000000000000000000, -1.000000000000000000 ) ) ;
#13290=DIRECTION ( 'NONE',  ( 0.000000000000000000, 2.212657494868377674E-16, 1.000000000000000000 ) ) ;
#13300=DIRECTION ( 'NONE',  ( -1.000000000000000000, 0.000000000000000000, 0.000000000000000000 ) ) ;
#13302=CARTESIAN_POINT ( 'NONE',  ( -2.073879752373330110, -2.575632606091952326, 0.1529717276801960957 ) ) ;
#13303=CARTESIAN_POINT ( 'NONE',  ( -1.190198933766852374, 0.3259758027579606199, 0.05905511811023622659 ) ) ;
#13304=CARTESIAN_POINT ( 'NONE',  ( -1.946192867917152292, -2.743611295743889844, 0.1749236412511669947 ) ) ;
#13307=CYLINDRICAL_SURFACE ( 'NONE', #1962, 0.07874015748031495954 ) ;
#13313=DIRECTION ( 'NONE',  ( -1.000000000000000000, 0.000000000000000000, 0.000000000000000000 ) ) ;
#13314=EDGE_CURVE ( 'NONE', #5035, #10983, #898, .T. ) ;
#13319=DIRECTION ( 'NONE',  ( 0.000000000000000000, 0.000000000000000000, -1.000000000000000000 ) ) ;
#13320=DIRECTION ( 'NONE',  ( -0.9995479251422038081, 0.03006568382583900759, 0.000000000000000000 ) ) ;
#13322=ORIENTED_EDGE ( 'NONE', *, *, #13183, .F. ) ;
#13323=CARTESIAN_POINT ( 'NONE',  ( -1.590519080053534484, 0.1214231549357164819, -0.06175753274851653041 ) ) ;
#13327=CARTESIAN_POINT ( 'NONE',  ( -0.002500327830563101039, -0.1605493263772690415, 0.000000000000000000 ) ) ;
#13331=EDGE_CURVE ( 'NONE', #1797, #4234, #387, .T. ) ;
#13339=TOROIDAL_SURFACE ( 'NONE', #3331, 3.149606299212599048, 0.01968503937007873988 ) ;
#13342=DIRECTION ( 'NONE',  ( 0.000000000000000000, 0.000000000000000000, -1.000000000000000000 ) ) ;
#13344=CIRCLE ( 'NONE', #10329, 0.01968503937007874682 ) ;
#13347=CARTESIAN_POINT ( 'NONE',  ( -0.03044903239804773801, 0.1717056406757087039, 0.01152843233334087912 ) ) ;
#13361=CARTESIAN_POINT ( 'NONE',  ( -2.109904669632267193, -1.821353904148520275, -0.1053094779739250780 ) ) ;
#13373=DIRECTION ( 'NONE',  ( 0.000000000000000000, -0.000000000000000000, -1.000000000000000000 ) ) ;
#13379=VERTEX_POINT ( 'NONE', #14696 ) ;
#13382=ORIENTED_EDGE ( 'NONE', *, *, #8579, .F. ) ;
#13383=( BOUNDED_SURFACE ( )  B_SPLINE_SURFACE ( 3, 2, ( 
 ( #10911, #109, #2457 ),
 ( #9674, #4874, #13492 ),
 ( #2755, #12315, #10756 ),
 ( #4792, #199, #7234 ),
 ( #3712, #8487, #4956 ),
 ( #9751, #14520, #14757 ),
 ( #6658, #8787, #8960 ),
 ( #4013, #6499, #6569 ),
 ( #11367, #7760, #1808 ),
 ( #6339, #2821, #3146 ) ),
 .UNSPECIFIED., .F., .F., .T. ) 
 B_SPLINE_SURFACE_WITH_KNOTS ( ( 4, 2, 2, 2, 4 ),
 ( 3, 3 ),
 ( 0.004862229905983068978, 0.005359824983622663366, 0.005857420061262256887, 0.006355015138901850408, 0.006852610216541444796 ),
 ( 0.000000000000000000, 1.000000000000000000 ),
 .UNSPECIFIED. ) 
 GEOMETRIC_REPRESENTATION_ITEM ( )  RATIONAL_B_SPLINE_SURFACE ( (
 ( 1.000000000000000000, 0.7071067811865475727, 1.000000000000000000),
 ( 1.000000000000000000, 0.7118664854617688942, 1.000000000000000000),
 ( 1.000000000000000000, 0.7168001159655631449, 1.000000000000000000),
 ( 1.000000000000000000, 0.7268793899691540217, 1.000000000000000000),
 ( 1.000000000000000000, 0.7317766985259492873, 1.000000000000000000),
 ( 1.000000000000000000, 0.7409494124080542310, 1.000000000000000000),
 ( 1.000000000000000000, 0.7450318297967697401, 1.000000000000000000),
 ( 1.000000000000000000, 0.7517743552594693401, 1.000000000000000000),
 ( 1.000000000000000000, 0.7543262850462577607, 1.000000000000000000),
 ( 1.000000000000000000, 0.7558617697692807669, 1.000000000000000000) ) ) 
 REPRESENTATION_ITEM ( '' )  SURFACE ( )  );
#13387=FACE_OUTER_BOUND ( 'NONE', #221, .T. ) ;
#13390=CARTESIAN_POINT ( 'NONE',  ( -0.07635964791965738074, -0.1878198040935885327, -0.03937007874015747977 ) ) ;
#13391=CARTESIAN_POINT ( 'NONE',  ( -2.188516668593762038, -1.823600774915123957, 0.1033333524257560032 ) ) ;
#13393=CARTESIAN_POINT ( 'NONE',  ( -1.115439883890946726, -0.06270839865334709717, 0.03937007874015747977 ) ) ;
#13394=CARTESIAN_POINT ( 'NONE',  ( -1.886696118240337450, -2.905094481821793639, 0.07206890175680845390 ) ) ;
#13397=CARTESIAN_POINT ( 'NONE',  ( -1.969094085985442444, -2.872830032507542874, 0.1272935473072890067 ) ) ;
#13402=ORIENTED_EDGE ( 'NONE', *, *, #5667, .F. ) ;
#13404=ORIENTED_EDGE ( 'NONE', *, *, #11823, .T. ) ;
#13406=CIRCLE ( 'NONE', #7902, 0.01968503937007880233 ) ;
#13411=CARTESIAN_POINT ( 'NONE',  ( -0.02220179245438161017, -0.1805881202044197775, -0.03580963740886420471 ) ) ;
#13420=VECTOR ( 'NONE', #4872, 39.37007874015748854 ) ;
#13424=ORIENTED_EDGE ( 'NONE', *, *, #8292, .F. ) ;
#13427=CARTESIAN_POINT ( 'NONE',  ( -1.974289017530427071, -2.655922424065692677, 0.1447746667326335335 ) ) ;
#13428=DIRECTION ( 'NONE',  ( -0.000000000000000000, 0.000000000000000000, 1.000000000000000000 ) ) ;
#13433=LINE ( 'NONE', #12103, #8858 ) ;
#13437=DIRECTION ( 'NONE',  ( 0.08093398607328358696, 0.9967194639908912857, 1.383226122518417559E-14 ) ) ;
#13438=ADVANCED_FACE ( 'NONE', ( #6211 ), #2394, .T. ) ;
#13440=AXIS2_PLACEMENT_3D ( 'NONE', #13140, #1393, #14714 ) ;
#13443=CIRCLE ( 'NONE', #5925, 0.01968503937007873988 ) ;
#13448=CARTESIAN_POINT ( 'NONE',  ( -1.929243765392412602, -2.937949247912258866, 0.06324214348988090040 ) ) ;
#13451=DIRECTION ( 'NONE',  ( -0.6722799013647310362, 0.7402970580929166822, 0.000000000000000000 ) ) ;
#13452=CARTESIAN_POINT ( 'NONE',  ( -1.979000582895977356, -2.792299510989483924, -0.1761417809285775182 ) ) ;
#13455=CARTESIAN_POINT ( 'NONE',  ( -1.883869515785526749, -2.912065805618242909, 0.05637122295548225442 ) ) ;
#13460=ORIENTED_EDGE ( 'NONE', *, *, #7552, .T. ) ;
#13464=ORIENTED_EDGE ( 'NONE', *, *, #1760, .T. ) ;
#13469=DIRECTION ( 'NONE',  ( 0.3150766955165275607, -0.9411644975924604584, 0.1222131924708509537 ) ) ;
#13470=CARTESIAN_POINT ( 'NONE',  ( -2.168819294502306594, -1.823050691322464223, 0.1033464566929130080 ) ) ;
#13473=CARTESIAN_POINT ( 'NONE',  ( -1.882336498508431433, -2.915825039791433149, -0.04527253493000575613 ) ) ;
#13476=CARTESIAN_POINT ( 'NONE',  ( -1.590143285779367810, 0.1215581459421218452, 0.06156531251089462919 ) ) ;
#13478=CARTESIAN_POINT ( 'NONE',  ( -1.398125690441303304, -0.003404927804347070153, -0.05905511811023622659 ) ) ;
#13481=EDGE_CURVE ( 'NONE', #9857, #13695, #3794, .T. ) ;
#13486=CARTESIAN_POINT ( 'NONE',  ( -1.387704745771440207, -0.02010536753476144939, -0.03937007874015747977 ) ) ;
#13488=CARTESIAN_POINT ( 'NONE',  ( -0.007502606504445012009, -0.1783918715466182581, -0.01493773385587683807 ) ) ;
#13490=CARTESIAN_POINT ( 'NONE',  ( -2.090051324975654268, -1.858423098537180129, 0.08664193191037310171 ) ) ;
#13492=CARTESIAN_POINT ( 'NONE',  ( -0.06997480235680504645, -0.1674783595965826377, 0.05905511811023622659 ) ) ;
#13497=CARTESIAN_POINT ( 'NONE',  ( -1.979215166314494567, -2.704546138957998114, 0.1698509068488507356 ) ) ;
#13500=CARTESIAN_POINT ( 'NONE',  ( -1.416802626423024680, -0.01064955486146301061, 0.06801238946443101396 ) ) ;
#13512=EDGE_CURVE ( 'NONE', #2402, #12118, #4023, .T. ) ;
#13514=CARTESIAN_POINT ( 'NONE',  ( -1.930132312531408934, -2.935508558968578097, 0.06929162352469166175 ) ) ;
#13516=CARTESIAN_POINT ( 'NONE',  ( -1.180847381051866485, 0.3433074774306730248, -0.04457070858981632827 ) ) ;
#13517=DIRECTION ( 'NONE',  ( 1.000000000000000000, 0.000000000000000000, 0.000000000000000000 ) ) ;
#13519=CARTESIAN_POINT ( 'NONE',  ( 0.9851651268172137987, -1.725292181286280480, -0.08366141732283420562 ) ) ;
#13520=CARTESIAN_POINT ( 'NONE',  ( -1.919180121628701441, -2.820811045952824170, -0.1478741305074587342 ) ) ;
#13524=EDGE_CURVE ( 'NONE', #9980, #8323, #11229, .T. ) ;
#13525=EDGE_LOOP ( 'NONE', ( #14984, #6000, #8533, #13560, #15197, #2294 ) ) ;
#13530=CARTESIAN_POINT ( 'NONE',  ( -1.395815242326012617, -0.02537006130049591218, -0.04028299403797801215 ) ) ;
#13537=CARTESIAN_POINT ( 'NONE',  ( -1.872041180245539449, -2.941023256354079241, 0.05466348536124700924 ) ) ;
#13538=ORIENTED_EDGE ( 'NONE', *, *, #404, .T. ) ;
#13540=CARTESIAN_POINT ( 'NONE',  ( -1.584115185264708847, 0.1296286773226380806, 0.05905511811023622659 ) ) ;
#13548=DIRECTION ( 'NONE',  ( -0.5801894994542512451, -0.8144815189573213488, 0.000000000000000000 ) ) ;
#13550=CARTESIAN_POINT ( 'NONE',  ( -0.002197004598026061628, -0.1775723205537574900, 0.001204381035045432730 ) ) ;
#13560=ORIENTED_EDGE ( 'NONE', *, *, #4194, .F. ) ;
#13563=CARTESIAN_POINT ( 'NONE',  ( -1.999703161025048193, -2.564938650654521091, 0.1343432867203113723 ) ) ;
#13576=ORIENTED_EDGE ( 'NONE', *, *, #546, .T. ) ;
#13578=ORIENTED_EDGE ( 'NONE', *, *, #5843, .T. ) ;
#13581=CARTESIAN_POINT ( 'NONE',  ( -0.2362204724409448231, -0.02638708502139245488, -0.03937007874015747977 ) ) ;
#13582=CARTESIAN_POINT ( 'NONE',  ( -1.950933367886963365, -2.918556150189103526, -0.1002687663322968242 ) ) ;
#13586=AXIS2_PLACEMENT_3D ( 'NONE', #8509, #3805, #14620 ) ;
#13590=CARTESIAN_POINT ( 'NONE',  ( -0.02018259705034725071, -0.1802452534892125813, 1.049219007154695292E-17 ) ) ;
#13591=AXIS2_PLACEMENT_3D ( 'NONE', #3147, #12851, #2122 ) ;
#13594=AXIS2_PLACEMENT_3D ( 'NONE', #6678, #4255, #3078 ) ;
#13598=B_SPLINE_CURVE_WITH_KNOTS ( 'NONE', 3,
 ( #2518, #6191, #1345, #10982, #4951, #11945, #263, #10905 ),
 .UNSPECIFIED., .F., .F.,
 ( 4, 2, 2, 4 ),
 ( 0.000000000000000000, 0.0009271389380264786345, 0.001390708407039718385, 0.001854277876052958136 ),
 .UNSPECIFIED. ) ;
#13599=ORIENTED_EDGE ( 'NONE', *, *, #3420, .T. ) ;
#13600=EDGE_LOOP ( 'NONE', ( #9260, #11693, #14087, #6472 ) ) ;
#13604=CARTESIAN_POINT ( 'NONE',  ( -1.395764539142011706, -0.02487486760722468909, -0.06610458043051951893 ) ) ;
#13609=CARTESIAN_POINT ( 'NONE',  ( -1.574484809660000373, 0.1100025355994882770, 0.06175692796175874522 ) ) ;
#13613=FACE_OUTER_BOUND ( 'NONE', #10966, .T. ) ;
#13615=EDGE_CURVE ( 'NONE', #7004, #14646, #175, .T. ) ;
#13616=DIRECTION ( 'NONE',  ( 0.000000000000000000, -0.000000000000000000, -1.000000000000000000 ) ) ;
#13617=CARTESIAN_POINT ( 'NONE',  ( -1.181342415325297157, 0.3435647566447596613, 0.03937007874014957637 ) ) ;
#13618=CARTESIAN_POINT ( 'NONE',  ( -1.875035009920013040, -2.933829477136298713, -0.07328349893415619931 ) ) ;
#13620=VERTEX_POINT ( 'NONE', #9990 ) ;
#13621=CARTESIAN_POINT ( 'NONE',  ( -2.010991777528383206, -2.758467574604078987, -0.1561691687464118738 ) ) ;
#13622=B_SPLINE_CURVE_WITH_KNOTS ( 'NONE', 3,
 ( #3330, #5818, #15324, #13047 ),
 .UNSPECIFIED., .F., .F.,
 ( 4, 4 ),
 ( 0.02290483811074940299, 0.02857925207800687817 ),
 .UNSPECIFIED. ) ;
#13626=CARTESIAN_POINT ( 'NONE',  ( -0.002500327830562678200, 0.1532658568795227105, 0.000000000000000000 ) ) ;
#13636=AXIS2_PLACEMENT_3D ( 'NONE', #12959, #14214, #11544 ) ;
#13644=CARTESIAN_POINT ( 'NONE',  ( -1.172017912842092668, 0.3609012623030119493, 0.03937007874015747977 ) ) ;
#13649=CARTESIAN_POINT ( 'NONE',  ( -1.407020747027296181, -0.03368500256908527751, -0.04737126204478120384 ) ) ;
#13650=CARTESIAN_POINT ( 'NONE',  ( -1.959562855619890964, -2.764754912074676607, 0.1771653543307128986 ) ) ;
#13651=EDGE_CURVE ( 'NONE', #3617, #1942, #2661, .T. ) ;
#13652=AXIS2_PLACEMENT_3D ( 'NONE', #1, #7192, #3444 ) ;
#13658=ADVANCED_FACE ( 'NONE', ( #4561 ), #3169, .T. ) ;
#13661=CARTESIAN_POINT ( 'NONE',  ( -1.945459748359986030, -2.745801194614590823, 0.1561691687464110689 ) ) ;
#13664=DIRECTION ( 'NONE',  ( -1.000000000000000000, 0.000000000000000000, 0.000000000000000000 ) ) ;
#13671=CIRCLE ( 'NONE', #2166, 0.01968503937007874682 ) ;
#13678=EDGE_CURVE ( 'NONE', #9785, #10031, #6823, .T. ) ;
#13683=CARTESIAN_POINT ( 'NONE',  ( -1.591501945092674841, 0.08600752902535289957, -0.1033464566929133410 ) ) ;
#13686=CARTESIAN_POINT ( 'NONE',  ( -1.977060571132597255, -2.798357741064777748, -0.1753504618005770066 ) ) ;
#13688=MECHANICAL_DESIGN_GEOMETRIC_PRESENTATION_REPRESENTATION('',(#2928),#2181);
#13690=CARTESIAN_POINT ( 'NONE',  ( -1.895297964913681854, -2.883558765292476345, -0.1043903633197201947 ) ) ;
#13691=CARTESIAN_POINT ( 'NONE',  ( -1.409916934715107484, -0.04334312390809511029, 0.08366141732283458032 ) ) ;
#13695=VERTEX_POINT ( 'NONE', #1135 ) ;
#13699=ORIENTED_EDGE ( 'NONE', *, *, #7087, .F. ) ;
#13706=DIRECTION ( 'NONE',  ( 1.000000000000000000, 0.000000000000000000, 0.000000000000000000 ) ) ;
#13709=CARTESIAN_POINT ( 'NONE',  ( -1.398495881576244937, -0.02731002314121834529, -0.07874015748031495954 ) ) ;
#13710=CARTESIAN_POINT ( 'NONE',  ( -1.879669289221657547, -2.922326730264934724, -0.005526921115518252693 ) ) ;
#13712=DIRECTION ( 'NONE',  ( 0.000000000000000000, 2.212657494868377674E-16, -1.000000000000000000 ) ) ;
#13717=ORIENTED_EDGE ( 'NONE', *, *, #1283, .T. ) ;
#13720=ORIENTED_EDGE ( 'NONE', *, *, #9806, .F. ) ;
#13721=EDGE_CURVE ( 'NONE', #13899, #9959, #13671, .T. ) ;
#13723=AXIS2_PLACEMENT_3D ( 'NONE', #1568, #2910, #13320 ) ;
#13729=DIRECTION ( 'NONE',  ( 0.000000000000000000, 0.000000000000000000, -1.000000000000000000 ) ) ;
#13733=DIRECTION ( 'NONE',  ( -0.000000000000000000, -0.000000000000000000, -1.000000000000000000 ) ) ;
#13738=VERTEX_POINT ( 'NONE', #8182 ) ;
#13740=DIRECTION ( 'NONE',  ( 0.000000000000000000, 2.212657494868377674E-16, 1.000000000000000000 ) ) ;
#13750=DIRECTION ( 'NONE',  ( 1.000000000000000000, 0.000000000000000000, 0.000000000000000000 ) ) ;
#13757=DIRECTION ( 'NONE',  ( 0.8144815189573203495, -0.5801894994542524664, 0.000000000000000000 ) ) ;
#13758=CARTESIAN_POINT ( 'NONE',  ( -1.977712674129580073, -2.850429627681845268, 0.1595853951502894108 ) ) ;
#13760=CARTESIAN_POINT ( 'NONE',  ( -1.190198933766853706, 0.3259758027579612860, -0.05905511811023622659 ) ) ;
#13764=EDGE_CURVE ( 'NONE', #7635, #749, #8170, .T. ) ;
#13765=CYLINDRICAL_SURFACE ( 'NONE', #8330, 0.01968503937007871907 ) ;
#13766=CARTESIAN_POINT ( 'NONE',  ( -2.005376571220952364, -2.566823862150081847, -0.1327647275340299027 ) ) ;
#13768=EDGE_LOOP ( 'NONE', ( #13599, #6421, #15329, #13322 ) ) ;
#13781=CARTESIAN_POINT ( 'NONE',  ( -1.892078352146237652, -2.891862086400596166, -0.1315695375898782160 ) ) ;
#13783=CARTESIAN_POINT ( 'NONE',  ( -2.119211488178678771, -2.391206066312333345, -0.1145569965096258497 ) ) ;
#13792=CARTESIAN_POINT ( 'NONE',  ( -1.185589860596527823, 0.3351407497371320376, -0.05695314934232800774 ) ) ;
#13796=CARTESIAN_POINT ( 'NONE',  ( -1.181342415325333350, 0.3435647566446739520, 0.05905511811023622659 ) ) ;
#13797=EDGE_CURVE ( 'NONE', #14935, #8061, #1507, .T. ) ;
#13807=CARTESIAN_POINT ( 'NONE',  ( -0.002322522588111458446, 0.1532890258252369575, 0.0007019553870511914279 ) ) ;
#13813=CARTESIAN_POINT ( 'NONE',  ( -2.111626822439224060, -2.421545435136615687, -0.1175637245596493491 ) ) ;
#13814=DIRECTION ( 'NONE',  ( -0.8144815189573203495, 0.5801894994542524664, 1.283760644411384150E-16 ) ) ;
#13818=EDGE_LOOP ( 'NONE', ( #1237, #4560, #14844, #12296, #8229 ) ) ;
#13823=CARTESIAN_POINT ( 'NONE',  ( -2.029388000666335845, -2.456681529620341475, -0.1220450449751008942 ) ) ;
#13825=CARTESIAN_POINT ( 'NONE',  ( -1.936923698693393536, -2.916673061415975265, -0.1029210798408209532 ) ) ;
#13831=AXIS2_PLACEMENT_3D ( 'NONE', #14716, #1395, #5133 ) ;
#13841=FACE_OUTER_BOUND ( 'NONE', #6502, .T. ) ;
#13850=CARTESIAN_POINT ( 'NONE',  ( -0.2362204724409448231, -0.02638708502139245488, 0.03937007874015747977 ) ) ;
#13851=CARTESIAN_POINT ( 'NONE',  ( -1.960453476960047681, -2.761858712000560434, -0.1772931260763774275 ) ) ;
#13863=CARTESIAN_POINT ( 'NONE',  ( -1.293236445124221312, 0.1355266887446167634, 0.05905511811023622659 ) ) ;
#13864=ADVANCED_FACE ( 'NONE', ( #12021 ), #14994, .T. ) ;
#13866=CARTESIAN_POINT ( 'NONE',  ( -1.431036756819011213, -0.02829858486107876200, 0.08366141732283460808 ) ) ;
#13867=FACE_OUTER_BOUND ( 'NONE', #811, .T. ) ;
#13875=AXIS2_PLACEMENT_3D ( 'NONE', #7272, #1551, #7506 ) ;
#13876=CARTESIAN_POINT ( 'NONE',  ( -1.417802900492933782, -0.04287136159519135820, -0.07874015748031495954 ) ) ;
#13877=DIRECTION ( 'NONE',  ( -1.000000000000000000, 0.000000000000000000, 0.000000000000000000 ) ) ;
#13879=DIRECTION ( 'NONE',  ( 0.000000000000000000, 0.000000000000000000, -1.000000000000000000 ) ) ;
#13882=EDGE_LOOP ( 'NONE', ( #9279, #3382, #1953, #12242, #13460, #12605, #4129, #6143 ) ) ;
#13884=CIRCLE ( 'NONE', #7126, 0.05905511811023627516 ) ;
#13885=CARTESIAN_POINT ( 'NONE',  ( -1.985311755390524624, -2.772329397582317778, 0.1771653543307079026 ) ) ;
#13897=AXIS2_PLACEMENT_3D ( 'NONE', #4926, #13069, #11916 ) ;
#13899=VERTEX_POINT ( 'NONE', #7231 ) ;
#13920=DIRECTION ( 'NONE',  ( -1.000000000000000000, 0.000000000000000000, 0.000000000000000000 ) ) ;
#13934=CARTESIAN_POINT ( 'NONE',  ( -0.07002222008683997578, -0.1674826920712330913, -0.05905511811023624741 ) ) ;
#13935=LINE ( 'NONE', #13709, #3185 ) ;
#13937=CARTESIAN_POINT ( 'NONE',  ( -1.946192867917151847, -2.743611295743893397, -0.1749236412511677441 ) ) ;
#13942=ORIENTED_EDGE ( 'NONE', *, *, #13174, .F. ) ;
#13957=DIRECTION ( 'NONE',  ( -0.000000000000000000, -0.000000000000000000, -1.000000000000000000 ) ) ;
#13960=EDGE_CURVE ( 'NONE', #877, #15414, #9182, .T. ) ;
#13961=LINE ( 'NONE', #874, #1097 ) ;
#13968=VERTEX_POINT ( 'NONE', #8863 ) ;
#13972=CARTESIAN_POINT ( 'NONE',  ( -0.05072818602969170199, 0.1683578795566404995, -0.03094016780478001452 ) ) ;
#13976=CARTESIAN_POINT ( 'NONE',  ( -0.04711866733795021939, -0.1840656518295271660, 0.03212400068286348082 ) ) ;
#13980=DIRECTION ( 'NONE',  ( -0.000000000000000000, 0.000000000000000000, 1.000000000000000000 ) ) ;
#13982=DIRECTION ( 'NONE',  ( 0.000000000000000000, 2.212657494868377674E-16, -1.000000000000000000 ) ) ;
#13987=DIRECTION ( 'NONE',  ( 0.000000000000000000, 2.212657494868377674E-16, 1.000000000000000000 ) ) ;
#13991=CARTESIAN_POINT ( 'NONE',  ( -1.990392212731196375, -2.816401147560732898, 0.1718120134069966720 ) ) ;
#13994=CARTESIAN_POINT ( 'NONE',  ( -1.401197114347125794, -0.004216232782927999655, 0.05905511811023622659 ) ) ;
#13996=DIRECTION ( 'NONE',  ( 0.8011800915434493797, -0.5984233124757342148, 0.000000000000000000 ) ) ;
#13999=ORIENTED_EDGE ( 'NONE', *, *, #5648, .F. ) ;
#14000=ORIENTED_EDGE ( 'NONE', *, *, #10687, .T. ) ;
#14001=VERTEX_POINT ( 'NONE', #496 ) ;
#14007=CARTESIAN_POINT ( 'NONE',  ( -0.07500546397816790223, 0.1646499958011359843, 0.03937007824588655003 ) ) ;
#14011=CARTESIAN_POINT ( 'NONE',  ( -1.930618484338028740, -2.788977046644874669, -0.1558575928594421456 ) ) ;
#14013=CARTESIAN_POINT ( 'NONE',  ( -0.2952755905511810219, -0.02638708502139244794, -0.03937007874015747977 ) ) ;
#14018=ORIENTED_EDGE ( 'NONE', *, *, #171, .T. ) ;
#14020=EDGE_LOOP ( 'NONE', ( #7212, #2602, #9770, #7063 ) ) ;
#14022=DIRECTION ( 'NONE',  ( -0.000000000000000000, 0.000000000000000000, 1.000000000000000000 ) ) ;
#14023=CARTESIAN_POINT ( 'NONE',  ( -1.978181763874820032, -2.794902419994705234, 0.1760903034428087099 ) ) ;
#14036=EDGE_CURVE ( 'NONE', #15416, #5248, #1187, .T. ) ;
#14042=DIRECTION ( 'NONE',  ( -1.000000000000000000, 0.000000000000000000, 0.000000000000000000 ) ) ;
#14045=LINE ( 'NONE', #10592, #362 ) ;
#14056=ORIENTED_EDGE ( 'NONE', *, *, #5670, .F. ) ;
#14065=( CONVERSION_BASED_UNIT ( 'INCH', #6843 ) LENGTH_UNIT ( ) NAMED_UNIT ( #10673 ) );
#14070=ORIENTED_EDGE ( 'NONE', *, *, #10230, .F. ) ;
#14071=CARTESIAN_POINT ( 'NONE',  ( 0.7052242655755273093, -1.858423098537180129, -0.08366141732283413623 ) ) ;
#14072=CARTESIAN_POINT ( 'NONE',  ( -1.511943070284283097, 0.2262540267724840182, 0.03937007874015747977 ) ) ;
#14074=CARTESIAN_POINT ( 'NONE',  ( -0.06427269473108324083, 0.1662356183067242588, 0.05825535267941785861 ) ) ;
#14075=DIRECTION ( 'NONE',  ( -0.000000000000000000, -0.000000000000000000, -1.000000000000000000 ) ) ;
#14080=CARTESIAN_POINT ( 'NONE',  ( -1.496171808639726875, 0.2144740403064263057, 0.03937007874015747977 ) ) ;
#14086=VERTEX_POINT ( 'NONE', #6978 ) ;
#14087=ORIENTED_EDGE ( 'NONE', *, *, #7042, .F. ) ;
#14096=CYLINDRICAL_SURFACE ( 'NONE', #8371, 3.169291338582677753 ) ;
#14098=CARTESIAN_POINT ( 'NONE',  ( -1.190198933766848377, 0.3259758027579584549, -0.05905511811023622659 ) ) ;
#14106=CARTESIAN_POINT ( 'NONE',  ( -1.602365476182131099, 0.1047621256497578840, 0.05341113178340452933 ) ) ;
#14117=CIRCLE ( 'NONE', #4607, 0.01968503937007871907 ) ;
#14121=CARTESIAN_POINT ( 'NONE',  ( -0.04489243112415652881, 0.1480120765563566754, -0.05194558739575130119 ) ) ;
#14123=CIRCLE ( 'NONE', #14367, 0.01968503937007875723 ) ;
#14125=AXIS2_PLACEMENT_3D ( 'NONE', #6582, #11383, #4249 ) ;
#14128=VERTEX_POINT ( 'NONE', #9417 ) ;
#14136=CIRCLE ( 'NONE', #13636, 0.01968503937007876417 ) ;
#14151=DIRECTION ( 'NONE',  ( 1.000000000000000000, -3.469446951953611428E-15, 0.000000000000000000 ) ) ;
#14154=CIRCLE ( 'NONE', #4377, 3.149606299212599048 ) ;
#14157=ADVANCED_FACE ( 'NONE', ( #15211 ), #7047, .T. ) ;
#14162=VERTEX_POINT ( 'NONE', #12846 ) ;
#14167=CYLINDRICAL_SURFACE ( 'NONE', #11867, 0.01968503937007871907 ) ;
#14168=CARTESIAN_POINT ( 'NONE',  ( -0.08151194962748882500, 0.1637246173173400321, 0.03937007874015747977 ) ) ;
#14169=CARTESIAN_POINT ( 'NONE',  ( -0.02371960882139430987, -0.1628608293428424891, -0.03730919803856837247 ) ) ;
#14173=ORIENTED_EDGE ( 'NONE', *, *, #3664, .F. ) ;
#14179=EDGE_LOOP ( 'NONE', ( #3155, #13538, #5737, #13578 ) ) ;
#14180=VERTEX_POINT ( 'NONE', #2118 ) ;
#14183=AXIS2_PLACEMENT_3D ( 'NONE', #4391, #11522, #959 ) ;
#14185=DIRECTION ( 'NONE',  ( -1.000000000000000000, 0.000000000000000000, 0.000000000000000000 ) ) ;
#14188=CARTESIAN_POINT ( 'NONE',  ( -1.916768853550577134, -2.896547607920614720, 0.1269301806022984647 ) ) ;
#14196=CARTESIAN_POINT ( 'NONE',  ( -1.293236445124221312, 0.1355266887446167634, -0.03937007874015747977 ) ) ;
#14198=EDGE_CURVE ( 'NONE', #8323, #9995, #11972, .T. ) ;
#14207=CARTESIAN_POINT ( 'NONE',  ( -1.417802899857368182, -0.04287136101802047766, 0.07345918205385276734 ) ) ;
#14209=SPHERICAL_SURFACE ( 'NONE', #14709, 0.01968503937007873988 ) ;
#14211=CARTESIAN_POINT ( 'NONE',  ( -1.491640810881974977, 0.2222636556240916161, 0.03937007874015747977 ) ) ;
#14212=EDGE_LOOP ( 'NONE', ( #5599, #5992, #7558, #1983 ) ) ;
#14213=CARTESIAN_POINT ( 'NONE',  ( -1.398125690441303304, -0.003404927804347041096, -0.03937007874015747977 ) ) ;
#14214=DIRECTION ( 'NONE',  ( -0.5163221703236040572, -0.6912615786549138885, 0.5055381749263252456 ) ) ;
#14219=EDGE_CURVE ( 'NONE', #4395, #5049, #7181, .T. ) ;
#14230=CARTESIAN_POINT ( 'NONE',  ( -1.929411732541991720, -2.859457149331156689, 0.1546924827060817687 ) ) ;
#14234=CARTESIAN_POINT ( 'NONE',  ( -1.579560458409178914, 0.1027931408841043642, -0.07190451969745018101 ) ) ;
#14235=CARTESIAN_POINT ( 'NONE',  ( -1.391807345368153870, -0.02266535781586121248, 0.03937007891299400264 ) ) ;
#14237=DIRECTION ( 'NONE',  ( -0.4005670834070305664, -0.9162674345903522033, -0.000000000000000000 ) ) ;
#14238=VERTEX_POINT ( 'NONE', #3762 ) ;
#14245=CARTESIAN_POINT ( 'NONE',  ( -0.02479723250354462505, 0.1726834024554401437, -0.005447726382807938084 ) ) ;
#14248=CARTESIAN_POINT ( 'NONE',  ( -1.580259682937487753, 0.1018956540318995824, -0.04477369844321314740 ) ) ;
#14257=CARTESIAN_POINT ( 'NONE',  ( -1.992382107315058271, -2.749515453455440905, 0.1756903148397124803 ) ) ;
#14258=DIRECTION ( 'NONE',  ( 0.5984233124757303290, 0.8011800915434521553, -0.000000000000000000 ) ) ;
#14260=EDGE_CURVE ( 'NONE', #9440, #15416, #5229, .T. ) ;
#14264=CARTESIAN_POINT ( 'NONE',  ( -1.181096721277146377, 0.3434326092093292204, -0.03937007874014959025 ) ) ;
#14266=CARTESIAN_POINT ( 'NONE',  ( -1.995625621700811925, -2.802058942328566893, 0.1561600152793889418 ) ) ;
#14276=CARTESIAN_POINT ( 'NONE',  ( -1.403183357138765963, -0.03069084635762514210, 0.04402914006448389178 ) ) ;
#14293=DIRECTION ( 'NONE',  ( 1.000000000000000000, -0.000000000000000000, -0.000000000000000000 ) ) ;
#14304=CARTESIAN_POINT ( 'NONE',  ( -1.403713693041773514, -0.03108975223222291279, 0.04439787872945648306 ) ) ;
#14308=ORIENTED_EDGE ( 'NONE', *, *, #9403, .T. ) ;
#14310=DIRECTION ( 'NONE',  ( -1.000000000000000000, 2.168404344971007142E-16, 0.000000000000000000 ) ) ;
#14311=ADVANCED_FACE ( 'NONE', ( #6310 ), #6979, .T. ) ;
#14320=CARTESIAN_POINT ( 'NONE',  ( -1.591501945092674841, 0.08600752902535285793, -0.08366141732283460808 ) ) ;
#14322=EDGE_LOOP ( 'NONE', ( #3084, #5346, #9486, #2651, #7230 ) ) ;
#14324=ADVANCED_FACE ( 'NONE', ( #10097 ), #15452, .T. ) ;
#14327=CARTESIAN_POINT ( 'NONE',  ( -1.607606114292111643, 0.09732815221480045631, 0.07874015748031495954 ) ) ;
#14328=CARTESIAN_POINT ( 'NONE',  ( -1.929310418580271191, -2.937766263536936151, -0.06371700066512400729 ) ) ;
#14329=DIRECTION ( 'NONE',  ( 1.000000000000000000, -0.000000000000000000, -0.000000000000000000 ) ) ;
#14330=CARTESIAN_POINT ( 'NONE',  ( -0.05260779769176850140, -0.1848037158363092514, -0.03481219553824698582 ) ) ;
#14333=CARTESIAN_POINT ( 'NONE',  ( -2.111938395807090529, -2.009781522894384054, 0.1096056828055473470 ) ) ;
#14334=ORIENTED_EDGE ( 'NONE', *, *, #3280, .F. ) ;
#14335=CARTESIAN_POINT ( 'NONE',  ( -1.951527508739262728, -2.917036378191013135, -0.07732708326134817012 ) ) ;
#14339=EDGE_LOOP ( 'NONE', ( #9853, #2652, #1652, #9583 ) ) ;
#14347=CARTESIAN_POINT ( 'NONE',  ( -1.417055254560940947, -0.04218366875896984586, 0.06815127639898536926 ) ) ;
#14349=DIRECTION ( 'NONE',  ( 5.688234090747695582E-25, 1.000000000000000000, 6.210310043996969398E-13 ) ) ;
#14352=ORIENTED_EDGE ( 'NONE', *, *, #7757, .T. ) ;
#14353=CARTESIAN_POINT ( 'NONE',  ( -1.602629991056316650, 0.1043896402808425078, -0.05327537141226647288 ) ) ;
#14358=CARTESIAN_POINT ( 'NONE',  ( -0.07002222008683994803, -0.1674826920712332579, 0.05905511811023622659 ) ) ;
#14367=AXIS2_PLACEMENT_3D ( 'NONE', #2665, #12237, #11034 ) ;
#14369=TOROIDAL_SURFACE ( 'NONE', #3379, 0.05905511811023614333, 0.01968503937007873988 ) ;
#14372=CARTESIAN_POINT ( 'NONE',  ( -1.922849157407968246, -2.878884448036508115, -0.1420113206368266712 ) ) ;
#14375=CARTESIAN_POINT ( 'NONE',  ( -0.06956272065387619774, 0.1654544434110864770, 0.03844121289758908183 ) ) ;
#14383=AXIS2_PLACEMENT_3D ( 'NONE', #5627, #14022, #12542 ) ;
#14386=CIRCLE ( 'NONE', #6866, 0.01968503937007871907 ) ;
#14396=EDGE_CURVE ( 'NONE', #7929, #5808, #8692, .T. ) ;
#14400=CARTESIAN_POINT ( 'NONE',  ( -0.2362204724409448231, -0.02638708502139245488, 0.05905511811023622659 ) ) ;
#14406=CARTESIAN_POINT ( 'NONE',  ( -2.184126211765464287, -1.693613514254861174, -0.08383392658277005749 ) ) ;
#14417=EDGE_CURVE ( 'NONE', #6036, #14128, #13443, .T. ) ;
#14418=CARTESIAN_POINT ( 'NONE',  ( -1.606548329185377932, 0.09883514492709696841, 0.06506891156472163762 ) ) ;
#14420=AXIS2_PLACEMENT_3D ( 'NONE', #7782, #13987, #9356 ) ;
#14423=CARTESIAN_POINT ( 'NONE',  ( -1.293236445124221312, 0.1355266887446167634, 0.05905511811023622659 ) ) ;
#14426=CARTESIAN_POINT ( 'NONE',  ( -1.923189478754104176, -2.809775139800132493, 0.1734120223863747368 ) ) ;
#14430=CARTESIAN_POINT ( 'NONE',  ( -0.02374036903667607959, 0.1505616924844533355, -0.03732860159234810404 ) ) ;
#14431=ORIENTED_EDGE ( 'NONE', *, *, #13512, .T. ) ;
#14440=FACE_OUTER_BOUND ( 'NONE', #2059, .T. ) ;
#14441=PLANE ( 'NONE',  #9637 ) ;
#14453=VERTEX_POINT ( 'NONE', #6717 ) ;
#14455=ORIENTED_EDGE ( 'NONE', *, *, #10166, .T. ) ;
#14459=CIRCLE ( 'NONE', #1210, 2.194881889763779181 ) ;
#14460=CARTESIAN_POINT ( 'NONE',  ( -1.293236445124221312, 0.1355266887446167634, 0.03937007874015747977 ) ) ;
#14461=CARTESIAN_POINT ( 'NONE',  ( -1.591501945092674841, 0.08600752902535294120, -0.07874015748031495954 ) ) ;
#14472=AXIS2_PLACEMENT_3D ( 'NONE', #486, #1650, #7576 ) ;
#14483=CARTESIAN_POINT ( 'NONE',  ( -1.527714331928839098, 0.2380340132385416752, -0.03937007874015747977 ) ) ;
#14489=EDGE_CURVE ( 'NONE', #15344, #10478, #9196, .T. ) ;
#14491=ORIENTED_EDGE ( 'NONE', *, *, #9143, .F. ) ;
#14499=CARTESIAN_POINT ( 'NONE',  ( -2.030412493207266689, -2.521649992949083874, 0.1490301379651515212 ) ) ;
#14508=CARTESIAN_POINT ( 'NONE',  ( -1.527714331928839098, 0.2380340132385416752, 0.05905511811023622659 ) ) ;
#14512=CARTESIAN_POINT ( 'NONE',  ( -1.398495881576244493, -0.02731002314121873387, 0.1968503937007874127 ) ) ;
#14514=CARTESIAN_POINT ( 'NONE',  ( -1.187759231255085313, 0.3304857737014040842, 0.05905511811023624741 ) ) ;
#14515=ADVANCED_FACE ( 'NONE', ( #15037 ), #9698, .T. ) ;
#14518=DIRECTION ( 'NONE',  ( 0.5750876580239430158, 0.8180917953313895374, 0.000000000000000000 ) ) ;
#14520=CARTESIAN_POINT ( 'NONE',  ( -0.02220179245438124935, -0.1805881202044197775, 0.03580963740886420471 ) ) ;
#14529=FACE_OUTER_BOUND ( 'NONE', #2825, .T. ) ;
#14536=DIRECTION ( 'NONE',  ( -0.5005078764078491060, -0.7027276007399325675, -0.5056340423784807525 ) ) ;
#14542=CARTESIAN_POINT ( 'NONE',  ( -1.964126537190516331, -2.749515453455444014, -0.1756903148397123138 ) ) ;
#14551=ORIENTED_EDGE ( 'NONE', *, *, #15054, .F. ) ;
#14556=VERTEX_POINT ( 'NONE', #10721 ) ;
#14557=DIRECTION ( 'NONE',  ( 1.000000000000000000, 0.000000000000000000, 0.000000000000000000 ) ) ;
#14564=CARTESIAN_POINT ( 'NONE',  ( -1.895376452690201940, -2.883359828382185963, -0.1046187747444000948 ) ) ;
#14568=ORIENTED_EDGE ( 'NONE', *, *, #11355, .F. ) ;
#14575=DIRECTION ( 'NONE',  ( -0.000000000000000000, -0.000000000000000000, -1.000000000000000000 ) ) ;
#14579=CARTESIAN_POINT ( 'NONE',  ( -0.05074681685833758865, -0.1845569960845552526, -0.03403827111684314816 ) ) ;
#14583=DIRECTION ( 'NONE',  ( 0.000000000000000000, -0.000000000000000000, 1.000000000000000000 ) ) ;
#14588=CIRCLE ( 'NONE', #10584, 0.01968503937007875723 ) ;
#14601=CARTESIAN_POINT ( 'NONE',  ( -1.993158829383584019, -2.659208322459291285, 0.1643215684482012828 ) ) ;
#14618=ORIENTED_EDGE ( 'NONE', *, *, #1110, .T. ) ;
#14620=DIRECTION ( 'NONE',  ( 1.000000000000000000, 0.000000000000000000, 0.000000000000000000 ) ) ;
#14621=CARTESIAN_POINT ( 'NONE',  ( -1.927720146670603762, -2.942124612819895901, 0.05098125556452735158 ) ) ;
#14626=DIRECTION ( 'NONE',  ( 6.667973881468103839E-14, 9.362029067655382729E-14, -1.000000000000000000 ) ) ;
#14627=AXIS2_PLACEMENT_3D ( 'NONE', #14979, #9173, #7752 ) ;
#14629=AXIS2_PLACEMENT_3D ( 'NONE', #5748, #9535, #15412 ) ;
#14631=TOROIDAL_SURFACE ( 'NONE', #7865, 2.814960629921260171, 0.01968503937007873988 ) ;
#14633=EDGE_CURVE ( 'NONE', #15414, #4395, #7643, .T. ) ;
#14634=PLANE ( 'NONE',  #4449 ) ;
#14635=CARTESIAN_POINT ( 'NONE',  ( -1.930582750161468297, -2.789131037002329006, 0.1561188479113173599 ) ) ;
#14645=EDGE_LOOP ( 'NONE', ( #4418, #2759, #3297, #10210, #12570 ) ) ;
#14646=VERTEX_POINT ( 'NONE', #1624 ) ;
#14648=CARTESIAN_POINT ( 'NONE',  ( -1.417802900119197629, -0.04287136125579330687, -0.07339284414834101877 ) ) ;
#14652=CIRCLE ( 'NONE', #8637, 0.01968503937007875723 ) ;
#14655=CARTESIAN_POINT ( 'NONE',  ( -1.899925859588517341, -2.943879019075679615, -0.04472015565144684540 ) ) ;
#14666=CIRCLE ( 'NONE', #1412, 0.01968503937007867396 ) ;
#14669=CARTESIAN_POINT ( 'NONE',  ( -1.945459748359985142, -2.745801194614594820, -0.1561691687464109024 ) ) ;
#14671=FACE_OUTER_BOUND ( 'NONE', #14212, .T. ) ;
#14672=DIRECTION ( 'NONE',  ( 1.000000000000000000, -1.349229370204184369E-15, 0.000000000000000000 ) ) ;
#14675=EDGE_CURVE ( 'NONE', #9296, #4567, #14459, .T. ) ;
#14685=EDGE_CURVE ( 'NONE', #7280, #9606, #12710, .T. ) ;
#14691=CARTESIAN_POINT ( 'NONE',  ( -2.000227613418059214, -2.562930154573033636, 0.1533876257101599305 ) ) ;
#14694=CARTESIAN_POINT ( 'NONE',  ( -1.419615703680148000, -0.01226548409420233701, 0.07587259468772762638 ) ) ;
#14696=CARTESIAN_POINT ( 'NONE',  ( -0.2952755905511810219, -0.02638708502139244100, 0.05905511811023622659 ) ) ;
#14709=AXIS2_PLACEMENT_3D ( 'NONE', #3478, #14349, #10682 ) ;
#14711=CARTESIAN_POINT ( 'NONE',  ( -1.945925679626857141, -2.930745767159171233, 0.04531667161755153356 ) ) ;
#14714=DIRECTION ( 'NONE',  ( 1.000000000000000000, 0.000000000000000000, 0.000000000000000000 ) ) ;
#14716=CARTESIAN_POINT ( 'NONE',  ( -1.591501945092674175, 0.08600752902535260813, 0.08366141732283462196 ) ) ;
#14718=CARTESIAN_POINT ( 'NONE',  ( -1.889966060128447367, -2.896982825862624011, 0.08667069204985511366 ) ) ;
#14725=AXIS2_PLACEMENT_3D ( 'NONE', #1662, #8543, #14672 ) ;
#14729=ORIENTED_EDGE ( 'NONE', *, *, #4265, .T. ) ;
#14732=ADVANCED_FACE ( 'NONE', ( #12798 ), #14634, .F. ) ;
#14734=CARTESIAN_POINT ( 'NONE',  ( -1.276200637803905691, -0.1988000726501942539, 0.03937007874015747977 ) ) ;
#14736=CARTESIAN_POINT ( 'NONE',  ( -2.176528721278613077, -2.014897391720707365, 0.1098265554920595383 ) ) ;
#14739=ADVANCED_BREP_SHAPE_REPRESENTATION ( '', ( #9754, #11481 ), #9487 ) ;
#14740=CARTESIAN_POINT ( 'NONE',  ( -1.897872764959702474, -2.949505210859929782, -0.006217786254915346096 ) ) ;
#14743=CARTESIAN_POINT ( 'NONE',  ( -1.592432191551354848, 0.1184937169706836296, 0.04125010960145494843 ) ) ;
#14744=DIRECTION ( 'NONE',  ( 1.000000000000000000, 0.000000000000000000, 0.000000000000000000 ) ) ;
#14751=DIRECTION ( 'NONE',  ( -0.000000000000000000, 0.000000000000000000, 1.000000000000000000 ) ) ;
#14753=LINE ( 'NONE', #10036, #9646 ) ;
#14757=CARTESIAN_POINT ( 'NONE',  ( -0.02345217991005641225, -0.1628325660491150295, 0.03705913340085396912 ) ) ;
#14760=ORIENTED_EDGE ( 'NONE', *, *, #8925, .T. ) ;
#14764=CARTESIAN_POINT ( 'NONE',  ( -0.06427269473107563580, 0.1662356183066786008, -0.05825535267941485407 ) ) ;
#14779=CARTESIAN_POINT ( 'NONE',  ( -1.943213546182679163, -2.937317732503017531, -0.01185211799045717516 ) ) ;
#14782=FACE_BOUND ( 'NONE', #8534, .T. ) ;
#14784=FACE_OUTER_BOUND ( 'NONE', #15239, .T. ) ;
#14785=CARTESIAN_POINT ( 'NONE',  ( -0.004403105188762939347, -0.1701273036488648305, 3.906667514412696694E-16 ) ) ;
#14786=CARTESIAN_POINT ( 'NONE',  ( -1.992382107315057160, -2.749515453455444014, -0.1756903148397123138 ) ) ;
#14788=VERTEX_POINT ( 'NONE', #35 ) ;
#14790=VERTEX_POINT ( 'NONE', #1576 ) ;
#14794=EDGE_CURVE ( 'NONE', #3678, #7280, #9717, .T. ) ;
#14797=DIRECTION ( 'NONE',  ( -0.000000000000000000, -0.000000000000000000, -1.000000000000000000 ) ) ;
#14798=DIRECTION ( 'NONE',  ( -0.000000000000000000, -0.000000000000000000, 1.000000000000000000 ) ) ;
#14802=CARTESIAN_POINT ( 'NONE',  ( -1.904949078685900909, -2.929982408226253110, 0.08107751447060709826 ) ) ;
#14805=CARTESIAN_POINT ( 'NONE',  ( -1.190198933766853706, 0.3259758027579612860, -0.05905511811023622659 ) ) ;
#14806=VERTEX_POINT ( 'NONE', #3633 ) ;
#14825=ORIENTED_EDGE ( 'NONE', *, *, #13721, .T. ) ;
#14829=FACE_OUTER_BOUND ( 'NONE', #14339, .T. ) ;
#14835=CARTESIAN_POINT ( 'NONE',  ( -2.010991777528384095, -2.758467574604078543, -0.1561691687464109024 ) ) ;
#14844=ORIENTED_EDGE ( 'NONE', *, *, #9901, .F. ) ;
#14848=CARTESIAN_POINT ( 'NONE',  ( -1.988221238975143690, -2.822304858211031942, 0.1701874367289316903 ) ) ;
#14851=CARTESIAN_POINT ( 'NONE',  ( -1.991649887250016571, -2.812956183489762285, -0.1538914628651122662 ) ) ;
#14855=CARTESIAN_POINT ( 'NONE',  ( -1.904776753227351849, -2.859193012224173991, -0.1268975449324867832 ) ) ;
#14860=CIRCLE ( 'NONE', #2838, 0.03937007874015751446 ) ;
#14861=ADVANCED_FACE ( 'NONE', ( #9897 ), #13383, .T. ) ;
#14864=ORIENTED_EDGE ( 'NONE', *, *, #6550, .F. ) ;
#14870=CARTESIAN_POINT ( 'NONE',  ( -1.399418326858319572, -0.02634099999489962138, -0.07486975863450967550 ) ) ;
#14875=TOROIDAL_SURFACE ( 'NONE', #3362, 1.885039370078740451, 0.01968503937007873988 ) ;
#14878=DIRECTION ( 'NONE',  ( -0.000000000000000000, 0.000000000000000000, 1.000000000000000000 ) ) ;
#14881=CARTESIAN_POINT ( 'NONE',  ( -1.181845651245105211, 0.3414517841021337818, 0.04963174987413059014 ) ) ;
#14882=CARTESIAN_POINT ( 'NONE',  ( -1.881745788400430719, -2.917268413851039188, 0.04011020394780418635 ) ) ;
#14884=CARTESIAN_POINT ( 'NONE',  ( -2.182693454834259139, -1.630005269948474389, -0.08366141732283419175 ) ) ;
#14888=VECTOR ( 'NONE', #8129, 39.37007874015748143 ) ;
#14895=EDGE_CURVE ( 'NONE', #4530, #1873, #11133, .T. ) ;
#14902=( BOUNDED_SURFACE ( )  B_SPLINE_SURFACE ( 3, 2, ( 
 ( #3914, #12063, #11102 ),
 ( #8527, #13302, #2429 ),
 ( #1325, #245, #8697 ),
 ( #4842, #14736, #8607 ),
 ( #13470, #13391, #7432 ),
 ( #1553, #12148, #2566 ) ),
 .UNSPECIFIED., .F., .F., .T. ) 
 B_SPLINE_SURFACE_WITH_KNOTS ( ( 4, 2, 4 ),
 ( 3, 3 ),
 ( 0.000000000000000000, 0.01443577820670500188, 0.02887155641341000376 ),
 ( 0.000000000000000000, 1.000000000000000000 ),
 .UNSPECIFIED. ) 
 GEOMETRIC_REPRESENTATION_ITEM ( )  RATIONAL_B_SPLINE_SURFACE ( (
 ( 1.000000000000000000, 0.6921057963906867005, 1.000000000000000000),
 ( 1.000000000000000000, 0.6972252234924993797, 1.000000000000000000),
 ( 1.000000000000000000, 0.7010830952492357326, 1.000000000000000000),
 ( 1.000000000000000000, 0.7061401876506447906, 1.000000000000000000),
 ( 1.000000000000000000, 0.7073403273859646401, 1.000000000000000000),
 ( 1.000000000000000000, 0.7071067811865475727, 1.000000000000000000) ) ) 
 REPRESENTATION_ITEM ( '' )  SURFACE ( )  );
#14909=CARTESIAN_POINT ( 'NONE',  ( -1.403716511496708508, -0.03109101116648428989, -0.04439443265226927088 ) ) ;
#14911=( NAMED_UNIT ( * ) SI_UNIT ( $, .STERADIAN. ) SOLID_ANGLE_UNIT ( ) );
#14915=VERTEX_POINT ( 'NONE', #5407 ) ;
#14922=CARTESIAN_POINT ( 'NONE',  ( -2.058365226014241767, -2.288432112655881756, 0.1082654573574225593 ) ) ;
#14930=B_SPLINE_CURVE_WITH_KNOTS ( 'NONE', 3,
 ( #3870, #12036, #7394, #13118 ),
 .UNSPECIFIED., .F., .F.,
 ( 4, 4 ),
 ( 0.02666797036717455383, 0.02905127165838908981 ),
 .UNSPECIFIED. ) ;
#14935=VERTEX_POINT ( 'NONE', #9025 ) ;
#14941=CARTESIAN_POINT ( 'NONE',  ( -2.007191670727864086, -2.769487694035170922, 0.1575912778707037332 ) ) ;
#14945=FACE_OUTER_BOUND ( 'NONE', #13882, .T. ) ;
#14949=CARTESIAN_POINT ( 'NONE',  ( -2.099922416332452801, -2.385393657770976894, -0.1341751375602835972 ) ) ;
#14952=ORIENTED_EDGE ( 'NONE', *, *, #13615, .F. ) ;
#14961=CARTESIAN_POINT ( 'NONE',  ( -1.417802900492933782, -0.04287136159519135126, 0.1968503937007874127 ) ) ;
#14977=EDGE_CURVE ( 'NONE', #14915, #1942, #12306, .T. ) ;
#14979=CARTESIAN_POINT ( 'NONE',  ( -1.293236445124221312, 0.1355266887446167634, -0.03937007874015747977 ) ) ;
#14984=ORIENTED_EDGE ( 'NONE', *, *, #12702, .T. ) ;
#14994=( BOUNDED_SURFACE ( )  B_SPLINE_SURFACE ( 3, 2, ( 
 ( #8318, #1347, #10753 ),
 ( #9575, #9749, #13190 ),
 ( #10816, #6031, #6112 ),
 ( #14353, #8485, #2520 ),
 ( #9670, #13259, #13097 ),
 ( #8546, #13323, #265 ) ),
 .UNSPECIFIED., .F., .F., .T. ) 
 B_SPLINE_SURFACE_WITH_KNOTS ( ( 4, 2, 4 ),
 ( 3, 3 ),
 ( 0.003230360849850198723, 0.003748134328100786311, 0.004265907806351373899 ),
 ( 0.000000000000000000, 1.000000000000000000 ),
 .UNSPECIFIED. ) 
 GEOMETRIC_REPRESENTATION_ITEM ( )  RATIONAL_B_SPLINE_SURFACE ( (
 ( 1.000000000000000000, 0.7048936089935846638, 1.000000000000000000),
 ( 1.000000000000000000, 0.7048811933884949754, 1.000000000000000000),
 ( 1.000000000000000000, 0.7052257929054446262, 1.000000000000000000),
 ( 1.000000000000000000, 0.7061645128344533617, 1.000000000000000000),
 ( 1.000000000000000000, 0.7067576505883527149, 1.000000000000000000),
 ( 1.000000000000000000, 0.7070941911968778859, 1.000000000000000000) ) ) 
 REPRESENTATION_ITEM ( '' )  SURFACE ( )  );
#14998=FACE_OUTER_BOUND ( 'NONE', #9966, .T. ) ;
#14999=DIRECTION ( 'NONE',  ( 1.000000000000000000, 0.000000000000000000, 0.000000000000000000 ) ) ;
#15001=LINE ( 'NONE', #12560, #928 ) ;
#15010=ORIENTED_EDGE ( 'NONE', *, *, #2513, .T. ) ;
#15015=CARTESIAN_POINT ( 'NONE',  ( -1.409916934715107484, -0.04334312390809513804, -0.08366141732283458032 ) ) ;
#15016=CARTESIAN_POINT ( 'NONE',  ( -1.969012519342776324, -2.873039925085861146, 0.1271406377893942174 ) ) ;
#15035=DIRECTION ( 'NONE',  ( -1.000000000000000000, 0.000000000000000000, 0.000000000000000000 ) ) ;
#15036=ORIENTED_EDGE ( 'NONE', *, *, #3431, .T. ) ;
#15037=FACE_OUTER_BOUND ( 'NONE', #3881, .T. ) ;
#15041=ORIENTED_EDGE ( 'NONE', *, *, #1508, .F. ) ;
#15042=LINE ( 'NONE', #781, #1877 ) ;
#15044=CARTESIAN_POINT ( 'NONE',  ( -1.431036756819011213, -0.02829858486107873078, -0.08366141732283458032 ) ) ;
#15047=ORIENTED_EDGE ( 'NONE', *, *, #14417, .T. ) ;
#15051=CARTESIAN_POINT ( 'NONE',  ( -1.293236445124221312, 0.1355266887446167634, -0.05905511811023622659 ) ) ;
#15052=ORIENTED_EDGE ( 'NONE', *, *, #12365, .T. ) ;
#15053=CYLINDRICAL_SURFACE ( 'NONE', #7676, 8.689140419947479543 ) ;
#15054=EDGE_CURVE ( 'NONE', #9631, #9959, #5946, .T. ) ;
#15061=DIRECTION ( 'NONE',  ( -0.5801894994542512451, -0.8144815189573213488, 0.000000000000000000 ) ) ;
#15063=CARTESIAN_POINT ( 'NONE',  ( -1.276200637803905691, -0.1988000726501942539, -0.03937007874015747977 ) ) ;
#15064=CYLINDRICAL_SURFACE ( 'NONE', #2113, 2.795275590551181466 ) ;
#15070=ORIENTED_EDGE ( 'NONE', *, *, #12761, .T. ) ;
#15074=ORIENTED_EDGE ( 'NONE', *, *, #15293, .T. ) ;
#15077=EDGE_CURVE ( 'NONE', #8242, #924, #2954, .T. ) ;
#15079=CARTESIAN_POINT ( 'NONE',  ( -1.984787441652870577, -2.774072082282616591, 0.1775757135651536422 ) ) ;
#15081=LINE ( 'NONE', #12580, #15349 ) ;
#15082=CARTESIAN_POINT ( 'NONE',  ( -1.992382107315057160, -2.752050336136266484, -0.1561691687464108746 ) ) ;
#15083=CARTESIAN_POINT ( 'NONE',  ( -2.024465277823495502, -2.569685212987940837, -0.1523387882505266022 ) ) ;
#15100=CYLINDRICAL_SURFACE ( 'NONE', #1391, 0.01968503937007875723 ) ;
#15103=CARTESIAN_POINT ( 'NONE',  ( -1.591501945092674841, 0.08600752902535303834, 0.1968503937007874127 ) ) ;
#15104=ORIENTED_EDGE ( 'NONE', *, *, #3883, .T. ) ;
#15110=AXIS2_PLACEMENT_3D ( 'NONE', #3556, #12032, #9456 ) ;
#15111=CIRCLE ( 'NONE', #7596, 2.194881889763779181 ) ;
#15112=ORIENTED_EDGE ( 'NONE', *, *, #5135, .F. ) ;
#15116=CARTESIAN_POINT ( 'NONE',  ( -1.981764468582493777, -2.783651129948214731, -0.1771653543307010470 ) ) ;
#15126=CARTESIAN_POINT ( 'NONE',  ( -1.398495881576244493, -0.02731002314121873387, 0.07874015748031495954 ) ) ;
#15130=DIRECTION ( 'NONE',  ( 0.000000000000000000, -1.000000000000000000, 2.208809394877300528E-16 ) ) ;
#15132=CARTESIAN_POINT ( 'NONE',  ( -1.607606114292111199, 0.09732815221480028978, 0.07874015748031495954 ) ) ;
#15135=ORIENTED_EDGE ( 'NONE', *, *, #7552, .F. ) ;
#15136=VECTOR ( 'NONE', #9275, 39.37007874015748143 ) ;
#15139=CARTESIAN_POINT ( 'NONE',  ( 0.7052242655755273093, -1.858423098537180129, -0.1033464566929129108 ) ) ;
#15144=CARTESIAN_POINT ( 'NONE',  ( -1.584115185264708625, 0.1296286773226378586, -0.03937007874015747977 ) ) ;
#15145=DIRECTION ( 'NONE',  ( 0.000000000000000000, -0.000000000000000000, -1.000000000000000000 ) ) ;
#15147=CARTESIAN_POINT ( 'NONE',  ( 0.7052242655755273093, -1.858423098537180129, 0.1968503937007874127 ) ) ;
#15169=CARTESIAN_POINT ( 'NONE',  ( -1.580080891953811628, 0.1020406297922293454, -0.07874015748031495954 ) ) ;
#15170=CARTESIAN_POINT ( 'NONE',  ( -1.580080891953811628, 0.1020406297922293454, 0.1968503937007874127 ) ) ;
#15174=FACE_OUTER_BOUND ( 'NONE', #7678, .T. ) ;
#15178=ORIENTED_EDGE ( 'NONE', *, *, #3717, .F. ) ;
#15182=LINE ( 'NONE', #10635, #10594 ) ;
#15186=CARTESIAN_POINT ( 'NONE',  ( -0.05072818602969413060, 0.1683578795566401942, 0.03094016780477576098 ) ) ;
#15188=CARTESIAN_POINT ( 'NONE',  ( -0.07874015748031543138, -0.1682792322177920907, -0.05905511811023622659 ) ) ;
#15191=CARTESIAN_POINT ( 'NONE',  ( -1.899862746731199259, -2.872024215252888535, -0.1471579868410207437 ) ) ;
#15192=ORIENTED_EDGE ( 'NONE', *, *, #1675, .F. ) ;
#15197=ORIENTED_EDGE ( 'NONE', *, *, #14219, .F. ) ;
#15200=ADVANCED_FACE ( 'NONE', ( #5951 ), #13307, .T. ) ;
#15206=CARTESIAN_POINT ( 'NONE',  ( -1.981764765370718440, -2.783650182701201903, 0.1771653543307413203 ) ) ;
#15211=FACE_OUTER_BOUND ( 'NONE', #4186, .T. ) ;
#15215=CARTESIAN_POINT ( 'NONE',  ( -1.181342415325333350, 0.3435647566446739520, 0.03937007874015747977 ) ) ;
#15228=CARTESIAN_POINT ( 'NONE',  ( -0.05260779769176852222, -0.1848037158363092514, 0.03481219553824697888 ) ) ;
#15230=DIRECTION ( 'NONE',  ( 0.9900370584898828819, 0.1408070410764336311, 9.808509035937714109E-16 ) ) ;
#15236=DIRECTION ( 'NONE',  ( -0.000000000000000000, 0.000000000000000000, 1.000000000000000000 ) ) ;
#15238=EDGE_CURVE ( 'NONE', #6320, #9631, #6138, .T. ) ;
#15239=EDGE_LOOP ( 'NONE', ( #3225, #6700, #13717, #11550 ) ) ;
#15240=B_SPLINE_CURVE_WITH_KNOTS ( 'NONE', 3,
 ( #3313, #2144, #3484, #5569, #9201, #9442 ),
 .UNSPECIFIED., .F., .F.,
 ( 4, 2, 4 ),
 ( 0.0002654705156154514491, 0.0005264791512502068564, 0.0007874877868849623720 ),
 .UNSPECIFIED. ) ;
#15244=CARTESIAN_POINT ( 'NONE',  ( -0.2362204724409448231, -0.02638708502139245488, 0.05905511811023622659 ) ) ;
#15247=DIRECTION ( 'NONE',  ( 0.7632379718491706377, 0.6461174802832411190, 0.000000000000000000 ) ) ;
#15250=DIRECTION ( 'NONE',  ( -0.5984233124757364353, -0.8011800915434477144, 0.000000000000000000 ) ) ;
#15252=VERTEX_POINT ( 'NONE', #14805 ) ;
#15254=ORIENTED_EDGE ( 'NONE', *, *, #3852, .T. ) ;
#15256=EDGE_CURVE ( 'NONE', #12712, #14790, #1716, .T. ) ;
#15257=CARTESIAN_POINT ( 'NONE',  ( -1.596030944582043976, 0.1136756404979572949, -0.04477369844321322373 ) ) ;
#15261=CARTESIAN_POINT ( 'NONE',  ( -2.755905511811024056, -2.749515453455440905, 0.1756903148397124803 ) ) ;
#15262=DIRECTION ( 'NONE',  ( -0.000000000000000000, 0.000000000000000000, 1.000000000000000000 ) ) ;
#15264=CARTESIAN_POINT ( 'NONE',  ( -1.923194646138151054, -2.809760929071067892, -0.1734154778929568597 ) ) ;
#15265=ORIENTED_EDGE ( 'NONE', *, *, #1110, .F. ) ;
#15276=EDGE_CURVE ( 'NONE', #3617, #9786, #12858, .T. ) ;
#15284=CARTESIAN_POINT ( 'NONE',  ( -0.07002599089419499212, 0.1451652216336531409, 0.05905511811023622659 ) ) ;
#15286=ORIENTED_EDGE ( 'NONE', *, *, #1071, .F. ) ;
#15293=EDGE_CURVE ( 'NONE', #13738, #4902, #8470, .T. ) ;
#15296=CARTESIAN_POINT ( 'NONE',  ( -0.03608642540485051259, 0.1707537476062188919, -0.01804586331702247651 ) ) ;
#15309=ORIENTED_EDGE ( 'NONE', *, *, #12662, .T. ) ;
#15311=ORIENTED_EDGE ( 'NONE', *, *, #2960, .F. ) ;
#15314=CARTESIAN_POINT ( 'NONE',  ( -2.087029306903609438, -1.707904051420249480, 0.08366141732283424726 ) ) ;
#15316=CARTESIAN_POINT ( 'NONE',  ( -1.919797936996253451, -2.887775577793183945, 0.1348761084896591966 ) ) ;
#15324=CARTESIAN_POINT ( 'NONE',  ( -2.086995670982084050, -1.707489817804680232, -0.08366141732283374766 ) ) ;
#15325=DIRECTION ( 'NONE',  ( 0.000000000000000000, 1.000000000000000000, 2.183568011719057743E-16 ) ) ;
#15328=EDGE_LOOP ( 'NONE', ( #2709, #10692, #12654, #10581 ) ) ;
#15329=ORIENTED_EDGE ( 'NONE', *, *, #2599, .F. ) ;
#15331=CARTESIAN_POINT ( 'NONE',  ( -0.06997329305368624186, 0.1451708428228431214, 0.05905511811023621271 ) ) ;
#15344=VERTEX_POINT ( 'NONE', #12046 ) ;
#15345=EDGE_CURVE ( 'NONE', #9943, #14086, #4462, .T. ) ;
#15349=VECTOR ( 'NONE', #6695, 39.37007874015748143 ) ;
#15354=CARTESIAN_POINT ( 'NONE',  ( -1.928486289398714915, -2.940034385472957812, 0.05833844333314246872 ) ) ;
#15356=CARTESIAN_POINT ( 'NONE',  ( -1.888479416392070398, -2.900872351736208277, 0.1227802583590561630 ) ) ;
#15361=CIRCLE ( 'NONE', #6075, 0.01968503937007875723 ) ;
#15364=CARTESIAN_POINT ( 'NONE',  ( -1.607606114292111199, 0.09732815221480028978, 0.07874015748031495954 ) ) ;
#15370=B_SPLINE_CURVE_WITH_KNOTS ( 'NONE', 3,
 ( #2094, #9390, #9236, #8282, #14169, #5759, #12993, #1950, #13934, #15188 ),
 .UNSPECIFIED., .F., .F.,
 ( 4, 2, 2, 2, 4 ),
 ( 0.000000000000000000, 0.0006596926164930297203, 0.001319385232986059441, 0.001979077849479089161, 0.002638770465972118881 ),
 .UNSPECIFIED. ) ;
#15371=ORIENTED_EDGE ( 'NONE', *, *, #12961, .T. ) ;
#15374=FACE_OUTER_BOUND ( 'NONE', #5598, .T. ) ;
#15375=VECTOR ( 'NONE', #8500, 39.37007874015748143 ) ;
#15378=CARTESIAN_POINT ( 'NONE',  ( -1.607606114292111643, 0.09732815221480056733, -0.07528735249397262852 ) ) ;
#15381=DIRECTION ( 'NONE',  ( 1.000000000000000000, -0.000000000000000000, -0.000000000000000000 ) ) ;
#15390=VECTOR ( 'NONE', #10360, 39.37007874015748143 ) ;
#15412=DIRECTION ( 'NONE',  ( 1.000000000000000000, 0.000000000000000000, 0.000000000000000000 ) ) ;
#15414=VERTEX_POINT ( 'NONE', #10782 ) ;
#15416=VERTEX_POINT ( 'NONE', #5128 ) ;
#15424=DIRECTION ( 'NONE',  ( 1.000000000000000000, 0.000000000000000000, 0.000000000000000000 ) ) ;
#15430=LINE ( 'NONE', #8048, #2607 ) ;
#15438=CARTESIAN_POINT ( 'NONE',  ( -1.987684632567998877, -2.764755981110976091, 0.1771653543306854761 ) ) ;
#15444=CARTESIAN_POINT ( 'NONE',  ( -1.949178430106353499, -2.798437798732091419, 0.1753388726975497469 ) ) ;
#15451=ORIENTED_EDGE ( 'NONE', *, *, #7757, .F. ) ;
#15452=TOROIDAL_SURFACE ( 'NONE', #4929, 0.2303149606299203511, 0.01968503937007873988 ) ;
#15462=CARTESIAN_POINT ( 'NONE',  ( -1.417133371508829898, -0.01083197275114198763, 0.06860104880227285706 ) ) ;
#15467=CARTESIAN_POINT ( 'NONE',  ( -1.185322955811905166, 0.3350001079061992182, 0.05695403563116168549 ) ) ;
#15468=EDGE_LOOP ( 'NONE', ( #1674, #6232, #15286, #11989, #3291 ) ) ;
#15513=COLOUR_RGB('Sky Blue',0.24,0.69,0.87);
#15514=FILL_AREA_STYLE_COLOUR('',#15513);
#15515=FILL_AREA_STYLE('',(#15514));
#15516=SURFACE_STYLE_FILL_AREA(#15515);
#15517=SURFACE_SIDE_STYLE('',(#15516));
#15518=SURFACE_STYLE_USAGE(.BOTH.,#15517);
#15519=PRESENTATION_STYLE_ASSIGNMENT((#15518));
ENDSEC;
END-ISO-10303-21;
